ISO-10303-21;
HEADER;
FILE_DESCRIPTION (('STEP AP214'),
    '1' );
FILE_NAME ('hand wheel.step',
    '2026-10-26T19:46:16',
    ( '' ),
    ( '' ),
    'SwSTEP 2.0',
    'SolidWorks 2025',
    '' );
FILE_SCHEMA (( 'AUTOMOTIVE_DESIGN' ));
ENDSEC;

DATA;
#3=VERTEX_POINT ( 'NONE', #4394 ) ;
#33=DIRECTION ( 'NONE',  ( 0.000000000000000000, 0.000000000000000000, 1.000000000000000000 ) ) ;
#92=CARTESIAN_POINT ( 'NONE',  ( -5.000000000000000888, 53.34243969459547685, -47.33397984627131905 ) ) ;
#99=CARTESIAN_POINT ( 'NONE',  ( 13.99999999999999822, 2.249999999994893862, 7.677076266393539683 ) ) ;
#104=CARTESIAN_POINT ( 'NONE',  ( 5.000000000000000000, 10.43216530810821219, 65.93415491242824089 ) ) ;
#105=CARTESIAN_POINT ( 'NONE',  ( 5.000000000000000888, 66.79063484153816432, -23.29724706625311370 ) ) ;
#115=CARTESIAN_POINT ( 'NONE',  ( -4.999999999999999112, -67.53158052529141742, -22.66975313813551907 ) ) ;
#148=CARTESIAN_POINT ( 'NONE',  ( 0.3752463838878496993, -10.12385607954436928, 70.07152133708838448 ) ) ;
#183=CARTESIAN_POINT ( 'NONE',  ( -0.4368895104449371236, 51.14729664189285785, -48.52014062454940557 ) ) ;
#226=CARTESIAN_POINT ( 'NONE',  ( 3.373128826976368178, -10.27267468567300668, -63.92035228378879452 ) ) ;
#253=DIRECTION ( 'NONE',  ( 1.000000000000000000, -0.000000000000000000, 0.000000000000000000 ) ) ;
#259=CARTESIAN_POINT ( 'NONE',  ( -3.511653767260603853, -51.69076377080480711, 48.72852442694462383 ) ) ;
#261=PLANE ( 'NONE',  #994 ) ;
#298=CARTESIAN_POINT ( 'NONE',  ( -0.8721677472748831095, -16.44158143986581422, -68.58266913489941885 ) ) ;
#301=CARTESIAN_POINT ( 'NONE',  ( -1.736494649845399918, -51.27805538754612513, -48.57014059985662868 ) ) ;
#307=EDGE_LOOP ( 'NONE', ( #31448, #30350, #12542, #61216 ) ) ;
#314=CARTESIAN_POINT ( 'NONE',  ( -5.000000000000000000, -50.64189880742115690, 41.08656465431877791 ) ) ;
#321=CARTESIAN_POINT ( 'NONE',  ( -5.000000000000000000, -10.28295106684163684, 65.17663434001590872 ) ) ;
#339=FACE_OUTER_BOUND ( 'NONE', #9097, .T. ) ;
#355=CARTESIAN_POINT ( 'NONE',  ( -5.000000000000000000, -53.20585484986825975, 47.69738026034712419 ) ) ;
#376=CARTESIAN_POINT ( 'NONE',  ( -2.266287154879899290, 60.33498852648347821, 22.96738997677451977 ) ) ;
#383=DIRECTION ( 'NONE',  ( 0.000000000000000000, -0.5207998305029613029, -0.8536788251726096233 ) ) ;
#385=CARTESIAN_POINT ( 'NONE',  ( 5.000000000000000000, 16.14408868864073554, 27.96238185062412640 ) ) ;
#410=CARTESIAN_POINT ( 'NONE',  ( -4.330454160168800470, 16.29811171461321706, -69.49285720719208825 ) ) ;
#460=AXIS2_PLACEMENT_3D ( 'NONE', #38862, #22233, #61866 ) ;
#461=CARTESIAN_POINT ( 'NONE',  ( -4.999999999999998224, 53.32026166094924235, -44.27875806161890182 ) ) ;
#475=CARTESIAN_POINT ( 'NONE',  ( 5.000000000000000888, 62.69792629052230382, -24.03557775816830500 ) ) ;
#477=ORIENTED_EDGE ( 'NONE', *, *, #61037, .F. ) ;
#501=( BOUNDED_SURFACE ( )  B_SPLINE_SURFACE ( 3, 2, ( 
 ( #20909, #43929, #9609 ),
 ( #55637, #25068, #36784 ),
 ( #59794, #25441, #71462 ),
 ( #14117, #71837, #20153 ),
 ( #60529, #31864, #51074 ),
 ( #74087, #61658, #15989 ),
 ( #9976, #57120, #62023 ),
 ( #11464, #4321, #45050 ),
 ( #21280, #34498, #27310 ),
 ( #39020, #22386, #50326 ),
 ( #73713, #34119, #16726 ),
 ( #33745, #39752, #3953 ),
 ( #63136, #10347, #68060 ),
 ( #21651, #45407, #17106 ),
 ( #28063, #22764, #33372 ),
 ( #33007, #62387, #56373 ),
 ( #68423, #4693, #56008 ),
 ( #39388, #73347, #26941 ) ),
 .UNSPECIFIED., .F., .F., .T. ) 
 B_SPLINE_SURFACE_WITH_KNOTS ( ( 4, 2, 2, 2, 2, 2, 2, 2, 4 ),
 ( 3, 3 ),
 ( 0.04202945594034800114, 0.04396162471218434398, 0.04589379348402068681, 0.04782596225585702965, 0.04975813102769336554, 0.05169029979952970144, 0.05265638418544787286, 0.05362246857136604428, 0.05748680611503872995 ),
 ( 0.000000000000000000, 1.000000000000000000 ),
 .UNSPECIFIED. ) 
 GEOMETRIC_REPRESENTATION_ITEM ( )  RATIONAL_B_SPLINE_SURFACE ( (
 ( 1.000000000000000000, 0.6241276099607504513, 1.000000000000000000),
 ( 1.000000000000000000, 0.6218761496800027100, 1.000000000000000000),
 ( 1.000000000000000000, 0.6198047272363174098, 1.000000000000000000),
 ( 1.000000000000000000, 0.6161935119824322182, 1.000000000000000000),
 ( 1.000000000000000000, 0.6146642324080623387, 1.000000000000000000),
 ( 1.000000000000000000, 0.6121850116870836134, 1.000000000000000000),
 ( 1.000000000000000000, 0.6112350889398197040, 1.000000000000000000),
 ( 1.000000000000000000, 0.6099522725974151349, 1.000000000000000000),
 ( 1.000000000000000000, 0.6096208180308361202, 1.000000000000000000),
 ( 1.000000000000000000, 0.6096183796348998429, 1.000000000000000000),
 ( 1.000000000000000000, 0.6099422200100823588, 1.000000000000000000),
 ( 1.000000000000000000, 0.6109087447823940975, 1.000000000000000000),
 ( 1.000000000000000000, 0.6113123981688524111, 1.000000000000000000),
 ( 1.000000000000000000, 0.6122677719809250796, 1.000000000000000000),
 ( 1.000000000000000000, 0.6128199619021360567, 1.000000000000000000),
 ( 1.000000000000000000, 0.6159350830264649357, 1.000000000000000000),
 ( 1.000000000000000000, 0.6195556778516543295, 1.000000000000000000),
 ( 1.000000000000000000, 0.6241278272307883013, 1.000000000000000000) ) ) 
 REPRESENTATION_ITEM ( '' )  SURFACE ( )  );
#514=CARTESIAN_POINT ( 'NONE',  ( -0.3794862803136856422, -10.12385276104027376, 70.07165850195889334 ) ) ;
#594=CARTESIAN_POINT ( 'NONE',  ( 5.000000000000000000, -10.26105934116143281, -64.40045319026697257 ) ) ;
#617=DIRECTION ( 'NONE',  ( 1.000000000000000000, -0.000000000000000000, -0.000000000000000000 ) ) ;
#631=CARTESIAN_POINT ( 'NONE',  ( -4.336811714532579742, -52.00708776949259260, 48.85034107299725292 ) ) ;
#638=CARTESIAN_POINT ( 'NONE',  ( -5.000000000000000000, 16.24494643555759410, 69.83755725260752456 ) ) ;
#660=B_SPLINE_CURVE_WITH_KNOTS ( 'NONE', 3,
 ( #33434, #4754, #74144, #61716, #22080, #21344, #10036, #57179, #33072, #68119, #44364, #4014, #26626, #62818, #16413, #27370, #67377, #56068, #50389, #72664, #62445, #73405 ),
 .UNSPECIFIED., .F., .F.,
 ( 4, 2, 2, 2, 2, 2, 2, 2, 2, 2, 4 ),
 ( 0.000000000000000000, 0.001156727053362476953, 0.001735090580043700901, 0.002313454106724924849, 0.003470181160087385322, 0.004048544686768620546, 0.004626908213449854902, 0.005783635266812324482, 0.006940362320174794063, 0.008097089373537263643, 0.009253816426899734091 ),
 .UNSPECIFIED. ) ;
#665=DIRECTION ( 'NONE',  ( 1.000000000000000000, -0.000000000000000000, 0.000000000000000000 ) ) ;
#673=CARTESIAN_POINT ( 'NONE',  ( -2.160335347077957380, -51.35526406371566566, -48.59969451235782856 ) ) ;
#743=EDGE_CURVE ( 'NONE', #22266, #8905, #71825, .T. ) ;
#747=CARTESIAN_POINT ( 'NONE',  ( 3.223881452106005518, 60.47365957010377002, 23.05198836891398528 ) ) ;
#750=CARTESIAN_POINT ( 'NONE',  ( -14.00000000000000178, 0.000000000000000000, 0.000000000000000000 ) ) ;
#778=CARTESIAN_POINT ( 'NONE',  ( 4.336811714531698669, 16.30209246799961065, -69.46462972172668060 ) ) ;
#801=LINE ( 'NONE', #7551, #68493 ) ;
#833=CARTESIAN_POINT ( 'NONE',  ( -0.8761883848948450737, 16.44150283900180654, -68.58316157021027948 ) ) ;
#836=( NAMED_UNIT ( * ) SI_UNIT ( $, .STERADIAN. ) SOLID_ANGLE_UNIT ( ) );
#844=CARTESIAN_POINT ( 'NONE',  ( 5.000000000000000888, 63.85408791058100064, -24.15552328276435290 ) ) ;
#921=CARTESIAN_POINT ( 'NONE',  ( -1.739508062057944393, 51.27839935804234983, -48.57027215863329417 ) ) ;
#976=CARTESIAN_POINT ( 'NONE',  ( 3.511653767258654302, 51.69076377080344997, 48.72852442694496489 ) ) ;
#994=AXIS2_PLACEMENT_3D ( 'NONE', #5165, #33472, #5905 ) ;
#995=CARTESIAN_POINT ( 'NONE',  ( 5.000000000000000000, -65.19475225706619881, -23.98307544244962841 ) ) ;
#999=CARTESIAN_POINT ( 'NONE',  ( -3.223881452105248790, 60.47365957010899962, -23.05198836891563730 ) ) ;
#1115=CARTESIAN_POINT ( 'NONE',  ( 3.074111742570772243, 67.95395293240336798, 20.32712440775923568 ) ) ;
#1116=CARTESIAN_POINT ( 'NONE',  ( 5.000000000000000000, -68.60357193678713372, 20.85024232999320404 ) ) ;
#1129=VERTEX_POINT ( 'NONE', #51401 ) ;
#1143=CARTESIAN_POINT ( 'NONE',  ( -0.3794862803194745116, 10.12385276104027376, -70.07165850195889334 ) ) ;
#1176=CARTESIAN_POINT ( 'NONE',  ( 5.000000000000000000, -16.24494643555759410, 69.83755725260752456 ) ) ;
#1275=CARTESIAN_POINT ( 'NONE',  ( 13.99999999999999822, 2.249999999994893862, 10.23492587299426404 ) ) ;
#1343=CARTESIAN_POINT ( 'NONE',  ( 4.336811714528937323, 52.00708776950180123, 48.85034107298458395 ) ) ;
#1357=CARTESIAN_POINT ( 'NONE',  ( 3.369429374625368734, -60.49191766694071504, 23.06312700027830687 ) ) ;
#1372=DIRECTION ( 'NONE',  ( -1.000000000000000000, -0.000000000000000000, -0.000000000000000000 ) ) ;
#1408=CARTESIAN_POINT ( 'NONE',  ( -4.217983994790169611, -51.98644305214799743, -48.84278562423040171 ) ) ;
#1458=CARTESIAN_POINT ( 'NONE',  ( -5.000000000000000000, 61.58609660504401973, -23.68302032025023252 ) ) ;
#1486=CARTESIAN_POINT ( 'NONE',  ( 0.7581620860322625388, 65.76154746682546204, 26.27794529688427971 ) ) ;
#1520=CARTESIAN_POINT ( 'NONE',  ( -1.308779242311570501, 10.28008949575769293, -63.61387346695496348 ) ) ;
#1540=CARTESIAN_POINT ( 'NONE',  ( -4.737866951563398210, -52.21905653845826834, -48.93292554254780669 ) ) ;
#1548=CARTESIAN_POINT ( 'NONE',  ( 2.666560895877943341E-14, -16.44602605510714355, 68.55492853905353456 ) ) ;
#1551=AXIS2_PLACEMENT_3D ( 'NONE', #8041, #30317, #12948 ) ;
#1704=ORIENTED_EDGE ( 'NONE', *, *, #52857, .F. ) ;
#1778=CARTESIAN_POINT ( 'NONE',  ( 5.000000000000000000, 14.89980876190738002, -69.94558486267359854 ) ) ;
#1816=CARTESIAN_POINT ( 'NONE',  ( -4.999999999999998224, -52.16438407847157777, 42.28020805311177810 ) ) ;
#1826=CARTESIAN_POINT ( 'NONE',  ( 5.000000000000000000, 16.14408868864073554, -27.96238185062347981 ) ) ;
#1841=CARTESIAN_POINT ( 'NONE',  ( -0.7509181236786398594, 65.76106071587237523, 26.27764834701797980 ) ) ;
#1867=CARTESIAN_POINT ( 'NONE',  ( -1.877992804784532677, 10.12031740952137859, -70.21778636471140089 ) ) ;
#1880=DIRECTION ( 'NONE',  ( 0.000000000000000000, -0.8536788251726096233, 0.5207998305029611918 ) ) ;
#1889=CARTESIAN_POINT ( 'NONE',  ( -6.298842414731647743, -51.07418104651127777, -41.32239042995288969 ) ) ;
#1921=CARTESIAN_POINT ( 'NONE',  ( -2.967813307894019431E-11, 16.44602605510714355, -68.55492853905352035 ) ) ;
#1930=ORIENTED_EDGE ( 'NONE', *, *, #71883, .T. ) ;
#2006=DIRECTION ( 'NONE',  ( 0.000000000000000000, -0.02418647091589873691, -0.9997074645238147594 ) ) ;
#2037=ORIENTED_EDGE ( 'NONE', *, *, #24852, .T. ) ;
#2072=CARTESIAN_POINT ( 'NONE',  ( -5.000000000000000000, -52.35862550122958936, 48.98731492261398301 ) ) ;
#2129=EDGE_LOOP ( 'NONE', ( #23480, #45274, #13668, #9620 ) ) ;
#2136=CARTESIAN_POINT ( 'NONE',  ( 5.000000000000000000, 11.00774715070946108, -67.37702390743022818 ) ) ;
#2156=DIRECTION ( 'NONE',  ( 1.000000000000000000, 0.000000000000000000, -0.000000000000000000 ) ) ;
#2178=CARTESIAN_POINT ( 'NONE',  ( -5.000000000000000000, -52.63770595436704269, 42.88862352055295446 ) ) ;
#2187=CARTESIAN_POINT ( 'NONE',  ( -5.000000000000000000, 16.24494643555759410, 69.83755725260752456 ) ) ;
#2201=CARTESIAN_POINT ( 'NONE',  ( -1.882291019709217084, 65.87523470714100426, 26.34730193751279614 ) ) ;
#2210=VERTEX_POINT ( 'NONE', #69563 ) ;
#2224=CARTESIAN_POINT ( 'NONE',  ( 5.000000000000001776, -10.38759426015435317, -65.74583990312707726 ) ) ;
#2226=EDGE_CURVE ( 'NONE', #69045, #31632, #19585, .T. ) ;
#2272=DIRECTION ( 'NONE',  ( 0.000000000000000000, 0.000000000000000000, -1.000000000000000000 ) ) ;
#2307=EDGE_CURVE ( 'NONE', #34668, #56998, #42953, .T. ) ;
#2380=CARTESIAN_POINT ( 'NONE',  ( 1.781595147087400743, 51.28498669164871870, -48.57279346520080310 ) ) ;
#2519=DIRECTION ( 'NONE',  ( 0.000000000000000000, 0.000000000000000000, -1.000000000000000000 ) ) ;
#2521=ADVANCED_FACE ( 'NONE', ( #45253 ), #73185, .F. ) ;
#2552=CARTESIAN_POINT ( 'NONE',  ( -4.999999999999999112, -53.55923425356129286, 45.42020841079056481 ) ) ;
#2579=CARTESIAN_POINT ( 'NONE',  ( 5.000000000000000000, 68.48952624890506513, 21.22548696402972013 ) ) ;
#2622=LINE ( 'NONE', #53564, #60954 ) ;
#2665=AXIS2_PLACEMENT_3D ( 'NONE', #14325, #6562, #8684 ) ;
#2680=ORIENTED_EDGE ( 'NONE', *, *, #9152, .F. ) ;
#2758=CARTESIAN_POINT ( 'NONE',  ( 4.465349678513709009, 56.41423509509570522, -44.23558526900735899 ) ) ;
#2765=ORIENTED_EDGE ( 'NONE', *, *, #72935, .F. ) ;
#2769=VERTEX_POINT ( 'NONE', #21964 ) ;
#2813=CARTESIAN_POINT ( 'NONE',  ( -5.000000000000000000, 51.88457047716679682, 42.00159762951515319 ) ) ;
#2857=CARTESIAN_POINT ( 'NONE',  ( -3.407298021519497233, 68.04056125361158536, -20.39715949456229183 ) ) ;
#2947=CARTESIAN_POINT ( 'NONE',  ( -2.219371606097053640, 67.78152867896183409, 20.18750705526327138 ) ) ;
#3034=CYLINDRICAL_SURFACE ( 'NONE', #10067, 5.000000000000000888 ) ;
#3067=DIRECTION ( 'NONE',  ( -0.000000000000000000, 0.9997074645238147594, 0.02418647091589873691 ) ) ;
#3120=VERTEX_POINT ( 'NONE', #1116 ) ;
#3124=EDGE_CURVE ( 'NONE', #17271, #6891, #66315, .T. ) ;
#3142=EDGE_CURVE ( 'NONE', #53254, #22266, #27614, .T. ) ;
#3159=AXIS2_PLACEMENT_3D ( 'NONE', #73508, #35037, #28609 ) ;
#3199=CARTESIAN_POINT ( 'NONE',  ( 5.000000000000000000, 32.28817737728141424, 3.295974604355933479E-13 ) ) ;
#3248=ORIENTED_EDGE ( 'NONE', *, *, #58752, .T. ) ;
#3271=CARTESIAN_POINT ( 'NONE',  ( -2.266287154879861987, -60.33498852648448008, -22.96738997677460858 ) ) ;
#3315=CARTESIAN_POINT ( 'NONE',  ( 4.999999999999998224, -53.50647209750589894, 45.02947987234036020 ) ) ;
#3323=CARTESIAN_POINT ( 'NONE',  ( 4.999999999999999112, 65.00653492603716188, 24.02639942437878773 ) ) ;
#3344=CARTESIAN_POINT ( 'NONE',  ( 4.999999999999999112, -11.44657803507905491, -68.01244171956638240 ) ) ;
#3376=CARTESIAN_POINT ( 'NONE',  ( 3.728321214240318149, -56.13798660958080688, -44.08488161416449458 ) ) ;
#3378=DIRECTION ( 'NONE',  ( 0.000000000000000000, 0.000000000000000000, -1.000000000000000000 ) ) ;
#3411=CARTESIAN_POINT ( 'NONE',  ( 13.99999999999999822, -2.250000000005106138, 10.23492587299426404 ) ) ;
#3455=VERTEX_POINT ( 'NONE', #28191 ) ;
#3550=CARTESIAN_POINT ( 'NONE',  ( -5.086519500874237210, -10.26068667857087213, 64.41585657734346171 ) ) ;
#3562=CARTESIAN_POINT ( 'NONE',  ( -5.000000000000000000, 53.35645474066748051, 47.33026262608808565 ) ) ;
#3582=CARTESIAN_POINT ( 'NONE',  ( -5.000000000000000000, -62.31673578527556145, 23.93255728291356021 ) ) ;
#3586=EDGE_LOOP ( 'NONE', ( #23027, #55411, #28461, #49599 ) ) ;
#3587=CARTESIAN_POINT ( 'NONE',  ( -4.999999999999999112, 13.57248045702108818, -69.64920683919132216 ) ) ;
#3641=CARTESIAN_POINT ( 'NONE',  ( 1.877992804783702008, -65.87054549412334836, -26.34444121135540939 ) ) ;
#3670=DIRECTION ( 'NONE',  ( 0.000000000000000000, 0.000000000000000000, -1.000000000000000000 ) ) ;
#3686=AXIS2_PLACEMENT_3D ( 'NONE', #69242, #46593, #22088 ) ;
#3688=ADVANCED_FACE ( 'NONE', ( #49184 ), #12805, .F. ) ;
#3696=ORIENTED_EDGE ( 'NONE', *, *, #73767, .T. ) ;
#3699=CARTESIAN_POINT ( 'NONE',  ( 5.000000000000000888, 68.32828612846134320, 21.58087353894222105 ) ) ;
#3712=AXIS2_PLACEMENT_3D ( 'NONE', #21323, #20946, #9648 ) ;
#3745=ADVANCED_FACE ( 'NONE', ( #11440 ), #51387, .F. ) ;
#3751=CARTESIAN_POINT ( 'NONE',  ( 2.997005883572143592, -55.94527535362117732, -43.97975057404410393 ) ) ;
#3833=B_SPLINE_CURVE_WITH_KNOTS ( 'NONE', 3,
 ( #34560, #28870, #57565, #69240, #52634, #39817, #6614, #68862, #17173, #57943, #17549, #40568 ),
 .UNSPECIFIED., .F., .F.,
 ( 4, 2, 2, 2, 2, 4 ),
 ( 0.000000000000000000, 0.002547658444427992625, 0.005095316888855985250, 0.006369146111069981346, 0.007642975333283978309, 0.01019063377771197050 ),
 .UNSPECIFIED. ) ;
#3856=VERTEX_POINT ( 'NONE', #14533 ) ;
#3858=EDGE_CURVE ( 'NONE', #34067, #29307, #30385, .T. ) ;
#3874=ORIENTED_EDGE ( 'NONE', *, *, #17034, .F. ) ;
#3875=CARTESIAN_POINT ( 'NONE',  ( 3.228176881614474247, -60.48309044411903557, 23.05774181791956678 ) ) ;
#3895=ORIENTED_EDGE ( 'NONE', *, *, #22159, .T. ) ;
#3933=CARTESIAN_POINT ( 'NONE',  ( -3.734423912253595379, -10.10901040137823159, 70.68514270129077204 ) ) ;
#3944=CARTESIAN_POINT ( 'NONE',  ( 5.000000000000000000, 0.000000000000000000, 0.000000000000000000 ) ) ;
#3953=CARTESIAN_POINT ( 'NONE',  ( -2.266287154886498456, -10.27715108473166694, -63.73532778936405663 ) ) ;
#3955=AXIS2_PLACEMENT_3D ( 'NONE', #52582, #57134, #18247 ) ;
#3989=VERTEX_POINT ( 'NONE', #638 ) ;
#4014=CARTESIAN_POINT ( 'NONE',  ( 5.000000000000000888, 53.31073972600231770, -44.28411094575927365 ) ) ;
#4026=CARTESIAN_POINT ( 'NONE',  ( 2.216418498321875319, -67.77535163244932903, -20.18253627485106705 ) ) ;
#4033=CARTESIAN_POINT ( 'NONE',  ( -5.000000000000000000, -12.24744670179871164, -68.85644987591972210 ) ) ;
#4038=EDGE_LOOP ( 'NONE', ( #32213, #36167, #62701, #46097 ) ) ;
#4049=CARTESIAN_POINT ( 'NONE',  ( 2.591411123053486421, -50.09422832877199738, 40.78779037275008790 ) ) ;
#4070=CARTESIAN_POINT ( 'NONE',  ( -1.347111479062088207E-15, 0.000000000000000000, 0.000000000000000000 ) ) ;
#4080=CARTESIAN_POINT ( 'NONE',  ( -3.407298021510799302, -16.35582233947175013, 69.12343428065700834 ) ) ;
#4089=CARTESIAN_POINT ( 'NONE',  ( 1.688721909672333155, 60.25432409644750464, -22.91817940688229527 ) ) ;
#4106=CARTESIAN_POINT ( 'NONE',  ( 2.160335347077974699, -51.35526406371597830, 48.59969451235745197 ) ) ;
#4150=CARTESIAN_POINT ( 'NONE',  ( 1.781595147095969001, 16.42277972781688433, 68.70049804031583562 ) ) ;
#4173=CARTESIAN_POINT ( 'NONE',  ( -4.465384415997284862, 56.41424811512398207, -44.23559237190911375 ) ) ;
#4180=ORIENTED_EDGE ( 'NONE', *, *, #50871, .T. ) ;
#4221=DIRECTION ( 'NONE',  ( 0.000000000000000000, -0.8778652960885044987, 0.4789076340208435756 ) ) ;
#4249=CARTESIAN_POINT ( 'NONE',  ( 5.126144196591281066, -68.65853088339385124, 20.89430926783037634 ) ) ;
#4278=EDGE_CURVE ( 'NONE', #58637, #20164, #37472, .T. ) ;
#4298=VERTEX_POINT ( 'NONE', #27465 ) ;
#4313=CARTESIAN_POINT ( 'NONE',  ( -5.000000000000001776, 53.53174224766548406, 46.57871628774437056 ) ) ;
#4314=LINE ( 'NONE', #62377, #30835 ) ;
#4321=CARTESIAN_POINT ( 'NONE',  ( 0.7581620860255156025, -10.12340554704895901, -70.09014334688596648 ) ) ;
#4330=VERTEX_POINT ( 'NONE', #21801 ) ;
#4337=CARTESIAN_POINT ( 'NONE',  ( -5.000000000000000888, 10.54112798502250214, -66.30787999718575065 ) ) ;
#4391=CARTESIAN_POINT ( 'NONE',  ( -0.7509181236779562951, -65.76106071587255997, -26.27764834702091434 ) ) ;
#4394=CARTESIAN_POINT ( 'NONE',  ( 5.000000000000000000, -29.68417822476656553, 4.268394125862918997 ) ) ;
#4432=DIRECTION ( 'NONE',  ( 1.000000000000000000, -0.000000000000000000, -0.000000000000000000 ) ) ;
#4501=CARTESIAN_POINT ( 'NONE',  ( 1.882291019708790536, -55.75505015263587438, -43.87597576789006126 ) ) ;
#4509=ORIENTED_EDGE ( 'NONE', *, *, #29684, .T. ) ;
#4538=CARTESIAN_POINT ( 'NONE',  ( 5.086519500873676769, 50.65542486323139570, -41.09394361258735984 ) ) ;
#4544=DIRECTION ( 'NONE',  ( 0.000000000000000000, 0.8778652960885079404, -0.4789076340208374138 ) ) ;
#4616=CARTESIAN_POINT ( 'NONE',  ( -0.4501631047672374208, -67.59340899456745433, 20.03485802339921307 ) ) ;
#4618=CARTESIAN_POINT ( 'NONE',  ( 4.999999999999999112, 51.89737250574476235, 42.00009673807167587 ) ) ;
#4620=CARTESIAN_POINT ( 'NONE',  ( 0.8761883848702602950, 67.61551161115370689, 20.05282165013497320 ) ) ;
#4628=DIRECTION ( 'NONE',  ( 0.000000000000000000, 0.02418647091589873691, 0.9997074645238147594 ) ) ;
#4653=ADVANCED_FACE ( 'NONE', ( #42124 ), #66305, .T. ) ;
#4661=VERTEX_POINT ( 'NONE', #7445 ) ;
#4673=CARTESIAN_POINT ( 'NONE',  ( 3.544144923088449861, -10.27124247550364977, 63.97955030412197175 ) ) ;
#4693=CARTESIAN_POINT ( 'NONE',  ( -3.728321214207148238, -10.10963409588650919, -70.65936332836869838 ) ) ;
#4711=CARTESIAN_POINT ( 'NONE',  ( -5.000000000000000000, 15.86295220590816513, -69.92641310672760824 ) ) ;
#4731=EDGE_CURVE ( 'NONE', #72830, #47939, #30813, .T. ) ;
#4754=CARTESIAN_POINT ( 'NONE',  ( 4.999999999999995559, 50.98531617258545623, -41.27391139027573530 ) ) ;
#4765=CARTESIAN_POINT ( 'NONE',  ( -7.456155213548121274, 51.58724325107812803, 41.60228463193340787 ) ) ;
#4767=FACE_OUTER_BOUND ( 'NONE', #41761, .T. ) ;
#4788=CARTESIAN_POINT ( 'NONE',  ( 3.734423912251746636, -56.16062404875972902, 44.09723116536054732 ) ) ;
#4851=CARTESIAN_POINT ( 'NONE',  ( -3.107148544787702027E-14, -51.14729664189371761, 48.52014062455021559 ) ) ;
#4853=VERTEX_POINT ( 'NONE', #31933 ) ;
#4858=ORIENTED_EDGE ( 'NONE', *, *, #9991, .T. ) ;
#4889=CARTESIAN_POINT ( 'NONE',  ( 4.104248244565246395, 10.10575198620100856, 70.81982386211579694 ) ) ;
#4912=CARTESIAN_POINT ( 'NONE',  ( 0.4368895104442291899, -67.59332269699979179, 20.03478791450223895 ) ) ;
#4918=CARTESIAN_POINT ( 'NONE',  ( -4.336811714531673800, 52.00708776950106227, -48.85034107298749007 ) ) ;
#4944=ORIENTED_EDGE ( 'NONE', *, *, #47539, .F. ) ;
#4960=MECHANICAL_DESIGN_GEOMETRIC_PRESENTATION_REPRESENTATION('',(#72431),#25446);
#4972=DIRECTION ( 'NONE',  ( 1.000000000000000000, 0.000000000000000000, 0.000000000000000000 ) ) ;
#4975=VECTOR ( 'NONE', #58243, 1000.000000000000000 ) ;
#4990=CARTESIAN_POINT ( 'NONE',  ( 1.739508062058950699, 67.70228923712218716, -20.12326043015055177 ) ) ;
#4992=CARTESIAN_POINT ( 'NONE',  ( -5.000000000000000888, 53.53067326687928329, -46.58593137613046764 ) ) ;
#4994=CARTESIAN_POINT ( 'NONE',  ( 7.456209740496413829, -61.82228229130296882, 23.87473629694196831 ) ) ;
#4995=ADVANCED_FACE ( 'NONE', ( #17175 ), #52268, .F. ) ;
#5006=LINE ( 'NONE', #56689, #48472 ) ;
#5010=ORIENTED_EDGE ( 'NONE', *, *, #19179, .F. ) ;
#5031=SHAPE_REPRESENTATION ( 'hand wheel', ( #57354 ), #64563 ) ;
#5048=ADVANCED_FACE ( 'NONE', ( #23214 ), #43403, .T. ) ;
#5049=CARTESIAN_POINT ( 'NONE',  ( 2.997005883567212869, -10.11494357241825526, 70.43990496500141774 ) ) ;
#5062=ORIENTED_EDGE ( 'NONE', *, *, #40069, .T. ) ;
#5159=CARTESIAN_POINT ( 'NONE',  ( 5.000000000000000000, -62.13136467932972806, -23.87699943806472547 ) ) ;
#5163=CARTESIAN_POINT ( 'NONE',  ( -4.737866951563012741, 68.48668487056758636, -20.75656675268732698 ) ) ;
#5165=CARTESIAN_POINT ( 'NONE',  ( 5.000000000000000000, 0.000000000000000000, 0.000000000000000000 ) ) ;
#5262=CARTESIAN_POINT ( 'NONE',  ( 0.6547826978431545708, 10.28110016890869716, 63.57209897671332754 ) ) ;
#5308=CARTESIAN_POINT ( 'NONE',  ( -4.465349678524273003, 10.10202304668574591, -70.97395336192860782 ) ) ;
#5358=CARTESIAN_POINT ( 'NONE',  ( -4.999999999999998224, 52.16438407847190462, -42.28020805311142993 ) ) ;
#5360=CARTESIAN_POINT ( 'NONE',  ( 2.436599634630554068, -67.82108862182708720, 20.21956363438967941 ) ) ;
#5382=CARTESIAN_POINT ( 'NONE',  ( -4.999999999999999112, -64.62627855237427354, -24.10294814404728569 ) ) ;
#5412=CARTESIAN_POINT ( 'NONE',  ( 1.317228840348607655, -10.12208498181994543, 70.14472670972676838 ) ) ;
#5417=ADVANCED_FACE ( 'NONE', ( #18487 ), #7171, .F. ) ;
#5433=CARTESIAN_POINT ( 'NONE',  ( 5.000000000000000000, 10.26105934116143459, -64.40045319026695836 ) ) ;
#5528=CARTESIAN_POINT ( 'NONE',  ( -5.126144196591224222, -52.42426806216685264, 49.01287729762206880 ) ) ;
#5566=CARTESIAN_POINT ( 'NONE',  ( -5.000000000000000000, -16.24494643555759410, -69.83755725260751035 ) ) ;
#5573=AXIS2_PLACEMENT_3D ( 'NONE', #19807, #19436, #41721 ) ;
#5579=PRODUCT_DEFINITION_CONTEXT ( 'detailed design', #51531, 'design' ) ;
#5590=CARTESIAN_POINT ( 'NONE',  ( -5.000000000000000000, -12.55023575007693104, 69.09043692422063998 ) ) ;
#5592=CARTESIAN_POINT ( 'NONE',  ( 4.999999999999999112, -67.91007042436125118, 22.22893179987950774 ) ) ;
#5605=CARTESIAN_POINT ( 'NONE',  ( -1.688721909672325161, 60.25432409644700726, 22.91817940688352451 ) ) ;
#5633=CARTESIAN_POINT ( 'NONE',  ( 7.456155213548131044, 10.23501372118544595, 65.47700548260780806 ) ) ;
#5682=EDGE_LOOP ( 'NONE', ( #48736, #15210, #70349, #71217, #9181 ) ) ;
#5701=PLANE ( 'NONE',  #26937 ) ;
#5728=CARTESIAN_POINT ( 'NONE',  ( -5.000000000000000000, -51.30314553820197432, -41.49361401976533870 ) ) ;
#5749=VECTOR ( 'NONE', #46069, 1000.000000000000000 ) ;
#5780=DIRECTION ( 'NONE',  ( 0.000000000000000000, -0.02418647091589873691, -0.9997074645238147594 ) ) ;
#5788=CARTESIAN_POINT ( 'NONE',  ( -2.620431783929382252, -65.99617417813543341, 26.42108291244370122 ) ) ;
#5858=ORIENTED_EDGE ( 'NONE', *, *, #18276, .F. ) ;
#5881=CARTESIAN_POINT ( 'NONE',  ( 2.219371606097276572, 51.37365828841448234, 48.60677221569496709 ) ) ;
#5887=CARTESIAN_POINT ( 'NONE',  ( 4.999999999999998224, -52.84634075987109014, -43.22150062466552356 ) ) ;
#5903=CARTESIAN_POINT ( 'NONE',  ( -0.6547826978430097977, 60.19560277018368311, -22.88235556322664976 ) ) ;
#5905=DIRECTION ( 'NONE',  ( -0.000000000000000000, 0.000000000000000000, 1.000000000000000000 ) ) ;
#5943=CARTESIAN_POINT ( 'NONE',  ( -2.170320029210515145, -16.41060967376241564, -68.77687409974784316 ) ) ;
#5956=VERTEX_POINT ( 'NONE', #39473 ) ;
#5959=CARTESIAN_POINT ( 'NONE',  ( -5.000000000000000000, -10.43216530810821219, 65.93415491242824089 ) ) ;
#5979=AXIS2_PLACEMENT_3D ( 'NONE', #6558, #14318, #23898 ) ;
#6000=EDGE_LOOP ( 'NONE', ( #3874, #24673, #39924, #17167, #61293 ) ) ;
#6017=CARTESIAN_POINT ( 'NONE',  ( 6.298842414732967576, 61.32333038069117492, 23.57034304878763464 ) ) ;
#6020=CARTESIAN_POINT ( 'NONE',  ( 0.8721677472496979222, -67.61512445009702788, 20.05250736213360341 ) ) ;
#6082=CARTESIAN_POINT ( 'NONE',  ( -4.217983994794604286, 51.98644305214961747, 48.84278562423152437 ) ) ;
#6104=CARTESIAN_POINT ( 'NONE',  ( -5.000000000000000000, -52.85372778481321632, -48.38359481482913083 ) ) ;
#6112=CARTESIAN_POINT ( 'NONE',  ( 5.000000000000001776, 68.60357193678683529, 20.85024232999420946 ) ) ;
#6120=CARTESIAN_POINT ( 'NONE',  ( 4.999999999999999112, 67.53158052529175848, -22.66975313813455273 ) ) ;
#6128=CARTESIAN_POINT ( 'NONE',  ( -4.999999999999998224, -62.69792629052194144, -24.03557775816916120 ) ) ;
#6159=CARTESIAN_POINT ( 'NONE',  ( 1.296342370391023291, -10.28012030475504091, 63.61260002839785699 ) ) ;
#6162=CARTESIAN_POINT ( 'NONE',  ( -14.00000000000000178, -2.250000000005106138, 7.677076266390546522 ) ) ;
#6191=VERTEX_POINT ( 'NONE', #52285 ) ;
#6194=CARTESIAN_POINT ( 'NONE',  ( -2.978189300774432354E-14, -67.59332269700065865, -20.03478791450352858 ) ) ;
#6195=CARTESIAN_POINT ( 'NONE',  ( -3.428378827818324037, 51.66489094707790031, -48.71857030467307936 ) ) ;
#6205=VERTEX_POINT ( 'NONE', #11917 ) ;
#6263=CARTESIAN_POINT ( 'NONE',  ( 4.999999999999999112, -53.34243969459480894, -47.33397984627203670 ) ) ;
#6319=DIRECTION ( 'NONE',  ( -1.000000000000000000, 0.000000000000000000, -0.000000000000000000 ) ) ;
#6338=CARTESIAN_POINT ( 'NONE',  ( 0.000000000000000000, 0.000000000000000000, -17.50000000000000000 ) ) ;
#6342=CARTESIAN_POINT ( 'NONE',  ( 5.000000000000001776, -67.10993666412744574, 23.06595724273596204 ) ) ;
#6370=CARTESIAN_POINT ( 'NONE',  ( -5.000000000000000000, 67.91996363552695470, -22.23680535815822168 ) ) ;
#6400=CARTESIAN_POINT ( 'NONE',  ( 3.428378827818083785, -68.02396499344416725, 20.38382289158473171 ) ) ;
#6415=CARTESIAN_POINT ( 'NONE',  ( 5.000000000000000000, 18.53862685874493010, -23.57305537018094554 ) ) ;
#6419=EDGE_LOOP ( 'NONE', ( #19798, #49970, #20312, #11281 ) ) ;
#6423=CARTESIAN_POINT ( 'NONE',  ( 5.000000000000000000, 16.14408868864073554, 27.96238185062412640 ) ) ;
#6427=CARTESIAN_POINT ( 'NONE',  ( 1.317228840344592422, 10.12208498181939120, -70.14472670972864421 ) ) ;
#6542=CARTESIAN_POINT ( 'NONE',  ( 5.000000000000000000, -16.14408868864072844, 22.96238185062368586 ) ) ;
#6544=VECTOR ( 'NONE', #43700, 1000.000000000000000 ) ;
#6558=CARTESIAN_POINT ( 'NONE',  ( 5.000000000000000000, 0.000000000000000000, 0.000000000000000000 ) ) ;
#6562=DIRECTION ( 'NONE',  ( 1.000000000000000000, -0.000000000000000000, -0.000000000000000000 ) ) ;
#6564=DIRECTION ( 'NONE',  ( 0.000000000000000000, -0.9997074645238147594, 0.02418647091589873691 ) ) ;
#6602=EDGE_CURVE ( 'NONE', #30597, #29307, #73342, .T. ) ;
#6610=CARTESIAN_POINT ( 'NONE',  ( -4.193030820683907756, -10.26769724739506984, -64.12608639927678666 ) ) ;
#6614=CARTESIAN_POINT ( 'NONE',  ( -0.8588954341814950544, -10.28066745654381542, 63.58998442112849858 ) ) ;
#6623=CARTESIAN_POINT ( 'NONE',  ( 3.728321214229567637, 56.13798660961509057, 44.08488161414512518 ) ) ;
#6634=CARTESIAN_POINT ( 'NONE',  ( -1.739508062077480766, -51.27839935804527016, 48.57027215863489999 ) ) ;
#6640=CARTESIAN_POINT ( 'NONE',  ( 5.000000000000000000, -67.66743717231483402, -22.54291394824973338 ) ) ;
#6645=CARTESIAN_POINT ( 'NONE',  ( -2.219371606100991823, -51.37365828841591053, 48.60677221569458339 ) ) ;
#6657=CARTESIAN_POINT ( 'NONE',  ( 5.000000000000000000, -10.42446448370085577, 65.94449134867498685 ) ) ;
#6672=DIRECTION ( 'NONE',  ( 1.000000000000000000, -0.000000000000000000, -0.000000000000000000 ) ) ;
#6687=CARTESIAN_POINT ( 'NONE',  ( -5.000000000000000000, -70.11723469343094450, -28.93519894129240910 ) ) ;
#6697=CARTESIAN_POINT ( 'NONE',  ( -4.999999999999999112, 15.48016642534407694, 69.96422921944753170 ) ) ;
#6716=CARTESIAN_POINT ( 'NONE',  ( -3.369429374625362517, 60.49191766694040240, 23.06312700027912399 ) ) ;
#6759=CARTESIAN_POINT ( 'NONE',  ( 5.126106709314291798, 68.65851429197792299, 20.89429596904683706 ) ) ;
#6783=ORIENTED_EDGE ( 'NONE', *, *, #64417, .F. ) ;
#6789=CARTESIAN_POINT ( 'NONE',  ( 0.8912353796322661781, 16.44139524822730891, -68.58382889509240954 ) ) ;
#6806=DIRECTION ( 'NONE',  ( 0.000000000000000000, 0.000000000000000000, -1.000000000000000000 ) ) ;
#6819=CARTESIAN_POINT ( 'NONE',  ( 3.428378827827394115, -16.35907404636618168, 69.10239319626211341 ) ) ;
#6840=CARTESIAN_POINT ( 'NONE',  ( -2.995737153994535884, 16.37687539610356424, -68.98994273415323164 ) ) ;
#6851=CARTESIAN_POINT ( 'NONE',  ( 5.000000000000000000, 15.86295220590816513, 69.92641310672760824 ) ) ;
#6859=ORIENTED_EDGE ( 'NONE', *, *, #61037, .T. ) ;
#6891=VERTEX_POINT ( 'NONE', #6542 ) ;
#6917=EDGE_CURVE ( 'NONE', #6191, #52335, #23884, .T. ) ;
#6987=DIRECTION ( 'NONE',  ( 1.000000000000000000, 0.000000000000000000, 0.000000000000000000 ) ) ;
#7015=ORIENTED_EDGE ( 'NONE', *, *, #58745, .F. ) ;
#7035=EDGE_CURVE ( 'NONE', #9105, #35502, #51979, .T. ) ;
#7065=CARTESIAN_POINT ( 'NONE',  ( -5.000000000000002665, 14.32120916179462711, 69.86289779849467152 ) ) ;
#7109=ORIENTED_EDGE ( 'NONE', *, *, #37673, .F. ) ;
#7116=CARTESIAN_POINT ( 'NONE',  ( -4.336811714531968676, 16.30209246799915590, 69.46462972172692218 ) ) ;
#7128=CARTESIAN_POINT ( 'NONE',  ( 3.734423912265594669, 66.26963445013785758, 26.58791153593135803 ) ) ;
#7146=EDGE_CURVE ( 'NONE', #37240, #2210, #36298, .T. ) ;
#7160=CARTESIAN_POINT ( 'NONE',  ( 1.506524674528621377, 10.12152537343868808, -70.16785718945648398 ) ) ;
#7171=PLANE ( 'NONE',  #42207 ) ;
#7228=CARTESIAN_POINT ( 'NONE',  ( 5.000000000000000888, 61.23620218020190009, -23.51718915682011257 ) ) ;
#7300=PLANE ( 'NONE',  #56810 ) ;
#7325=AXIS2_PLACEMENT_3D ( 'NONE', #68528, #39858, #62859 ) ;
#7364=CYLINDRICAL_SURFACE ( 'NONE', #62828, 8.000000000000000000 ) ;
#7420=CARTESIAN_POINT ( 'NONE',  ( 1.736494649864627426, 51.27805538755001180, -48.57014059985714027 ) ) ;
#7445=CARTESIAN_POINT ( 'NONE',  ( -4.999999999999996447, 16.24494643555759410, -69.83755725260752456 ) ) ;
#7471=CARTESIAN_POINT ( 'NONE',  ( -5.000000000000000000, 68.32828612846176952, -21.58087353894079641 ) ) ;
#7477=CARTESIAN_POINT ( 'NONE',  ( -5.000000000000000000, -52.35862550122958936, 48.98731492261398301 ) ) ;
#7498=CARTESIAN_POINT ( 'NONE',  ( -0.8912353796320175991, 67.61603573606919326, 20.05324848891948619 ) ) ;
#7528=EDGE_CURVE ( 'NONE', #49656, #36985, #14632, .T. ) ;
#7551=CARTESIAN_POINT ( 'NONE',  ( 5.000000000000000000, -60.11723469343085213, -46.25570701698114107 ) ) ;
#7558=CARTESIAN_POINT ( 'NONE',  ( -5.000000000000000000, 50.64189880742145533, -41.08656465431843685 ) ) ;
#7583=CARTESIAN_POINT ( 'NONE',  ( -4.999999999999996447, 16.24494643555759410, -69.83755725260752456 ) ) ;
#7628=ORIENTED_EDGE ( 'NONE', *, *, #10943, .T. ) ;
#7629=B_SPLINE_CURVE_WITH_KNOTS ( 'NONE', 3,
 ( #7583, #47190, #64554, #46823, #6840, #64912, #36626, #833, #64186, #1921 ),
 .UNSPECIFIED., .F., .F.,
 ( 4, 2, 2, 2, 4 ),
 ( 0.000000000000000000, 0.001314083742615249203, 0.002628167485230497539, 0.003942251227845745658, 0.005256334970460992476 ),
 .UNSPECIFIED. ) ;
#7648=DIRECTION ( 'NONE',  ( 1.000000000000000000, -0.000000000000000000, -0.000000000000000000 ) ) ;
#7685=CARTESIAN_POINT ( 'NONE',  ( -14.00000000000000178, 2.143131898507868248E-15, 17.50000000000000000 ) ) ;
#7738=VERTEX_POINT ( 'NONE', #65910 ) ;
#7790=EDGE_CURVE ( 'NONE', #60459, #17960, #71938, .T. ) ;
#7802=CARTESIAN_POINT ( 'NONE',  ( 4.999999999999996447, 15.86406185656353429, -69.92615499037644611 ) ) ;
#7850=CARTESIAN_POINT ( 'NONE',  ( -2.170320029210516921, 67.76782500014660116, 20.17643218080578293 ) ) ;
#7888=CARTESIAN_POINT ( 'NONE',  ( 5.000000000000000000, -11.69579520003551920, -68.31051037013783400 ) ) ;
#7890=AXIS2_PLACEMENT_3D ( 'NONE', #27902, #22230, #22604 ) ;
#7946=EDGE_LOOP ( 'NONE', ( #21215, #12970, #10881, #2680, #10506 ) ) ;
#7971=ADVANCED_FACE ( 'NONE', ( #50797 ), #67414, .F. ) ;
#7978=ORIENTED_EDGE ( 'NONE', *, *, #65768, .T. ) ;
#8033=B_SPLINE_CURVE_WITH_KNOTS ( 'NONE', 3,
 ( #34407, #50609, #67604, #33658, #56285, #63415, #73261, #67970, #17393, #73629, #23058, #46067 ),
 .UNSPECIFIED., .F., .F.,
 ( 4, 2, 2, 2, 2, 4 ),
 ( 1.618164387277533384E-15, 0.002547658444429635408, 0.005095316888857652320, 0.006369146111071660558, 0.007642975333285669665, 0.01019063377771368614 ),
 .UNSPECIFIED. ) ;
#8040=CARTESIAN_POINT ( 'NONE',  ( -0.7509181236840809515, 55.63764137816388455, -43.81192498624520226 ) ) ;
#8041=CARTESIAN_POINT ( 'NONE',  ( 0.000000000000000000, 0.000000000000000000, 0.000000000000000000 ) ) ;
#8176=ORIENTED_EDGE ( 'NONE', *, *, #70233, .T. ) ;
#8231=CARTESIAN_POINT ( 'NONE',  ( -5.126144196591286395, 68.65853088339355281, 20.89430926783131426 ) ) ;
#8233=CARTESIAN_POINT ( 'NONE',  ( 4.999999999999992895, 61.23691386381934620, 23.51762333030286811 ) ) ;
#8241=CARTESIAN_POINT ( 'NONE',  ( 4.193030820682222881, 60.66866849074683188, -23.17095654502590207 ) ) ;
#8298=CARTESIAN_POINT ( 'NONE',  ( 5.000000000000000000, 11.14555136602166741, -27.84144949604398533 ) ) ;
#8362=AXIS2_PLACEMENT_3D ( 'NONE', #16342, #51433, #29178 ) ;
#8394=CARTESIAN_POINT ( 'NONE',  ( 4.999999999999999112, 2.143131898507868248E-15, 17.50000000000000000 ) ) ;
#8409=CARTESIAN_POINT ( 'NONE',  ( 0.3794862803134621543, 55.62190996748000771, -43.80334292620879211 ) ) ;
#8512=CARTESIAN_POINT ( 'NONE',  ( -4.615726161709423181, 68.43878643976954379, -20.71807028113809679 ) ) ;
#8534=CARTESIAN_POINT ( 'NONE',  ( 5.000000000000000000, 10.25161785469019193, -64.79070129774501652 ) ) ;
#8583=CIRCLE ( 'NONE', #66414, 17.50000000000000000 ) ;
#8603=CARTESIAN_POINT ( 'NONE',  ( -3.511653767258388736, 68.04552192806590938, 20.40125235306568996 ) ) ;
#8623=EDGE_CURVE ( 'NONE', #71522, #17647, #53016, .T. ) ;
#8630=CARTESIAN_POINT ( 'NONE',  ( 4.999999999999999112, -12.55023575007693104, -69.09043692422062577 ) ) ;
#8684=DIRECTION ( 'NONE',  ( 0.000000000000000000, 0.000000000000000000, -1.000000000000000000 ) ) ;
#8687=ORIENTED_EDGE ( 'NONE', *, *, #17656, .F. ) ;
#8695=AXIS2_PLACEMENT_3D ( 'NONE', #63338, #34698, #57706 ) ;
#8743=AXIS2_PLACEMENT_3D ( 'NONE', #750, #28649, #68643 ) ;
#8777=CARTESIAN_POINT ( 'NONE',  ( -5.000000000000000000, 52.85071664756748788, -48.38833198888215037 ) ) ;
#8847=CARTESIAN_POINT ( 'NONE',  ( -4.999999999999999112, 52.28182290968012325, 42.43119126381112238 ) ) ;
#8905=VERTEX_POINT ( 'NONE', #54436 ) ;
#8928=CARTESIAN_POINT ( 'NONE',  ( 2.620431783929788150, -65.99617417813075804, -26.42108291243856399 ) ) ;
#8934=CARTESIAN_POINT ( 'NONE',  ( -5.000000000000000000, -10.82378452496245735, -67.02990231369408036 ) ) ;
#8954=CARTESIAN_POINT ( 'NONE',  ( -5.000000000000000000, -51.30401030464765455, 41.49390406302032375 ) ) ;
#8955=DIRECTION ( 'NONE',  ( 1.000000000000000000, 0.000000000000000000, 0.000000000000000000 ) ) ;
#8965=CARTESIAN_POINT ( 'NONE',  ( -2.170320029210519586, 16.41060967376241209, 68.77687409974782895 ) ) ;
#9004=CARTESIAN_POINT ( 'NONE',  ( 5.000000000000000000, -10.60557809245594640, -66.49298242784793445 ) ) ;
#9034=CARTESIAN_POINT ( 'NONE',  ( -3.496982156821605070, -51.71401992552402049, -48.73755072030548519 ) ) ;
#9091=ADVANCED_FACE ( 'NONE', ( #21206 ), #55560, .F. ) ;
#9097=EDGE_LOOP ( 'NONE', ( #42952, #21291, #66728, #7109 ) ) ;
#9100=FACE_OUTER_BOUND ( 'NONE', #25221, .T. ) ;
#9105=VERTEX_POINT ( 'NONE', #10273 ) ;
#9142=EDGE_CURVE ( 'NONE', #56998, #19443, #35006, .T. ) ;
#9149=DIRECTION ( 'NONE',  ( 1.000000000000000000, 0.000000000000000000, 0.000000000000000000 ) ) ;
#9152=EDGE_CURVE ( 'NONE', #7738, #13141, #69982, .T. ) ;
#9181=ORIENTED_EDGE ( 'NONE', *, *, #9991, .F. ) ;
#9202=ORIENTED_EDGE ( 'NONE', *, *, #64844, .T. ) ;
#9206=CARTESIAN_POINT ( 'NONE',  ( -6.298842414715106308, -10.24914933418239471, 64.89273347873384523 ) ) ;
#9217=DIRECTION ( 'NONE',  ( 0.000000000000000000, 0.000000000000000000, -1.000000000000000000 ) ) ;
#9247=CARTESIAN_POINT ( 'NONE',  ( -5.000000000000000000, 60.11723469343052528, 46.25570701698154608 ) ) ;
#9274=FACE_OUTER_BOUND ( 'NONE', #28957, .T. ) ;
#9294=ORIENTED_EDGE ( 'NONE', *, *, #40490, .T. ) ;
#9300=CARTESIAN_POINT ( 'NONE',  ( 0.7581620860337424661, -65.76154746681217489, -26.27794529688043923 ) ) ;
#9312=ADVANCED_FACE ( 'NONE', ( #47158 ), #5701, .F. ) ;
#9325=FACE_OUTER_BOUND ( 'NONE', #70172, .T. ) ;
#9335=ORIENTED_EDGE ( 'NONE', *, *, #33893, .F. ) ;
#9355=CARTESIAN_POINT ( 'NONE',  ( -4.193030820682224658, -60.66866849074650503, -23.17095654502674762 ) ) ;
#9356=CARTESIAN_POINT ( 'NONE',  ( 5.000000000000000000, 65.19475225706599986, 23.98307544245006184 ) ) ;
#9362=ORIENTED_EDGE ( 'NONE', *, *, #40761, .F. ) ;
#9383=CARTESIAN_POINT ( 'NONE',  ( 2.995737153982844347, -51.55860531535523705, 48.67776149471320934 ) ) ;
#9412=CARTESIAN_POINT ( 'NONE',  ( 1.296342370383407161, -49.95006747298835847, -40.70914535207442952 ) ) ;
#9456=ADVANCED_FACE ( 'NONE', ( #72019 ), #30920, .F. ) ;
#9500=ADVANCED_FACE ( 'NONE', ( #25984 ), #70337, .F. ) ;
#9505=CARTESIAN_POINT ( 'NONE',  ( 5.000000000000000000, -18.53862685874495853, -23.57305537018139674 ) ) ;
#9601=DIRECTION ( 'NONE',  ( 1.000000000000000000, -0.000000000000000000, 0.000000000000000000 ) ) ;
#9609=CARTESIAN_POINT ( 'NONE',  ( 7.456155213531538095, -10.23501372118566444, -65.47700548259878417 ) ) ;
#9620=ORIENTED_EDGE ( 'NONE', *, *, #64417, .T. ) ;
#9621=CARTESIAN_POINT ( 'NONE',  ( -4.999999999999999112, -67.66743717231497612, 22.54291394824926442 ) ) ;
#9647=AXIS2_PLACEMENT_3D ( 'NONE', #66370, #14676, #3378 ) ;
#9648=DIRECTION ( 'NONE',  ( -0.000000000000000000, 0.000000000000000000, -1.000000000000000000 ) ) ;
#9658=PLANE ( 'NONE',  #29413 ) ;
#9733=CARTESIAN_POINT ( 'NONE',  ( -3.369429374625359852, -60.49191766694055872, -23.06312700027871898 ) ) ;
#9741=CIRCLE ( 'NONE', #42188, 8.000000000000000000 ) ;
#9769=B_SPLINE_CURVE_WITH_KNOTS ( 'NONE', 3,
 ( #40957, #16804, #17187, #28139, #57956, #6263, #39467, #74161, #29267, #10792, #52279, #45485, #50776, #5887, #40206, #73790, #33828, #39832, #56825, #11172 ),
 .UNSPECIFIED., .F., .F.,
 ( 4, 2, 2, 2, 2, 2, 2, 2, 2, 4 ),
 ( 0.000000000000000000, 0.001156441540184007140, 0.001734662310276010493, 0.002312883080368014280, 0.003469324620552016215, 0.004625766160736019018, 0.005782207700920020954, 0.006938649241104022890, 0.008095090781288024825, 0.009251532321472025894 ),
 .UNSPECIFIED. ) ;
#9788=CARTESIAN_POINT ( 'NONE',  ( 0.3752463838824673381, -55.62178951997624665, -43.80327721769167226 ) ) ;
#9801=CARTESIAN_POINT ( 'NONE',  ( 2.620431783929502600, 10.11675809140012383, 70.36490484707876192 ) ) ;
#9823=CARTESIAN_POINT ( 'NONE',  ( -3.228176881619808647, 50.21013539028093220, -40.85102191503846569 ) ) ;
#9854=ORIENTED_EDGE ( 'NONE', *, *, #45601, .F. ) ;
#9902=CARTESIAN_POINT ( 'NONE',  ( -3.223881452105937573, -60.47365957010883619, 23.05198836891605652 ) ) ;
#9927=AXIS2_PLACEMENT_3D ( 'NONE', #61489, #10553, #50167 ) ;
#9960=ADVANCED_FACE ( 'NONE', ( #42795 ), #501, .F. ) ;
#9971=CARTESIAN_POINT ( 'NONE',  ( 0.000000000000000000, 2.143131898507868248E-15, 17.50000000000000000 ) ) ;
#9976=CARTESIAN_POINT ( 'NONE',  ( 1.781595147088347098, -16.42277972782010309, -68.70049804031377505 ) ) ;
#9988=CARTESIAN_POINT ( 'NONE',  ( -5.000000000000000888, -65.19475225706635513, 23.98307544244917011 ) ) ;
#9991=EDGE_CURVE ( 'NONE', #38797, #28093, #61026, .T. ) ;
#10013=EDGE_LOOP ( 'NONE', ( #36358, #31435, #62778, #66756 ) ) ;
#10026=DIRECTION ( 'NONE',  ( 1.000000000000000000, -0.000000000000000000, 0.000000000000000000 ) ) ;
#10036=CARTESIAN_POINT ( 'NONE',  ( 4.999999999999999112, 52.28182290968099011, -42.43119126381003525 ) ) ;
#10048=CARTESIAN_POINT ( 'NONE',  ( -3.511653767256468051, -68.04552192806512778, -20.40125235306675222 ) ) ;
#10055=CARTESIAN_POINT ( 'NONE',  ( -4.999999999999995559, -15.86406185656355916, -69.92615499037641769 ) ) ;
#10060=ORIENTED_EDGE ( 'NONE', *, *, #19650, .T. ) ;
#10067=AXIS2_PLACEMENT_3D ( 'NONE', #61116, #66778, #26018 ) ;
#10113=ORIENTED_EDGE ( 'NONE', *, *, #65766, .T. ) ;
#10164=LINE ( 'NONE', #33201, #41097 ) ;
#10170=CARTESIAN_POINT ( 'NONE',  ( 6.891449706541182607, 10.24244278380985662, 65.16993756079884292 ) ) ;
#10181=CARTESIAN_POINT ( 'NONE',  ( 5.000000000000000000, 10.00000000000000000, 75.19090595827292134 ) ) ;
#10189=CARTESIAN_POINT ( 'NONE',  ( -5.000000000000000000, -18.53862685874495142, 23.57305537018116581 ) ) ;
#10195=CARTESIAN_POINT ( 'NONE',  ( 0.7581620860261992778, 55.63814191976882029, -43.81219804999550149 ) ) ;
#10273=CARTESIAN_POINT ( 'NONE',  ( 0.000000000000000000, 1.132798289211301698E-14, 92.50000000000000000 ) ) ;
#10275=CARTESIAN_POINT ( 'NONE',  ( 1.506524674528582741, -65.82790954190812727, 26.31843049628270848 ) ) ;
#10277=CARTESIAN_POINT ( 'NONE',  ( 5.000000000000001776, 53.53067326687830985, 46.58593137613159030 ) ) ;
#10328=CARTESIAN_POINT ( 'NONE',  ( 5.107860025165524398, -10.26152767799308840, 64.38109526789187953 ) ) ;
#10339=CARTESIAN_POINT ( 'NONE',  ( -5.000000000000000000, 52.84347807771100491, 43.21644271080270983 ) ) ;
#10343=VERTEX_POINT ( 'NONE', #71015 ) ;
#10347=CARTESIAN_POINT ( 'NONE',  ( -1.506524674531949826, -10.12152537343867031, -70.16785718946157147 ) ) ;
#10413=ORIENTED_EDGE ( 'NONE', *, *, #11225, .T. ) ;
#10416=CARTESIAN_POINT ( 'NONE',  ( -4.737866951563840523, 52.21905653845793438, 48.93292554254848881 ) ) ;
#10418=CARTESIAN_POINT ( 'NONE',  ( -6.308070865144149053, -61.28915309314432847, -23.54949267152977299 ) ) ;
#10463=EDGE_CURVE ( 'NONE', #48525, #74324, #55942, .T. ) ;
#10483=CIRCLE ( 'NONE', #20101, 5.000000000000000888 ) ;
#10495=CARTESIAN_POINT ( 'NONE',  ( -4.999999999999999112, -14.31098243164692008, 69.87317657433686691 ) ) ;
#10503=AXIS2_PLACEMENT_3D ( 'NONE', #16596, #73958, #63750 ) ;
#10506=ORIENTED_EDGE ( 'NONE', *, *, #48693, .F. ) ;
#10520=ORIENTED_EDGE ( 'NONE', *, *, #13878, .T. ) ;
#10527=CARTESIAN_POINT ( 'NONE',  ( 2.436599634630353783, -51.42120007173177498, -48.62500384162233047 ) ) ;
#10534=EDGE_LOOP ( 'NONE', ( #44254, #17406, #59187, #41194, #17869 ) ) ;
#10553=DIRECTION ( 'NONE',  ( 1.000000000000000000, -0.000000000000000000, -0.000000000000000000 ) ) ;
#10565=CARTESIAN_POINT ( 'NONE',  ( -1.882291019712828861, 55.75505015263576070, -43.87597576788949993 ) ) ;
#10571=DIRECTION ( 'NONE',  ( 1.000000000000000000, -0.000000000000000000, -0.000000000000000000 ) ) ;
#10596=EDGE_LOOP ( 'NONE', ( #15558, #52591, #59222, #6783 ) ) ;
#10640=CARTESIAN_POINT ( 'NONE',  ( 0.4368895104463361156, 67.59332269699999074, -20.03478791450181973 ) ) ;
#10642=CARTESIAN_POINT ( 'NONE',  ( -5.000000000000000000, 51.30401030464796008, -41.49390406301998269 ) ) ;
#10644=CARTESIAN_POINT ( 'NONE',  ( 2.069125466538022096, -65.90280720053424091, 26.36412295902750103 ) ) ;
#10653=CARTESIAN_POINT ( 'NONE',  ( 5.000000000000000000, 11.32881245867859121, 67.85521288293392672 ) ) ;
#10695=AXIS2_PLACEMENT_3D ( 'NONE', #1826, #49316, #48197 ) ;
#10708=VECTOR ( 'NONE', #46006, 1000.000000000000000 ) ;
#10725=CARTESIAN_POINT ( 'NONE',  ( 5.000000000000000000, -50.64189880742087269, -41.08656465431914029 ) ) ;
#10747=VERTEX_POINT ( 'NONE', #61321 ) ;
#10785=CARTESIAN_POINT ( 'NONE',  ( -3.734423912261892298, 56.16062404875953007, 44.09723116535829490 ) ) ;
#10792=CARTESIAN_POINT ( 'NONE',  ( 5.000000000000000000, -53.55923425356098733, -45.42020841079093429 ) ) ;
#10794=DIRECTION ( 'NONE',  ( 0.000000000000000000, 0.02418647091589873691, 0.9997074645238147594 ) ) ;
#10869=CARTESIAN_POINT ( 'NONE',  ( -4.999999999999999112, -15.47455834364811622, 69.96446835377025764 ) ) ;
#10881=ORIENTED_EDGE ( 'NONE', *, *, #51498, .F. ) ;
#10943=EDGE_CURVE ( 'NONE', #63554, #71456, #20300, .T. ) ;
#10965=CARTESIAN_POINT ( 'NONE',  ( -5.126106709314341536, 16.23426604260439632, -69.90716554747308464 ) ) ;
#10999=DIRECTION ( 'NONE',  ( 0.000000000000000000, 0.000000000000000000, -1.000000000000000000 ) ) ;
#11016=CARTESIAN_POINT ( 'NONE',  ( 0.8721677472516105034, 67.61512445009731209, -20.05250736213323748 ) ) ;
#11031=CARTESIAN_POINT ( 'NONE',  ( 5.000000000000000888, 11.44657803507906024, 68.01244171956641082 ) ) ;
#11043=CARTESIAN_POINT ( 'NONE',  ( -4.999999999999999112, -67.66364885638941473, -22.52891795222312865 ) ) ;
#11053=ORIENTED_EDGE ( 'NONE', *, *, #51498, .T. ) ;
#11074=CARTESIAN_POINT ( 'NONE',  ( 0.6474643998439180148, -10.28110762191874983, 63.57179091896463063 ) ) ;
#11094=CARTESIAN_POINT ( 'NONE',  ( 3.369429374625374951, 10.27270496052241278, -63.91910092334653370 ) ) ;
#11120=ORIENTED_EDGE ( 'NONE', *, *, #45759, .T. ) ;
#11165=CARTESIAN_POINT ( 'NONE',  ( -1.781595147095501597, 51.28498669165002610, 48.57279346520133601 ) ) ;
#11172=CARTESIAN_POINT ( 'NONE',  ( 5.000000000000000000, -50.64189880742087269, -41.08656465431914029 ) ) ;
#11181=CARTESIAN_POINT ( 'NONE',  ( 5.000000000000000000, 0.000000000000000000, 0.000000000000000000 ) ) ;
#11187=CARTESIAN_POINT ( 'NONE',  ( -2.591411123066599487, 60.37037679142435564, -22.98897912932020660 ) ) ;
#11225=EDGE_CURVE ( 'NONE', #10747, #40213, #41107, .T. ) ;
#11244=CARTESIAN_POINT ( 'NONE',  ( 4.999999999999999112, -68.33088307291114916, 21.57589723056470987 ) ) ;
#11255=ORIENTED_EDGE ( 'NONE', *, *, #17034, .T. ) ;
#11258=CARTESIAN_POINT ( 'NONE',  ( 1.704527592502766531, 60.27089976682777461, 22.92829164824435395 ) ) ;
#11281=ORIENTED_EDGE ( 'NONE', *, *, #41105, .T. ) ;
#11311=LINE ( 'NONE', #52419, #10708 ) ;
#11324=EDGE_CURVE ( 'NONE', #72156, #34067, #70080, .T. ) ;
#11333=FACE_OUTER_BOUND ( 'NONE', #48841, .T. ) ;
#11337=B_SPLINE_CURVE_WITH_KNOTS ( 'NONE', 3,
 ( #53826, #7802, #48145, #1778, #25865, #47773, #31173, #59124, #65504, #54198, #71154, #25127, #43230, #2136, #37212, #37586, #36844, #70795, #8534, #48885 ),
 .UNSPECIFIED., .F., .F.,
 ( 4, 2, 2, 2, 2, 2, 2, 2, 2, 4 ),
 ( 0.000000000000000000, 0.001156441540183998683, 0.001734662310276000301, 0.002312883080368001703, 0.003469324620552004506, 0.004625766160736007743, 0.005782207700920009678, 0.006938649241104013349, 0.008095090781288016152, 0.009251532321472018955 ),
 .UNSPECIFIED. ) ;
#11357=CARTESIAN_POINT ( 'NONE',  ( 5.000000000000000000, 60.11723469343052528, 46.25570701698154608 ) ) ;
#11390=CARTESIAN_POINT ( 'NONE',  ( 5.000000000000000000, 51.30401030464707901, 41.49390406302104850 ) ) ;
#11409=LINE ( 'NONE', #11777, #12448 ) ;
#11422=DIRECTION ( 'NONE',  ( 0.000000000000000000, 0.000000000000000000, 1.000000000000000000 ) ) ;
#11440=FACE_OUTER_BOUND ( 'NONE', #12646, .T. ) ;
#11442=CARTESIAN_POINT ( 'NONE',  ( -5.000000000000000000, 63.85408791058048905, 24.15552328276567806 ) ) ;
#11454=CARTESIAN_POINT ( 'NONE',  ( 5.000000000000000000, 8.780967503833453037E-15, 71.70204102886728492 ) ) ;
#11464=CARTESIAN_POINT ( 'NONE',  ( 0.8997857290925440621, -16.44125064681548309, -68.58473395859590482 ) ) ;
#11465=CARTESIAN_POINT ( 'NONE',  ( -2.986204309486589110E-14, 67.59332269700053075, 20.03478791450399399 ) ) ;
#11532=CARTESIAN_POINT ( 'NONE',  ( -3.223881452105235024, 50.20043732027804850, 40.84573126306825230 ) ) ;
#11545=ORIENTED_EDGE ( 'NONE', *, *, #69448, .T. ) ;
#11555=FACE_OUTER_BOUND ( 'NONE', #43241, .T. ) ;
#11591=DIRECTION ( 'NONE',  ( 0.000000000000000000, -0.8536788251726021848, -0.5207998305029730712 ) ) ;
#11611=CARTESIAN_POINT ( 'NONE',  ( -5.000000000000000888, -10.54112798502250214, 66.30787999718575065 ) ) ;
#11668=CARTESIAN_POINT ( 'NONE',  ( 0.3794862803195203083, 65.74576272852577574, 26.26831557574585219 ) ) ;
#11682=CARTESIAN_POINT ( 'NONE',  ( -1.347111479062088207E-15, 0.000000000000000000, 0.000000000000000000 ) ) ;
#11755=CARTESIAN_POINT ( 'NONE',  ( -4.999999999999999112, -53.57153130924464079, -46.19535935661085091 ) ) ;
#11758=LINE ( 'NONE', #9247, #23309 ) ;
#11761=( LENGTH_UNIT ( ) NAMED_UNIT ( * ) SI_UNIT ( .MILLI., .METRE. ) );
#11763=CARTESIAN_POINT ( 'NONE',  ( -2.986204309486589110E-14, 67.59332269700053075, 20.03478791450399399 ) ) ;
#11777=CARTESIAN_POINT ( 'NONE',  ( -5.000000000000000000, -29.68417822476653711, -4.268394125863121502 ) ) ;
#11796=ORIENTED_EDGE ( 'NONE', *, *, #54912, .T. ) ;
#11801=LINE ( 'NONE', #40102, #66324 ) ;
#11808=EDGE_CURVE ( 'NONE', #4330, #17054, #660, .T. ) ;
#11809=CARTESIAN_POINT ( 'NONE',  ( -2.216418498320922748, -67.77535163244887428, 20.18253627485176693 ) ) ;
#11840=ORIENTED_EDGE ( 'NONE', *, *, #46837, .T. ) ;
#11843=CARTESIAN_POINT ( 'NONE',  ( -2.124081043562911830, -50.03790111639190741, -40.75706181777510295 ) ) ;
#11846=CARTESIAN_POINT ( 'NONE',  ( -2.170320029193735234, 51.35721532638135045, -48.60044191894100862 ) ) ;
#11889=ORIENTED_EDGE ( 'NONE', *, *, #4731, .T. ) ;
#11893=CARTESIAN_POINT ( 'NONE',  ( -0.8419854211627032514, -10.28111362163632769, -63.57154293063803152 ) ) ;
#11904=CARTESIAN_POINT ( 'NONE',  ( 3.228176881614417848, 50.21013539027831030, 40.85102191503853675 ) ) ;
#11914=CARTESIAN_POINT ( 'NONE',  ( 4.615726161707415010, -16.27701803902728273, -69.62876280158644704 ) ) ;
#11917=CARTESIAN_POINT ( 'NONE',  ( 5.000000000000000000, 60.90295814858271939, -23.31388853594749833 ) ) ;
#11922=CARTESIAN_POINT ( 'NONE',  ( 5.000000000000001776, -62.69487254116403108, -24.02505537902060695 ) ) ;
#11926=CARTESIAN_POINT ( 'NONE',  ( -0.8912353796373138071, -51.17464048784082564, 48.53058040617325020 ) ) ;
#11933=CARTESIAN_POINT ( 'NONE',  ( -14.00000000000000178, -2.250000000005106138, 10.23492587299426404 ) ) ;
#11939=CARTESIAN_POINT ( 'NONE',  ( 5.000000000000000000, -10.26105934116143459, 64.40045319026695836 ) ) ;
#11971=EDGE_CURVE ( 'NONE', #18291, #21807, #57641, .T. ) ;
#11976=ORIENTED_EDGE ( 'NONE', *, *, #48891, .T. ) ;
#11980=DIRECTION ( 'NONE',  ( 0.000000000000000000, 0.000000000000000000, -1.000000000000000000 ) ) ;
#12004=ORIENTED_EDGE ( 'NONE', *, *, #72604, .T. ) ;
#12014=CARTESIAN_POINT ( 'NONE',  ( -5.000000000000000888, 63.46295559274128806, -24.14151313015300104 ) ) ;
#12040=CARTESIAN_POINT ( 'NONE',  ( 4.471435261917194204, 60.74652839096584955, 23.21845616858769645 ) ) ;
#12043=CARTESIAN_POINT ( 'NONE',  ( -3.034644841523098859E-11, -67.59332269700080076, 20.03478791450305962 ) ) ;
#12045=DIRECTION ( 'NONE',  ( 0.000000000000000000, 0.8536788251726095123, -0.5207998305029611918 ) ) ;
#12070=CARTESIAN_POINT ( 'NONE',  ( 1.558072418983080354, 16.42747873774318990, -68.67104701338824668 ) ) ;
#12131=ORIENTED_EDGE ( 'NONE', *, *, #40761, .T. ) ;
#12202=CARTESIAN_POINT ( 'NONE',  ( 5.000000000000000000, -50.64189880742116401, 41.08656465431877791 ) ) ;
#12207=CARTESIAN_POINT ( 'NONE',  ( 5.000000000000000000, 70.11723469343073134, 28.93519894129288517 ) ) ;
#12272=CARTESIAN_POINT ( 'NONE',  ( -5.000000000000000000, -11.14555136602166208, 27.84144949604419494 ) ) ;
#12328=VERTEX_POINT ( 'NONE', #40953 ) ;
#12336=CARTESIAN_POINT ( 'NONE',  ( 2.726951573962122902E-14, -51.14729664189338365, -48.52014062455057797 ) ) ;
#12339=VECTOR ( 'NONE', #23576, 1000.000000000000000 ) ;
#12346=CARTESIAN_POINT ( 'NONE',  ( -4.999999999999997335, 15.86406185656356271, 69.92615499037644611 ) ) ;
#12353=CARTESIAN_POINT ( 'NONE',  ( -5.000000000000000000, -60.11723469343085213, -46.25570701698114107 ) ) ;
#12414=CYLINDRICAL_SURFACE ( 'NONE', #29985, 4.999999999999997335 ) ;
#12436=CARTESIAN_POINT ( 'NONE',  ( -6.298842414732201078, 10.24914933418224194, -64.89273347874026854 ) ) ;
#12448=VECTOR ( 'NONE', #34816, 1000.000000000000000 ) ;
#12471=ORIENTED_EDGE ( 'NONE', *, *, #20266, .T. ) ;
#12500=ORIENTED_EDGE ( 'NONE', *, *, #35639, .F. ) ;
#12507=ORIENTED_EDGE ( 'NONE', *, *, #26143, .T. ) ;
#12542=ORIENTED_EDGE ( 'NONE', *, *, #2226, .F. ) ;
#12646=EDGE_LOOP ( 'NONE', ( #1704, #13636, #5010, #19322, #12500 ) ) ;
#12650=CARTESIAN_POINT ( 'NONE',  ( 5.000000000000000888, -61.58609660504367866, -23.68302032025107806 ) ) ;
#12666=CARTESIAN_POINT ( 'NONE',  ( 5.000000000000002665, -14.32120916179451697, 69.86289779849465731 ) ) ;
#12675=ORIENTED_EDGE ( 'NONE', *, *, #37673, .T. ) ;
#12744=CARTESIAN_POINT ( 'NONE',  ( -5.000000000000000000, 66.10919140998015564, -23.67639547905944752 ) ) ;
#12787=B_SPLINE_CURVE_WITH_KNOTS ( 'NONE', 3,
 ( #50038, #10055, #50778, #44011, #15318, #38354, #66640, #73792, #26264, #14947, #4033, #72685, #73052, #21360, #8934, #44384, #66268, #67395, #38739, #14575 ),
 .UNSPECIFIED., .F., .F.,
 ( 4, 2, 2, 2, 2, 2, 2, 2, 2, 4 ),
 ( 0.000000000000000000, 0.001156441540183929945, 0.001734662310275897085, 0.002312883080367864226, 0.003469324620551793303, 0.004625766160735722381, 0.005782207700919650591, 0.006938649241103580535, 0.008095090781287509613, 0.009251532321471437822 ),
 .UNSPECIFIED. ) ;
#12788=EDGE_CURVE ( 'NONE', #37917, #22266, #16709, .T. ) ;
#12801=CARTESIAN_POINT ( 'NONE',  ( -0.7581620860332122236, 10.12340554704894657, -70.09014334687758208 ) ) ;
#12805=( BOUNDED_SURFACE ( )  B_SPLINE_SURFACE ( 3, 2, ( 
 ( #66537, #66168, #20507 ),
 ( #55616, #43522, #37886 ),
 ( #60884, #3933, #9206 ),
 ( #32226, #55244, #3550 ),
 ( #21261, #26540, #44285 ),
 ( #49565, #15225, #67299 ),
 ( #27292, #61638, #32988 ),
 ( #29168, #68776, #23124 ),
 ( #38999, #514, #17086 ),
 ( #22366, #148, #11074 ),
 ( #74066, #68404, #6159 ),
 ( #46136, #5412, #62003 ),
 ( #74436, #57097, #28785 ),
 ( #56354, #57483, #62365 ),
 ( #63487, #33353, #4673 ),
 ( #52183, #5049, #10328 ),
 ( #27669, #67671, #16331 ),
 ( #22744, #23494, #69153 ) ),
 .UNSPECIFIED., .F., .F., .T. ) 
 B_SPLINE_SURFACE_WITH_KNOTS ( ( 4, 2, 2, 2, 2, 2, 2, 2, 4 ),
 ( 3, 3 ),
 ( 0.04202945594034821625, 0.04396162471218456602, 0.04589379348402090886, 0.04782596225585725169, 0.04975813102769359453, 0.05169029979952993736, 0.05265638418544810878, 0.05362246857136628020, 0.05748680611503896587 ),
 ( 0.000000000000000000, 1.000000000000000000 ),
 .UNSPECIFIED. ) 
 GEOMETRIC_REPRESENTATION_ITEM ( )  RATIONAL_B_SPLINE_SURFACE ( (
 ( 1.000000000000000000, 0.6241276099607504513, 1.000000000000000000),
 ( 1.000000000000000000, 0.6218761496800573330, 1.000000000000000000),
 ( 1.000000000000000000, 0.6198047272362451343, 1.000000000000000000),
 ( 1.000000000000000000, 0.6161935119825044938, 1.000000000000000000),
 ( 1.000000000000000000, 0.6146642324079192310, 1.000000000000000000),
 ( 1.000000000000000000, 0.6121850116872262770, 1.000000000000000000),
 ( 1.000000000000000000, 0.6112350889398914244, 1.000000000000000000),
 ( 1.000000000000000000, 0.6099522725973434145, 1.000000000000000000),
 ( 1.000000000000000000, 0.6096208180308361202, 1.000000000000000000),
 ( 1.000000000000000000, 0.6096183796348998429, 1.000000000000000000),
 ( 1.000000000000000000, 0.6099422200101185521, 1.000000000000000000),
 ( 1.000000000000000000, 0.6109087447823760009, 1.000000000000000000),
 ( 1.000000000000000000, 0.6113123981688344255, 1.000000000000000000),
 ( 1.000000000000000000, 0.6122677719809430652, 1.000000000000000000),
 ( 1.000000000000000000, 0.6128199619021360567, 1.000000000000000000),
 ( 1.000000000000000000, 0.6159350830264649357, 1.000000000000000000),
 ( 1.000000000000000000, 0.6195556778516543295, 1.000000000000000000),
 ( 1.000000000000000000, 0.6241278272307883013, 1.000000000000000000) ) ) 
 REPRESENTATION_ITEM ( '' )  SURFACE ( )  );
#12814=DIRECTION ( 'NONE',  ( 0.000000000000000000, 1.224646799147353700E-16, 1.000000000000000000 ) ) ;
#12822=CARTESIAN_POINT ( 'NONE',  ( -4.465349678524266785, -56.41423509509906609, -44.23558526901030774 ) ) ;
#12865=CARTESIAN_POINT ( 'NONE',  ( 4.999999999999999112, 67.91007042436142171, -22.22893179987901746 ) ) ;
#12910=CARTESIAN_POINT ( 'NONE',  ( -5.000000000000000000, 0.000000000000000000, 0.000000000000000000 ) ) ;
#12948=DIRECTION ( 'NONE',  ( 0.000000000000000000, 0.000000000000000000, -1.000000000000000000 ) ) ;
#12970=ORIENTED_EDGE ( 'NONE', *, *, #39918, .F. ) ;
#12983=CARTESIAN_POINT ( 'NONE',  ( 0.8588954341814353244, -10.28066745654381720, -63.58998442112848437 ) ) ;
#13004=CARTESIAN_POINT ( 'NONE',  ( -14.00000000000000178, -2.250000000005106138, 10.23492587299426404 ) ) ;
#13008=ORIENTED_EDGE ( 'NONE', *, *, #11324, .T. ) ;
#13018=CARTESIAN_POINT ( 'NONE',  ( 2.219371606097240601, 67.78152867896243094, -20.18750705526135647 ) ) ;
#13068=EDGE_CURVE ( 'NONE', #24245, #4661, #47561, .T. ) ;
#13105=CARTESIAN_POINT ( 'NONE',  ( -4.999999999999999112, 65.74990953740004329, -23.82322416715241431 ) ) ;
#13134=CARTESIAN_POINT ( 'NONE',  ( -0.4451317748866090995, 67.59323688304503719, 20.03471819849916002 ) ) ;
#13141=VERTEX_POINT ( 'NONE', #70634 ) ;
#13186=CARTESIAN_POINT ( 'NONE',  ( -4.330454160167402478, -52.03352386568571575, -48.86100738216764228 ) ) ;
#13231=LINE ( 'NONE', #48309, #52033 ) ;
#13358=CARTESIAN_POINT ( 'NONE',  ( 4.465384415997338152, 56.41424811512310811, 44.23559237191029325 ) ) ;
#13359=CARTESIAN_POINT ( 'NONE',  ( -5.000000000000000000, -16.14408868864072844, 27.96238185062368586 ) ) ;
#13432=AXIS2_PLACEMENT_3D ( 'NONE', #3199, #26562, #49206 ) ;
#13436=CARTESIAN_POINT ( 'NONE',  ( -5.000000000000000000, 11.00774715070965470, 67.37702390743054082 ) ) ;
#13481=CARTESIAN_POINT ( 'NONE',  ( -3.034644841523098859E-11, -67.59332269700080076, 20.03478791450305962 ) ) ;
#13522=ORIENTED_EDGE ( 'NONE', *, *, #42848, .F. ) ;
#13529=CARTESIAN_POINT ( 'NONE',  ( -0.8419854211626224272, 49.91401432488780188, -40.68947704084985872 ) ) ;
#13565=VECTOR ( 'NONE', #11591, 1000.000000000000227 ) ;
#13586=ORIENTED_EDGE ( 'NONE', *, *, #56789, .T. ) ;
#13636=ORIENTED_EDGE ( 'NONE', *, *, #45759, .F. ) ;
#13668=ORIENTED_EDGE ( 'NONE', *, *, #41704, .T. ) ;
#13714=AXIS2_PLACEMENT_3D ( 'NONE', #42830, #71501, #48127 ) ;
#13742=B_SPLINE_CURVE_WITH_KNOTS ( 'NONE', 3,
 ( #66717, #55038, #60684, #2224, #26334, #31263, #9004, #15021, #38055, #31643, #3344, #7888, #19564, #43322, #8630, #61055, #66337, #54291, #25222, #47865, #42942, #42579 ),
 .UNSPECIFIED., .F., .F.,
 ( 4, 2, 2, 2, 2, 2, 2, 2, 2, 2, 4 ),
 ( 0.000000000000000000, 0.001156727053362478904, 0.001735090580043718465, 0.002313454106724957809, 0.003470181160087434762, 0.004048544686768671720, 0.004626908213449908679, 0.005783635266812357442, 0.006940362320174807073, 0.008097089373537256704, 0.009253816426899704600 ),
 .UNSPECIFIED. ) ;
#13748=CARTESIAN_POINT ( 'NONE',  ( 1.506524674528596730, 65.82790954191280264, -26.31843049628337639 ) ) ;
#13768=DIRECTION ( 'NONE',  ( 0.000000000000000000, 0.000000000000000000, -1.000000000000000000 ) ) ;
#13796=CIRCLE ( 'NONE', #56005, 17.50000000000000000 ) ;
#13800=CARTESIAN_POINT ( 'NONE',  ( -5.000000000000000000, 10.53354221205070829, 66.31578581128123062 ) ) ;
#13850=CARTESIAN_POINT ( 'NONE',  ( -3.428378827827393671, 68.02396499344679626, 20.38382289158802863 ) ) ;
#13864=CARTESIAN_POINT ( 'NONE',  ( -2.997005883569024753, 66.06021892604954360, 26.46015439093776322 ) ) ;
#13865=CARTESIAN_POINT ( 'NONE',  ( 4.193070328474952646, -60.66867996115637851, -23.17096354272581493 ) ) ;
#13866=CARTESIAN_POINT ( 'NONE',  ( 1.688721909672346033, 49.97488762307308718, 40.72268565194335110 ) ) ;
#13878=EDGE_CURVE ( 'NONE', #8905, #29247, #51861, .T. ) ;
#13896=ORIENTED_EDGE ( 'NONE', *, *, #50675, .F. ) ;
#13897=CARTESIAN_POINT ( 'NONE',  ( 0.4320110153365225858, 49.91454558246021378, -40.68976686129062870 ) ) ;
#13925=CYLINDRICAL_SURFACE ( 'NONE', #54497, 17.50000000000000000 ) ;
#13944=CARTESIAN_POINT ( 'NONE',  ( 5.000000000000000000, -68.60357193678697740, -20.85024232999374050 ) ) ;
#13980=( BOUNDED_SURFACE ( )  B_SPLINE_SURFACE ( 3, 2, ( 
 ( #22840, #63577, #4765 ),
 ( #10416, #17556, #33447 ),
 ( #45478, #10785, #16797 ),
 ( #39091, #39825, #62094 ),
 ( #28506, #62829, #40200 ),
 ( #44749, #67763, #11532 ),
 ( #11165, #56446, #46229 ),
 ( #27757, #50769, #34187 ),
 ( #57191, #34565, #73783 ),
 ( #51515, #33821, #74530 ),
 ( #45118, #68129, #57571 ),
 ( #45853, #39458, #62457 ),
 ( #68870, #69246, #56818 ),
 ( #5881, #28877, #11904 ),
 ( #69996, #23959, #19037 ),
 ( #976, #41319, #53748 ),
 ( #1343, #6623, #29260 ),
 ( #47696, #13358, #34937 ) ),
 .UNSPECIFIED., .F., .F., .F. ) 
 B_SPLINE_SURFACE_WITH_KNOTS ( ( 4, 2, 2, 2, 2, 2, 2, 2, 4 ),
 ( 3, 3 ),
 ( 0.04202945594032910653, 0.04396162471216781553, 0.04589379348400653147, 0.04782596225584524741, 0.04975813102768396334, 0.05169029979952267928, 0.05265638418544203725, 0.05362246857136139522, 0.05748680611503882015 ),
 ( 0.000000000000000000, 1.000000000000000000 ),
 .UNSPECIFIED. ) 
 GEOMETRIC_REPRESENTATION_ITEM ( )  RATIONAL_B_SPLINE_SURFACE ( (
 ( 1.000000000000000000, 0.6241276099608161765, 1.000000000000000000),
 ( 1.000000000000000000, 0.6218761496803369981, 1.000000000000000000),
 ( 1.000000000000000000, 0.6198047272360041049, 1.000000000000000000),
 ( 1.000000000000000000, 0.6161935119828376717, 1.000000000000000000),
 ( 1.000000000000000000, 0.6146642324084842235, 1.000000000000000000),
 ( 1.000000000000000000, 0.6121850116867159075, 1.000000000000000000),
 ( 1.000000000000000000, 0.6112350889402272669, 1.000000000000000000),
 ( 1.000000000000000000, 0.6099522725970315529, 1.000000000000000000),
 ( 1.000000000000000000, 0.6096208180308009261, 1.000000000000000000),
 ( 1.000000000000000000, 0.6096183796349370354, 1.000000000000000000),
 ( 1.000000000000000000, 0.6099422200101830560, 1.000000000000000000),
 ( 1.000000000000000000, 0.6109087447823331463, 1.000000000000000000),
 ( 1.000000000000000000, 0.6113123981686992003, 1.000000000000000000),
 ( 1.000000000000000000, 0.6122677719810616370, 1.000000000000000000),
 ( 1.000000000000000000, 0.6128199619022168809, 1.000000000000000000),
 ( 1.000000000000000000, 0.6159350830261014487, 1.000000000000000000),
 ( 1.000000000000000000, 0.6195556778519170082, 1.000000000000000000),
 ( 1.000000000000000000, 0.6241278272307890784, 1.000000000000000000) ) ) 
 REPRESENTATION_ITEM ( '' )  SURFACE ( )  );
#14020=ORIENTED_EDGE ( 'NONE', *, *, #52857, .T. ) ;
#14050=CARTESIAN_POINT ( 'NONE',  ( -5.107860025166923279, 50.62490018645984691, -41.07729128472220026 ) ) ;
#14062=ORIENTED_EDGE ( 'NONE', *, *, #55105, .T. ) ;
#14093=CARTESIAN_POINT ( 'NONE',  ( 1.739508062077475881, -51.27839935804492910, -48.57027215863523395 ) ) ;
#14117=CARTESIAN_POINT ( 'NONE',  ( 3.496982156810621412, -16.35094707925534863, -69.15443034746733986 ) ) ;
#14125=CARTESIAN_POINT ( 'NONE',  ( 3.511653767258104963, 68.04552192806764310, -20.40125235305975337 ) ) ;
#14153=ADVANCED_FACE ( 'NONE', ( #71463 ), #26187, .F. ) ;
#14154=B_SPLINE_CURVE_WITH_KNOTS ( 'NONE', 3,
 ( #19403, #31098, #36405, #59418, #70725, #70369, #47344, #53019, #24694 ),
 .UNSPECIFIED., .F., .F.,
 ( 4, 2, 1, 2, 4 ),
 ( 0.000000000000000000, 0.001314083742615069009, 0.002628167485230138017, 0.003942251227845207026, 0.005256334970460276035 ),
 .UNSPECIFIED. ) ;
#14156=ORIENTED_EDGE ( 'NONE', *, *, #13068, .F. ) ;
#14177=CARTESIAN_POINT ( 'NONE',  ( -4.999999999999999112, 10.82378452496245735, 67.02990231369408036 ) ) ;
#14179=ORIENTED_EDGE ( 'NONE', *, *, #58752, .F. ) ;
#14246=CARTESIAN_POINT ( 'NONE',  ( -3.544144923083014653, 60.54353712382538077, 23.09461823984563011 ) ) ;
#14248=CARTESIAN_POINT ( 'NONE',  ( 5.000000000000000000, 67.91996363552645732, 22.23680535815963921 ) ) ;
#14274=CARTESIAN_POINT ( 'NONE',  ( 4.193070328474947317, 50.40098303874201235, -40.95513628906619630 ) ) ;
#14318=DIRECTION ( 'NONE',  ( 1.000000000000000000, 0.000000000000000000, 0.000000000000000000 ) ) ;
#14325=CARTESIAN_POINT ( 'NONE',  ( -1.347111479062088207E-15, 0.000000000000000000, 0.000000000000000000 ) ) ;
#14384=AXIS2_PLACEMENT_3D ( 'NONE', #31856, #27302, #55627 ) ;
#14398=CARTESIAN_POINT ( 'NONE',  ( 5.000000000000000000, -10.00000000000000000, -75.19090595827292134 ) ) ;
#14457=VERTEX_POINT ( 'NONE', #11465 ) ;
#14467=CARTESIAN_POINT ( 'NONE',  ( 3.428378827827396336, -51.66489094708061458, -48.71857030467509020 ) ) ;
#14469=VECTOR ( 'NONE', #58765, 1000.000000000000000 ) ;
#14483=CARTESIAN_POINT ( 'NONE',  ( -5.000000000000000000, 50.98531617258460358, 41.27391139027680111 ) ) ;
#14533=CARTESIAN_POINT ( 'NONE',  ( -5.000000000000000000, 52.35862550122891435, 48.98731492261470777 ) ) ;
#14541=DIRECTION ( 'NONE',  ( -1.000000000000000000, 0.000000000000000000, 0.000000000000000000 ) ) ;
#14575=CARTESIAN_POINT ( 'NONE',  ( -5.000000000000000000, -10.26105934116142215, -64.40045319026754100 ) ) ;
#14592=DIRECTION ( 'NONE',  ( -1.000000000000000000, 0.000000000000000000, 0.000000000000000000 ) ) ;
#14595=CARTESIAN_POINT ( 'NONE',  ( -5.000000000000000000, -53.57132521838729389, 46.19376297453487012 ) ) ;
#14596=CARTESIAN_POINT ( 'NONE',  ( 5.000000000000000000, -16.14408868864072844, -27.96238185062390613 ) ) ;
#14621=CARTESIAN_POINT ( 'NONE',  ( 1.704527592502762756, -60.27089976682793093, -22.92829164824393118 ) ) ;
#14632=CIRCLE ( 'NONE', #64039, 8.000000000000000000 ) ;
#14674=CARTESIAN_POINT ( 'NONE',  ( 4.465384415997316836, -56.41424811512342785, -44.23559237190989535 ) ) ;
#14676=DIRECTION ( 'NONE',  ( 1.000000000000000000, -0.000000000000000000, -0.000000000000000000 ) ) ;
#14689=LINE ( 'NONE', #8298, #56371 ) ;
#14693=B_SPLINE_CURVE_WITH_KNOTS ( 'NONE', 3,
 ( #28566, #57629, #298, #28942, #5943, #56510, #16487, #5566 ),
 .UNSPECIFIED., .F., .F.,
 ( 4, 2, 2, 4 ),
 ( 0.005256334970490767269, 0.006570121696662000604, 0.007883908422833233939, 0.01051148187517570234 ),
 .UNSPECIFIED. ) ;
#14774=ORIENTED_EDGE ( 'NONE', *, *, #34232, .F. ) ;
#14882=ORIENTED_EDGE ( 'NONE', *, *, #26302, .F. ) ;
#14902=CARTESIAN_POINT ( 'NONE',  ( -2.804140485925949776E-11, 67.59332269700094287, -20.03478791450258001 ) ) ;
#14947=CARTESIAN_POINT ( 'NONE',  ( -5.000000000000000888, -12.55543720214795478, -69.09376167622117748 ) ) ;
#14993=CARTESIAN_POINT ( 'NONE',  ( -0.8419854211626188745, -60.19512794652365528, -22.88206588978800582 ) ) ;
#15001=EDGE_CURVE ( 'NONE', #45416, #18291, #10164, .T. ) ;
#15003=AXIS2_PLACEMENT_3D ( 'NONE', #42507, #37232, #2156 ) ;
#15018=AXIS2_PLACEMENT_3D ( 'NONE', #12910, #34481, #46513 ) ;
#15021=CARTESIAN_POINT ( 'NONE',  ( 5.000000000000000888, -10.82431413986195956, -67.03128830763427004 ) ) ;
#15041=CARTESIAN_POINT ( 'NONE',  ( 2.957351242930898602E-11, 51.14729664189404446, -48.52014062454985321 ) ) ;
#15071=DIRECTION ( 'NONE',  ( 0.000000000000000000, 1.000000000000000000, -1.224646799147353207E-16 ) ) ;
#15079=ORIENTED_EDGE ( 'NONE', *, *, #7528, .T. ) ;
#15188=B_SPLINE_CURVE_WITH_KNOTS ( 'NONE', 3,
 ( #18046, #70833, #1458, #70471, #69358, #17668, #18789, #12014, #35047, #24064, #47074, #58059, #64443, #13105, #12744, #41794, #65161, #64803, #6370, #7471, #30476, #53493 ),
 .UNSPECIFIED., .F., .F.,
 ( 4, 2, 2, 2, 2, 2, 2, 2, 2, 2, 4 ),
 ( 0.000000000000000000, 0.001156727053362452667, 0.001735090580043686806, 0.002313454106724920946, 0.003470181160087388791, 0.004048544686768622280, 0.004626908213449855770, 0.005783635266812325350, 0.006940362320174795797, 0.008097089373537265378, 0.009253816426899735825 ),
 .UNSPECIFIED. ) ;
#15210=ORIENTED_EDGE ( 'NONE', *, *, #11225, .F. ) ;
#15225=CARTESIAN_POINT ( 'NONE',  ( -1.877992804776299263, -10.12031740952197545, 70.21778636471883317 ) ) ;
#15236=CYLINDRICAL_SURFACE ( 'NONE', #14384, 17.50000000000000000 ) ;
#15285=ORIENTED_EDGE ( 'NONE', *, *, #10943, .F. ) ;
#15312=CARTESIAN_POINT ( 'NONE',  ( 3.223881452105731515, -60.47365957010915594, -23.05198836891676351 ) ) ;
#15318=CARTESIAN_POINT ( 'NONE',  ( -5.000000000000000000, -14.70421557449315486, -69.92631206022691970 ) ) ;
#15336=CARTESIAN_POINT ( 'NONE',  ( 6.891449706512932316, -51.31760009880697027, 41.45518442799505721 ) ) ;
#15361=CARTESIAN_POINT ( 'NONE',  ( 4.999999999999999112, -53.09993190648272332, 43.73864582539214751 ) ) ;
#15369=CARTESIAN_POINT ( 'NONE',  ( 5.000000000000000888, 64.42874436516095216, 24.11656705754242580 ) ) ;
#15421=CARTESIAN_POINT ( 'NONE',  ( -3.223881452104699008, -50.20043732027927774, -40.84573126306842283 ) ) ;
#15437=CARTESIAN_POINT ( 'NONE',  ( 3.734423912265155465, 10.10901040137928852, 70.68514270129381316 ) ) ;
#15461=CARTESIAN_POINT ( 'NONE',  ( 1.877992804776344338, 55.75022808459620904, -43.87334515337072105 ) ) ;
#15493=VERTEX_POINT ( 'NONE', #13481 ) ;
#15511=CARTESIAN_POINT ( 'NONE',  ( -5.000000000000000000, 50.64189880742059557, 41.08656465431948845 ) ) ;
#15558=ORIENTED_EDGE ( 'NONE', *, *, #22614, .F. ) ;
#15582=ORIENTED_EDGE ( 'NONE', *, *, #25290, .T. ) ;
#15690=DIRECTION ( 'NONE',  ( 1.000000000000000000, -0.000000000000000000, -0.000000000000000000 ) ) ;
#15710=CARTESIAN_POINT ( 'NONE',  ( 4.471435261904115777, -50.48103707412492724, 40.99880869399019190 ) ) ;
#15761=AXIS2_PLACEMENT_3D ( 'NONE', #30654, #47992, #65351 ) ;
#15774=EDGE_CURVE ( 'NONE', #10747, #34668, #59133, .T. ) ;
#15834=CARTESIAN_POINT ( 'NONE',  ( 3.074111742560642124, 51.58078258920254910, -48.68628732315515606 ) ) ;
#15926=CARTESIAN_POINT ( 'NONE',  ( -5.000000000000000000, 29.68417822476651580, 4.268394125863321342 ) ) ;
#15939=ADVANCED_FACE ( 'NONE', ( #62489 ), #45511, .F. ) ;
#15983=LINE ( 'NONE', #62016, #16576 ) ;
#15989=CARTESIAN_POINT ( 'NONE',  ( 3.223881452092225430, -10.27322224982958687, -63.89771963198325011 ) ) ;
#16008=CARTESIAN_POINT ( 'NONE',  ( -5.000000000000000000, 11.00479820989369806, -67.37201579502529114 ) ) ;
#16037=DIRECTION ( 'NONE',  ( 0.000000000000000000, 0.000000000000000000, -1.000000000000000000 ) ) ;
#16059=CARTESIAN_POINT ( 'NONE',  ( 0.3794862803195819256, -65.74576272852144143, -26.26831557574764986 ) ) ;
#16078=CARTESIAN_POINT ( 'NONE',  ( 0.6547826978324309266, -49.91450260127135863, 40.68974341348022961 ) ) ;
#16134=ORIENTED_EDGE ( 'NONE', *, *, #44067, .T. ) ;
#16159=CARTESIAN_POINT ( 'NONE',  ( 1.317228840344440322, -55.68607278123021587, -43.83834608838390068 ) ) ;
#16199=CARTESIAN_POINT ( 'NONE',  ( 6.298842414715673854, 51.07418104650354707, -41.32239042994763878 ) ) ;
#16223=AXIS2_PLACEMENT_3D ( 'NONE', #66462, #4972, #49106 ) ;
#16276=DIRECTION ( 'NONE',  ( 0.000000000000000000, 0.000000000000000000, -1.000000000000000000 ) ) ;
#16278=CARTESIAN_POINT ( 'NONE',  ( -1.506680654955288245, -65.82403019918164944, 26.31606384388981112 ) ) ;
#16307=ORIENTED_EDGE ( 'NONE', *, *, #23310, .F. ) ;
#16331=CARTESIAN_POINT ( 'NONE',  ( 6.308070865109145053, -10.25011764679052995, 64.85270989093093874 ) ) ;
#16333=CARTESIAN_POINT ( 'NONE',  ( -5.000000000000000888, 66.79063484153765273, 23.29724706625453479 ) ) ;
#16342=CARTESIAN_POINT ( 'NONE',  ( -5.000000000000000000, -16.14408868864072844, 27.96238185062368586 ) ) ;
#16350=CARTESIAN_POINT ( 'NONE',  ( -5.000000000000000000, 10.26105934116143281, -64.40045319026697257 ) ) ;
#16362=CARTESIAN_POINT ( 'NONE',  ( -5.000000000000000000, -50.64189880742087269, -41.08656465431914029 ) ) ;
#16375=VERTEX_POINT ( 'NONE', #6194 ) ;
#16413=CARTESIAN_POINT ( 'NONE',  ( 5.000000000000000000, 53.55895565990340401, -45.41404144516010888 ) ) ;
#16426=CARTESIAN_POINT ( 'NONE',  ( 1.781595147095572207, -67.70776641946376628, -20.12770457511637190 ) ) ;
#16440=CARTESIAN_POINT ( 'NONE',  ( 0.000000000000000000, 0.000000000000000000, -92.50000000000000000 ) ) ;
#16448=CARTESIAN_POINT ( 'NONE',  ( 7.456155213531532766, -51.58724325107078812, 41.60228463192836301 ) ) ;
#16487=CARTESIAN_POINT ( 'NONE',  ( -4.231687259407054036, -16.30907003467246597, -69.42009600258494117 ) ) ;
#16504=CARTESIAN_POINT ( 'NONE',  ( -5.000000000000000000, -11.32881245867859121, 67.85521288293392672 ) ) ;
#16505=CARTESIAN_POINT ( 'NONE',  ( 4.231687259402825418, 51.96503165405418656, 48.83411696341816821 ) ) ;
#16508=CARTESIAN_POINT ( 'NONE',  ( 4.615726161707419450, -52.16176840074130183, 48.91069252044830051 ) ) ;
#16511=ADVANCED_FACE ( 'NONE', ( #21665 ), #7300, .F. ) ;
#16549=CARTESIAN_POINT ( 'NONE',  ( 0.3794862803194714584, 10.12385276103914222, 70.07165850195889334 ) ) ;
#16573=DIRECTION ( 'NONE',  ( -1.000000000000000000, -0.000000000000000000, -0.000000000000000000 ) ) ;
#16576=VECTOR ( 'NONE', #68053, 1000.000000000000000 ) ;
#16594=CIRCLE ( 'NONE', #22633, 5.000000000000000888 ) ;
#16596=CARTESIAN_POINT ( 'NONE',  ( 0.000000000000000000, 0.000000000000000000, 0.000000000000000000 ) ) ;
#16599=CARTESIAN_POINT ( 'NONE',  ( -3.734423912265298018, 10.10901040137928852, -70.68514270129381316 ) ) ;
#16602=ORIENTED_EDGE ( 'NONE', *, *, #17162, .T. ) ;
#16638=ADVANCED_FACE ( 'NONE', ( #64997 ), #24632, .F. ) ;
#16651=CARTESIAN_POINT ( 'NONE',  ( 1.296342370383565035, -60.23018777774463217, 22.90345467631815168 ) ) ;
#16709=LINE ( 'NONE', #39739, #28237 ) ;
#16726=CARTESIAN_POINT ( 'NONE',  ( -1.296342370391218246, -10.28012030475504268, -63.61260002839784278 ) ) ;
#16734=CARTESIAN_POINT ( 'NONE',  ( -3.369429374625374063, -50.21921270641836088, 40.85597392306797815 ) ) ;
#16795=PRODUCT_DEFINITION_SHAPE ( 'NONE', 'NONE',  #37611 ) ;
#16797=CARTESIAN_POINT ( 'NONE',  ( -6.298842414731628203, 51.07418104650923851, 41.32239042995228573 ) ) ;
#16804=CARTESIAN_POINT ( 'NONE',  ( 4.999999999999992895, -52.62579568235199190, -48.70175807018021885 ) ) ;
#16859=CARTESIAN_POINT ( 'NONE',  ( -0.4369882809721274963, -16.44602605510714710, 68.55492853905352035 ) ) ;
#16878=CARTESIAN_POINT ( 'NONE',  ( -5.000000000000000888, 13.57926339724869536, 69.65188861886714733 ) ) ;
#16897=VERTEX_POINT ( 'NONE', #72141 ) ;
#16976=ORIENTED_EDGE ( 'NONE', *, *, #7146, .F. ) ;
#17029=CARTESIAN_POINT ( 'NONE',  ( -2.804140485925949776E-11, 67.59332269700094287, -20.03478791450258001 ) ) ;
#17031=CARTESIAN_POINT ( 'NONE',  ( -4.999999999999999112, -53.36732872257274352, -44.46877392682785057 ) ) ;
#17032=ORIENTED_EDGE ( 'NONE', *, *, #22159, .F. ) ;
#17033=CARTESIAN_POINT ( 'NONE',  ( 2.997005883566703055, -66.06021892604988466, 26.46015439093906352 ) ) ;
#17034=EDGE_CURVE ( 'NONE', #45651, #72830, #62953, .T. ) ;
#17041=CARTESIAN_POINT ( 'NONE',  ( 4.217983994790206914, 68.29231466825460473, 20.60018752343912141 ) ) ;
#17054=VERTEX_POINT ( 'NONE', #58537 ) ;
#17058=CARTESIAN_POINT ( 'NONE',  ( -4.999999999999999112, -65.00666015986166713, -24.03732210400576008 ) ) ;
#17086=CARTESIAN_POINT ( 'NONE',  ( -0.6547826978331323655, -10.28110016890870071, 63.57209897671329912 ) ) ;
#17088=CARTESIAN_POINT ( 'NONE',  ( -5.000000000000000000, 62.69792629052177091, 24.03557775816959463 ) ) ;
#17106=CARTESIAN_POINT ( 'NONE',  ( -3.228176881619507999, -10.27295505383823304, -63.90876373295927237 ) ) ;
#17122=CARTESIAN_POINT ( 'NONE',  ( -0.8721677472503426287, 51.17354301023129892, -48.53016177276298038 ) ) ;
#17160=MANIFOLD_SOLID_BREP ( 'Cut-Extrude1', #65951 ) ;
#17162=EDGE_CURVE ( 'NONE', #71456, #38888, #21854, .T. ) ;
#17167=ORIENTED_EDGE ( 'NONE', *, *, #29684, .F. ) ;
#17173=CARTESIAN_POINT ( 'NONE',  ( -2.124081043562909610, -10.27770035960974582, 63.71262442773669932 ) ) ;
#17175=FACE_OUTER_BOUND ( 'NONE', #6419, .T. ) ;
#17187=CARTESIAN_POINT ( 'NONE',  ( 4.999999999999998224, -52.85071664756681287, -48.38833198888288223 ) ) ;
#17208=ORIENTED_EDGE ( 'NONE', *, *, #29903, .T. ) ;
#17241=FACE_BOUND ( 'NONE', #38672, .T. ) ;
#17244=CARTESIAN_POINT ( 'NONE',  ( -4.615726161707376818, -52.16176840074092524, -48.91069252044866289 ) ) ;
#17271=VERTEX_POINT ( 'NONE', #36992 ) ;
#17273=EDGE_CURVE ( 'NONE', #52335, #12328, #73835, .T. ) ;
#17300=FACE_OUTER_BOUND ( 'NONE', #39245, .T. ) ;
#17307=CARTESIAN_POINT ( 'NONE',  ( -3.511653767256416092, 16.35475815725936499, 69.12977678000893889 ) ) ;
#17342=B_SPLINE_CURVE_WITH_KNOTS ( 'NONE', 3,
 ( #45198, #35021, #11244, #39911, #5592, #64043, #62918, #6342, #22174, #51228, #74239, #22545, #23300, #34649, #28964, #28589, #23676, #57654, #74615, #29712 ),
 .UNSPECIFIED., .F., .F.,
 ( 4, 2, 2, 2, 2, 2, 2, 2, 2, 4 ),
 ( 2.797157557069881010E-17, 0.001156441540184017982, 0.001734662310276006807, 0.002312883080367995198, 0.003469324620551979786, 0.004625766160735963507, 0.005782207700919948096, 0.006938649241103932684, 0.008095090781287915538, 0.009251532321471899259 ),
 .UNSPECIFIED. ) ;
#17393=CARTESIAN_POINT ( 'NONE',  ( 2.124081043562865201, 10.27770035960974582, 63.71262442773669221 ) ) ;
#17405=CARTESIAN_POINT ( 'NONE',  ( -5.000000000000000000, -52.63864145287891461, -42.88977517748093504 ) ) ;
#17406=ORIENTED_EDGE ( 'NONE', *, *, #61527, .F. ) ;
#17418=CARTESIAN_POINT ( 'NONE',  ( 5.000000000000000000, 12.55023575007693104, 69.09043692422063998 ) ) ;
#17429=CARTESIAN_POINT ( 'NONE',  ( -5.000000000000000000, -65.75515815785537654, -23.82162496270666452 ) ) ;
#17461=CARTESIAN_POINT ( 'NONE',  ( -6.891449706547808418, -61.56004288259260449, 23.71475313280533115 ) ) ;
#17498=CARTESIAN_POINT ( 'NONE',  ( -4.193070328474953534, -50.40098303874145103, -40.95513628906691395 ) ) ;
#17549=CARTESIAN_POINT ( 'NONE',  ( -4.193070328474945541, -10.26769692241485643, 64.12609983179220308 ) ) ;
#17556=CARTESIAN_POINT ( 'NONE',  ( -4.104248244567547665, 56.27889056303344262, 44.16174987545375785 ) ) ;
#17566=CARTESIAN_POINT ( 'NONE',  ( 0.8761883848702571864, -16.44150283900215825, -68.58316157020809101 ) ) ;
#17575=CARTESIAN_POINT ( 'NONE',  ( 4.999999999999999112, -61.23691386381950252, -23.51762333030244534 ) ) ;
#17580=CARTESIAN_POINT ( 'NONE',  ( -6.891449706532799979, 61.56004288261516422, -23.71475313281856501 ) ) ;
#17620=CARTESIAN_POINT ( 'NONE',  ( -4.999999999999953815, -52.35862550122923409, -48.98731492261434539 ) ) ;
#17630=CARTESIAN_POINT ( 'NONE',  ( 5.000000000000000000, -32.28817737728140003, -1.075528555105620399E-13 ) ) ;
#17632=ORIENTED_EDGE ( 'NONE', *, *, #4278, .T. ) ;
#17647=VERTEX_POINT ( 'NONE', #70047 ) ;
#17656=EDGE_CURVE ( 'NONE', #37508, #49656, #58003, .T. ) ;
#17668=CARTESIAN_POINT ( 'NONE',  ( -5.000000000000001776, 62.69487254116438635, -24.02505537901974009 ) ) ;
#17697=CARTESIAN_POINT ( 'NONE',  ( -4.999999999999944045, 68.60357193678724741, -20.85024232999276350 ) ) ;
#17701=CARTESIAN_POINT ( 'NONE',  ( 5.000000000000000000, 70.11723469343132820, -28.93519894129142145 ) ) ;
#17726=VERTEX_POINT ( 'NONE', #59099 ) ;
#17727=CARTESIAN_POINT ( 'NONE',  ( 3.511653767256929459, 16.35475815725939341, -69.12977678000905257 ) ) ;
#17762=CARTESIAN_POINT ( 'NONE',  ( -5.000000000000000000, 52.35862550122891435, 48.98731492261470777 ) ) ;
#17782=CARTESIAN_POINT ( 'NONE',  ( -5.000000000000001776, 53.12474899268234907, -47.87640533067806814 ) ) ;
#17800=ORIENTED_EDGE ( 'NONE', *, *, #50993, .T. ) ;
#17806=CARTESIAN_POINT ( 'NONE',  ( -4.999999999999999112, -63.85408791058067379, -24.15552328276524463 ) ) ;
#17869=ORIENTED_EDGE ( 'NONE', *, *, #33288, .F. ) ;
#17956=CARTESIAN_POINT ( 'NONE',  ( -3.544144923088103472, -50.27229464832340966, 40.88493206427740745 ) ) ;
#17960=VERTEX_POINT ( 'NONE', #15926 ) ;
#17961=DIRECTION ( 'NONE',  ( 0.000000000000000000, 0.000000000000000000, -1.000000000000000000 ) ) ;
#18046=CARTESIAN_POINT ( 'NONE',  ( -5.000000000000000000, 60.90295814858271939, -23.31388853594749833 ) ) ;
#18078=DIRECTION ( 'NONE',  ( 1.000000000000000000, -0.000000000000000000, -0.000000000000000000 ) ) ;
#18164=DIRECTION ( 'NONE',  ( 1.000000000000000000, 0.000000000000000000, 0.000000000000000000 ) ) ;
#18166=EDGE_CURVE ( 'NONE', #24578, #6205, #21380, .T. ) ;
#18247=DIRECTION ( 'NONE',  ( 0.000000000000000000, -1.387778780781445676E-15, 1.000000000000000000 ) ) ;
#18276=EDGE_CURVE ( 'NONE', #46734, #55139, #13231, .T. ) ;
#18291=VERTEX_POINT ( 'NONE', #53984 ) ;
#18305=DIRECTION ( 'NONE',  ( 0.000000000000000000, 2.081668171172168119E-15, 1.000000000000000000 ) ) ;
#18323=CARTESIAN_POINT ( 'NONE',  ( 5.000000000000000000, -68.32828612846148530, -21.58087353894176275 ) ) ;
#18327=CARTESIAN_POINT ( 'NONE',  ( -5.107860025166927720, -50.62490018645955558, 41.07729128472254843 ) ) ;
#18382=CARTESIAN_POINT ( 'NONE',  ( -5.000000000000000000, 14.89980876190746351, 69.94558486267358433 ) ) ;
#18437=( BOUNDED_SURFACE ( )  B_SPLINE_SURFACE ( 3, 2, ( 
 ( #10965, #5308, #73960 ),
 ( #45289, #68300, #28310 ),
 ( #410, #16599, #12436 ),
 ( #52441, #42211, #64501 ),
 ( #24123, #35468, #58481 ),
 ( #63753, #1867, #64127 ),
 ( #69791, #36201, #18475 ),
 ( #40743, #12801, #1520 ),
 ( #29798, #1143, #47136 ),
 ( #41487, #35832, #58847 ),
 ( #6789, #52809, #70167 ),
 ( #12070, #6427, #46766 ),
 ( #35106, #7160, #24498 ),
 ( #30165, #19206, #29431 ),
 ( #47502, #53182, #70527 ),
 ( #17727, #58118, #70891 ),
 ( #778, #23763, #18843 ),
 ( #41851, #64860, #30536 ) ),
 .UNSPECIFIED., .F., .F., .F. ) 
 B_SPLINE_SURFACE_WITH_KNOTS ( ( 4, 2, 2, 2, 2, 2, 2, 2, 4 ),
 ( 3, 3 ),
 ( 0.04202945594032914123, 0.04396162471216785717, 0.04589379348400656616, 0.04782596225584527516, 0.04975813102768399110, 0.05169029979952270704, 0.05265638418544206500, 0.05362246857136142297, 0.05748680611503884791 ),
 ( 0.000000000000000000, 1.000000000000000000 ),
 .UNSPECIFIED. ) 
 GEOMETRIC_REPRESENTATION_ITEM ( )  RATIONAL_B_SPLINE_SURFACE ( (
 ( 1.000000000000000000, 0.6241276099608163985, 1.000000000000000000),
 ( 1.000000000000000000, 0.6218761496800119248, 1.000000000000000000),
 ( 1.000000000000000000, 0.6198047272364380911, 1.000000000000000000),
 ( 1.000000000000000000, 0.6161935119824036855, 1.000000000000000000),
 ( 1.000000000000000000, 0.6146642324079838460, 1.000000000000000000),
 ( 1.000000000000000000, 0.6121850116872165071, 1.000000000000000000),
 ( 1.000000000000000000, 0.6112350889399397191, 1.000000000000000000),
 ( 1.000000000000000000, 0.6099522725973182125, 1.000000000000000000),
 ( 1.000000000000000000, 0.6096208180308724245, 1.000000000000000000),
 ( 1.000000000000000000, 0.6096183796348639827, 1.000000000000000000),
 ( 1.000000000000000000, 0.6099422200103278291, 1.000000000000000000),
 ( 1.000000000000000000, 0.6109087447822608707, 1.000000000000000000),
 ( 1.000000000000000000, 0.6113123981687891284, 1.000000000000000000),
 ( 1.000000000000000000, 0.6122677719809712649, 1.000000000000000000),
 ( 1.000000000000000000, 0.6128199619020906486, 1.000000000000000000),
 ( 1.000000000000000000, 0.6159350830266026033, 1.000000000000000000),
 ( 1.000000000000000000, 0.6195556778515390883, 1.000000000000000000),
 ( 1.000000000000000000, 0.6241278272307889674, 1.000000000000000000) ) ) 
 REPRESENTATION_ITEM ( '' )  SURFACE ( )  );
#18445=CARTESIAN_POINT ( 'NONE',  ( 1.877992804784440972, 65.87054549411425342, 26.34444121134915662 ) ) ;
#18454=ORIENTED_EDGE ( 'NONE', *, *, #23183, .T. ) ;
#18475=CARTESIAN_POINT ( 'NONE',  ( -2.591411123065824551, 10.27614846265000637, -63.77676950207272455 ) ) ;
#18487=FACE_OUTER_BOUND ( 'NONE', #24400, .T. ) ;
#18508=CARTESIAN_POINT ( 'NONE',  ( 0.8721677472748811111, -16.44158143986581777, 68.58266913489941885 ) ) ;
#18569=VERTEX_POINT ( 'NONE', #28290 ) ;
#18575=LINE ( 'NONE', #41585, #42228 ) ;
#18669=AXIS2_PLACEMENT_3D ( 'NONE', #17630, #63654, #11980 ) ;
#18733=DIRECTION ( 'NONE',  ( 1.000000000000000000, 0.000000000000000000, 0.000000000000000000 ) ) ;
#18756=CARTESIAN_POINT ( 'NONE',  ( 5.000000000000000000, 16.24494643555759410, -69.83755725260752456 ) ) ;
#18789=CARTESIAN_POINT ( 'NONE',  ( -5.000000000000000888, 62.88740100213682638, -24.06179116403683338 ) ) ;
#18817=CARTESIAN_POINT ( 'NONE',  ( 0.4501631047671865726, 67.59340899456755380, 20.03485802339891109 ) ) ;
#18843=CARTESIAN_POINT ( 'NONE',  ( 6.308070865145555040, 10.25011764679231341, -64.85270989085731230 ) ) ;
#18926=EDGE_CURVE ( 'NONE', #44017, #25179, #62803, .T. ) ;
#19031=CIRCLE ( 'NONE', #73219, 71.70204102886728492 ) ;
#19037=CARTESIAN_POINT ( 'NONE',  ( 3.544144923083259791, 50.27229464832175410, 40.88493206427750692 ) ) ;
#19054=CARTESIAN_POINT ( 'NONE',  ( 5.000000000000000000, -18.53862685874497274, -23.57305537018140384 ) ) ;
#19064=CARTESIAN_POINT ( 'NONE',  ( 5.000000000000000000, -18.53862685874495142, 23.57305537018116581 ) ) ;
#19109=EDGE_CURVE ( 'NONE', #29247, #27168, #9769, .T. ) ;
#19110=CARTESIAN_POINT ( 'NONE',  ( -5.000000000000000000, 10.25161785469021680, 64.79070129774557074 ) ) ;
#19142=ADVANCED_FACE ( 'NONE', ( #53756 ), #7364, .F. ) ;
#19151=CARTESIAN_POINT ( 'NONE',  ( -5.000000000000000000, -50.64189880742115690, 41.08656465431877791 ) ) ;
#19162=CARTESIAN_POINT ( 'NONE',  ( -0.4368895104719995870, 16.44602605510714710, 68.55492853905352035 ) ) ;
#19163=CARTESIAN_POINT ( 'NONE',  ( -0.8721677472748841087, 67.61512445009852001, 20.05250736213596952 ) ) ;
#19174=CARTESIAN_POINT ( 'NONE',  ( -1.558072418983263985, 67.68461058694082055, 20.10890959968151748 ) ) ;
#19179=EDGE_CURVE ( 'NONE', #20924, #15493, #14154, .T. ) ;
#19206=CARTESIAN_POINT ( 'NONE',  ( 1.882291019709046553, 10.12018455450524002, -70.22327770540687197 ) ) ;
#19298=AXIS2_PLACEMENT_3D ( 'NONE', #11181, #253, #56466 ) ;
#19321=CARTESIAN_POINT ( 'NONE',  ( 0.000000000000000000, 0.000000000000000000, 0.000000000000000000 ) ) ;
#19322=ORIENTED_EDGE ( 'NONE', *, *, #48597, .F. ) ;
#19329=DIRECTION ( 'NONE',  ( 0.000000000000000000, 1.387778780781445676E-15, 1.000000000000000000 ) ) ;
#19349=ORIENTED_EDGE ( 'NONE', *, *, #28386, .F. ) ;
#19383=CARTESIAN_POINT ( 'NONE',  ( -5.000000000000000000, 0.000000000000000000, 0.000000000000000000 ) ) ;
#19403=CARTESIAN_POINT ( 'NONE',  ( -4.999999999999952927, -68.60357193678709109, 20.85024232999324667 ) ) ;
#19427=CARTESIAN_POINT ( 'NONE',  ( 5.000000000000000000, -32.28817737728140003, -1.075528555105620399E-13 ) ) ;
#19436=DIRECTION ( 'NONE',  ( 1.000000000000000000, -0.000000000000000000, 0.000000000000000000 ) ) ;
#19443=VERTEX_POINT ( 'NONE', #7558 ) ;
#19491=PLANE ( 'NONE',  #15003 ) ;
#19538=CARTESIAN_POINT ( 'NONE',  ( -2.436599634630237432, 67.82108862182660403, 20.21956363439100457 ) ) ;
#19564=CARTESIAN_POINT ( 'NONE',  ( 5.000000000000000000, -11.82742353449333095, -68.45184936927694253 ) ) ;
#19585=CIRCLE ( 'NONE', #3955, 5.000000000000000000 ) ;
#19599=CARTESIAN_POINT ( 'NONE',  ( 0.000000000000000000, 0.000000000000000000, 0.000000000000000000 ) ) ;
#19616=ADVANCED_FACE ( 'NONE', ( #26369 ), #13925, .T. ) ;
#19621=CARTESIAN_POINT ( 'NONE',  ( -2.978189300774432354E-14, -67.59332269700065865, -20.03478791450352858 ) ) ;
#19634=ORIENTED_EDGE ( 'NONE', *, *, #70233, .F. ) ;
#19636=CARTESIAN_POINT ( 'NONE',  ( 4.999999999999999112, 13.22058908515350062, 69.49198671174478648 ) ) ;
#19650=EDGE_CURVE ( 'NONE', #60656, #18569, #60937, .T. ) ;
#19723=CARTESIAN_POINT ( 'NONE',  ( -2.589639417659073573, 50.10293296561771115, -40.79253907059123208 ) ) ;
#19792=VECTOR ( 'NONE', #37304, 1000.000000000000227 ) ;
#19795=CARTESIAN_POINT ( 'NONE',  ( 1.558072418983049268, 67.68461058694150267, -20.10890959967917624 ) ) ;
#19798=ORIENTED_EDGE ( 'NONE', *, *, #53301, .F. ) ;
#19807=CARTESIAN_POINT ( 'NONE',  ( 5.000000000000000000, 0.000000000000000000, 0.000000000000000000 ) ) ;
#19941=CARTESIAN_POINT ( 'NONE',  ( -1.688721909672344479, 49.97488762307396115, -40.72268565194232082 ) ) ;
#20029=ORIENTED_EDGE ( 'NONE', *, *, #66198, .T. ) ;
#20101=AXIS2_PLACEMENT_3D ( 'NONE', #13359, #6987, #18305 ) ;
#20106=CARTESIAN_POINT ( 'NONE',  ( 13.99999999999999822, 2.249999999994893862, 10.23492587299426404 ) ) ;
#20109=ADVANCED_FACE ( 'NONE', ( #17300 ), #64129, .T. ) ;
#20147=CARTESIAN_POINT ( 'NONE',  ( -4.999999999999999112, 52.85372778481288947, 48.38359481482947899 ) ) ;
#20153=CARTESIAN_POINT ( 'NONE',  ( 5.086519500874520539, -10.26068667857087391, -64.41585657734346171 ) ) ;
#20164=VERTEX_POINT ( 'NONE', #68992 ) ;
#20210=CARTESIAN_POINT ( 'NONE',  ( -4.999999999999999112, 10.28276986844631935, 65.17752827135416283 ) ) ;
#20257=ORIENTED_EDGE ( 'NONE', *, *, #7035, .F. ) ;
#20266=EDGE_CURVE ( 'NONE', #57466, #71522, #26714, .T. ) ;
#20279=CARTESIAN_POINT ( 'NONE',  ( -4.193070328474950870, 50.40098303874115260, 40.95513628906723369 ) ) ;
#20300=LINE ( 'NONE', #61053, #6544 ) ;
#20312=ORIENTED_EDGE ( 'NONE', *, *, #58745, .T. ) ;
#20339=CARTESIAN_POINT ( 'NONE',  ( 2.995737153982848344, 16.37687539610414333, 68.98994273414960787 ) ) ;
#20348=CARTESIAN_POINT ( 'NONE',  ( -3.428378827827395892, -68.02396499344693837, -20.38382289158757033 ) ) ;
#20383=ORIENTED_EDGE ( 'NONE', *, *, #55931, .T. ) ;
#20411=CARTESIAN_POINT ( 'NONE',  ( -5.000000000000000000, 10.00000000000000000, 75.19090595827292134 ) ) ;
#20494=ORIENTED_EDGE ( 'NONE', *, *, #8623, .F. ) ;
#20507=CARTESIAN_POINT ( 'NONE',  ( -7.456155213531540760, -10.23501372118566266, 65.47700548259878417 ) ) ;
#20519=CARTESIAN_POINT ( 'NONE',  ( -5.000000000000000000, 52.35862550122891435, 48.98731492261470777 ) ) ;
#20547=VERTEX_POINT ( 'NONE', #39812 ) ;
#20548=CARTESIAN_POINT ( 'NONE',  ( -5.000000000000000000, 10.28295106684163684, -65.17663434001590872 ) ) ;
#20595=AXIS2_PLACEMENT_3D ( 'NONE', #12207, #58262, #31039 ) ;
#20596=CARTESIAN_POINT ( 'NONE',  ( -5.000000000000000000, -60.90295814858238543, -23.31388853594834032 ) ) ;
#20620=ADVANCED_FACE ( 'NONE', ( #27369 ), #33809, .F. ) ;
#20654=CARTESIAN_POINT ( 'NONE',  ( 5.000000000000000000, -52.28182290968072010, 42.43119126381040473 ) ) ;
#20662=CARTESIAN_POINT ( 'NONE',  ( 0.8419854211626158769, 49.91401432488694923, 40.68947704085089612 ) ) ;
#20672=VECTOR ( 'NONE', #14592, 1000.000000000000000 ) ;
#20706=EDGE_CURVE ( 'NONE', #67442, #24245, #72538, .T. ) ;
#20776=EDGE_LOOP ( 'NONE', ( #27523, #66144, #17032, #7628 ) ) ;
#20866=EDGE_CURVE ( 'NONE', #27257, #17726, #29616, .T. ) ;
#20909=CARTESIAN_POINT ( 'NONE',  ( 5.126106709302931996, -16.23426604260537331, -69.90716554746668976 ) ) ;
#20924=VERTEX_POINT ( 'NONE', #32598 ) ;
#20925=CARTESIAN_POINT ( 'NONE',  ( -5.000000000000000000, 11.82742353449332917, -68.45184936927694253 ) ) ;
#20946=DIRECTION ( 'NONE',  ( 1.000000000000000000, 0.000000000000000000, -0.000000000000000000 ) ) ;
#20982=CARTESIAN_POINT ( 'NONE',  ( 2.990854866098545894, -66.07503719301321610, -26.46919450144743635 ) ) ;
#21002=CARTESIAN_POINT ( 'NONE',  ( 5.126106709302927555, -52.42424824936786365, 49.01286957842454939 ) ) ;
#21035=CARTESIAN_POINT ( 'NONE',  ( 2.124081043562902948, -60.31560147600172428, -22.95556260996213283 ) ) ;
#21036=CARTESIAN_POINT ( 'NONE',  ( 4.999999999999999112, 63.46295559274079068, 24.14151313015431199 ) ) ;
#21062=CARTESIAN_POINT ( 'NONE',  ( 0.000000000000000000, 0.000000000000000000, -81.50000000000000000 ) ) ;
#21094=CARTESIAN_POINT ( 'NONE',  ( 2.219371606097089611, -51.37365828841584658, -48.60677221569350337 ) ) ;
#21109=CARTESIAN_POINT ( 'NONE',  ( 4.330454160168551780, 16.29811171461319574, 69.49285720719198878 ) ) ;
#21206=FACE_OUTER_BOUND ( 'NONE', #71489, .T. ) ;
#21215=ORIENTED_EDGE ( 'NONE', *, *, #19109, .F. ) ;
#21239=VERTEX_POINT ( 'NONE', #56344 ) ;
#21249=DIRECTION ( 'NONE',  ( 0.000000000000000000, 0.000000000000000000, -1.000000000000000000 ) ) ;
#21261=CARTESIAN_POINT ( 'NONE',  ( -3.074111742560043936, -16.37317034319901410, 69.01341173090899872 ) ) ;
#21280=CARTESIAN_POINT ( 'NONE',  ( 0.4501631047601223345, -16.44600848780494218, -68.55503832938644848 ) ) ;
#21291=ORIENTED_EDGE ( 'NONE', *, *, #54232, .T. ) ;
#21300=CARTESIAN_POINT ( 'NONE',  ( -4.999999999999996447, 16.24494643555759410, -69.83755725260752456 ) ) ;
#21323=CARTESIAN_POINT ( 'NONE',  ( -14.00000000000000000, 0.000000000000000000, 17.50000000000000000 ) ) ;
#21344=CARTESIAN_POINT ( 'NONE',  ( 4.999999999999999112, 52.15374455614202276, -42.28282461816495186 ) ) ;
#21354=CARTESIAN_POINT ( 'NONE',  ( -1.780377099648641437, -67.71330631781127352, -20.13219356122175441 ) ) ;
#21360=CARTESIAN_POINT ( 'NONE',  ( -5.000000000000000000, -11.00774715070965648, -67.37702390743055503 ) ) ;
#21368=AXIS2_PLACEMENT_3D ( 'NONE', #30285, #7648, #30653 ) ;
#21380=B_SPLINE_CURVE_WITH_KNOTS ( 'NONE', 3,
 ( #29497, #64568, #69112, #23455, #12865, #63442, #6120, #34435, #105, #35901, #57813, #24561, #58918, #844, #23830, #475, #57436, #46094, #7228, #29124 ),
 .UNSPECIFIED., .F., .F.,
 ( 4, 2, 2, 2, 2, 2, 2, 2, 2, 4 ),
 ( 2.797157557069881010E-17, 0.001156441540184027089, 0.001734662310276020251, 0.002312883080368013412, 0.003469324620551992363, 0.004625766160735971314, 0.005782207700919949830, 0.006938649241103929215, 0.008095090781287906864, 0.009251532321471885381 ),
 .UNSPECIFIED. ) ;
#21381=DIRECTION ( 'NONE',  ( 0.000000000000000000, 0.000000000000000000, -1.000000000000000000 ) ) ;
#21399=CARTESIAN_POINT ( 'NONE',  ( 4.999999999999999112, -52.15374455614175275, 42.28282461816533555 ) ) ;
#21464=CARTESIAN_POINT ( 'NONE',  ( -0.6547826978428695766, -49.91450260127106731, -40.68974341348058488 ) ) ;
#21479=CARTESIAN_POINT ( 'NONE',  ( 4.465349678524270338, 10.10202304668574413, 70.97395336192860782 ) ) ;
#21503=CARTESIAN_POINT ( 'NONE',  ( 0.4501631047599979341, 51.14740050676149963, -48.52018030598747345 ) ) ;
#21525=AXIS2_PLACEMENT_3D ( 'NONE', #70778, #665, #53441 ) ;
#21578=CARTESIAN_POINT ( 'NONE',  ( 3.511653767256979197, -68.04552192806536937, 20.40125235306631524 ) ) ;
#21594=ORIENTED_EDGE ( 'NONE', *, *, #4278, .F. ) ;
#21618=AXIS2_PLACEMENT_3D ( 'NONE', #29078, #57390, #6806 ) ;
#21651=CARTESIAN_POINT ( 'NONE',  ( -2.219371606101216976, -16.40787039054615448, -68.79427927095674988 ) ) ;
#21663=CARTESIAN_POINT ( 'NONE',  ( -5.000000000000000000, -65.00653492603748873, 24.02639942437790310 ) ) ;
#21665=FACE_OUTER_BOUND ( 'NONE', #67777, .T. ) ;
#21684=EDGE_LOOP ( 'NONE', ( #47603, #19634, #67814, #23138 ) ) ;
#21700=ORIENTED_EDGE ( 'NONE', *, *, #60460, .T. ) ;
#21717=AXIS2_PLACEMENT_3D ( 'NONE', #21062, #48978, #44086 ) ;
#21722=CARTESIAN_POINT ( 'NONE',  ( -1.882291019709504631, -65.87523470714120322, -26.34730193751288851 ) ) ;
#21744=CARTESIAN_POINT ( 'NONE',  ( 4.465349678513689469, -56.41423509509540679, 44.23558526900774979 ) ) ;
#21755=VERTEX_POINT ( 'NONE', #49837 ) ;
#21769=CARTESIAN_POINT ( 'NONE',  ( 5.000000000000000888, -52.62657404299726238, 48.70092614269855602 ) ) ;
#21777=CARTESIAN_POINT ( 'NONE',  ( -4.615726161707419450, -16.27701803902728273, 69.62876280158647546 ) ) ;
#21801=CARTESIAN_POINT ( 'NONE',  ( 5.000000000000000000, 50.64189880742144823, -41.08656465431842975 ) ) ;
#21807=VERTEX_POINT ( 'NONE', #62269 ) ;
#21828=CARTESIAN_POINT ( 'NONE',  ( -3.074111742570392547, -51.58078258920560444, -48.68628732315601582 ) ) ;
#21854=CIRCLE ( 'NONE', #47112, 4.999999999999997335 ) ;
#21878=ORIENTED_EDGE ( 'NONE', *, *, #71554, .T. ) ;
#21930=AXIS2_PLACEMENT_3D ( 'NONE', #29653, #35334, #17961 ) ;
#21964=CARTESIAN_POINT ( 'NONE',  ( -5.000000000000000000, 60.90295814858222201, 23.31388853594875599 ) ) ;
#22024=CARTESIAN_POINT ( 'NONE',  ( -1.704527592502766309, 10.27896685065642934, -63.66027613114052031 ) ) ;
#22035=CARTESIAN_POINT ( 'NONE',  ( 0.8419854211626223162, -49.91401432488723344, -40.68947704085055506 ) ) ;
#22062=B_SPLINE_CURVE_WITH_KNOTS ( 'NONE', 3,
 ( #60644, #19162, #42164, #59902, #8965, #31978, #53877, #2187 ),
 .UNSPECIFIED., .F., .F.,
 ( 4, 2, 2, 4 ),
 ( 0.005256334970490775943, 0.006570121696662011880, 0.007883908422833247817, 0.01051148187517572143 ),
 .UNSPECIFIED. ) ;
#22076=VERTEX_POINT ( 'NONE', #54590 ) ;
#22079=CARTESIAN_POINT ( 'NONE',  ( 5.000000000000000000, 60.11723469343148452, -46.25570701698029552 ) ) ;
#22080=CARTESIAN_POINT ( 'NONE',  ( 4.999999999999999112, 51.88457047716768500, -42.00159762951405895 ) ) ;
#22088=DIRECTION ( 'NONE',  ( 0.000000000000000000, 0.000000000000000000, -1.000000000000000000 ) ) ;
#22094=CARTESIAN_POINT ( 'NONE',  ( -2.069125466538180191, -65.90280720052957975, -26.36412295902851355 ) ) ;
#22115=CARTESIAN_POINT ( 'NONE',  ( -0.4451317748922283268, -51.14719335908487352, 48.52010116548744634 ) ) ;
#22159=EDGE_CURVE ( 'NONE', #63554, #21755, #37604, .T. ) ;
#22174=CARTESIAN_POINT ( 'NONE',  ( 5.000000000000000000, -66.79063484153797958, 23.29724706625358266 ) ) ;
#22177=CARTESIAN_POINT ( 'NONE',  ( 1.736494649845411908, -51.27805538754646619, 48.57014059985625209 ) ) ;
#22203=CARTESIAN_POINT ( 'NONE',  ( 0.4451317748863459212, -51.14719335908540643, -48.52010116548649421 ) ) ;
#22215=CARTESIAN_POINT ( 'NONE',  ( 0.7581620860333473377, 10.12340554704894657, 70.09014334687759629 ) ) ;
#22230=DIRECTION ( 'NONE',  ( -0.000000000000000000, -1.000000000000000000, -0.000000000000000000 ) ) ;
#22233=DIRECTION ( 'NONE',  ( 1.000000000000000000, 0.000000000000000000, 0.000000000000000000 ) ) ;
#22266=VERTEX_POINT ( 'NONE', #56819 ) ;
#22311=CARTESIAN_POINT ( 'NONE',  ( -4.999999999999999112, -51.88457047716706683, -42.00159762951478370 ) ) ;
#22313=CARTESIAN_POINT ( 'NONE',  ( -2.591411123065472832, -60.37037679142518698, 22.98897912932123688 ) ) ;
#22316=CARTESIAN_POINT ( 'NONE',  ( 5.000000000000000000, 52.35862550122891435, 48.98731492261470777 ) ) ;
#22324=CARTESIAN_POINT ( 'NONE',  ( 5.000000000000000000, 10.25159769123454900, 64.79153472057838314 ) ) ;
#22366=CARTESIAN_POINT ( 'NONE',  ( 0.4451317748927060558, -16.44604352396231661, 68.55481936398555831 ) ) ;
#22386=CARTESIAN_POINT ( 'NONE',  ( -0.3752463838877027058, -10.12385607954436573, -70.07152133708838448 ) ) ;
#22394=CARTESIAN_POINT ( 'NONE',  ( -5.000000000000000000, -50.64189880742115690, 41.08656465431877791 ) ) ;
#22424=CARTESIAN_POINT ( 'NONE',  ( 5.000000000000000000, -29.68417822476651580, -4.268394125863113509 ) ) ;
#22481=CARTESIAN_POINT ( 'NONE',  ( -7.456155213548138150, 61.82225697226427030, -23.87472085067443572 ) ) ;
#22494=DIRECTION ( 'NONE',  ( 0.000000000000000000, 0.000000000000000000, -1.000000000000000000 ) ) ;
#22507=CARTESIAN_POINT ( 'NONE',  ( 5.000000000000000000, -16.14408868864072844, -27.96238185062390613 ) ) ;
#22519=CARTESIAN_POINT ( 'NONE',  ( -0.8761883848702631816, -16.44150283900215825, 68.58316157020809101 ) ) ;
#22522=FACE_OUTER_BOUND ( 'NONE', #26573, .T. ) ;
#22530=VERTEX_POINT ( 'NONE', #53749 ) ;
#22545=CARTESIAN_POINT ( 'NONE',  ( 4.999999999999999112, -65.00666015986186608, 24.03732210400530178 ) ) ;
#22590=CARTESIAN_POINT ( 'NONE',  ( 5.086519500888148748, 10.26068667857073358, 64.41585657734925974 ) ) ;
#22604=DIRECTION ( 'NONE',  ( 0.000000000000000000, 0.000000000000000000, -1.000000000000000000 ) ) ;
#22614=EDGE_CURVE ( 'NONE', #17271, #46951, #10483, .T. ) ;
#22633=AXIS2_PLACEMENT_3D ( 'NONE', #22507, #68546, #62877 ) ;
#22673=EDGE_CURVE ( 'NONE', #20547, #6191, #42042, .T. ) ;
#22687=CARTESIAN_POINT ( 'NONE',  ( 4.231687259402619361, 68.27410168872769702, -20.58597903916443173 ) ) ;
#22689=CARTESIAN_POINT ( 'NONE',  ( -5.000000000000000000, -53.31073972600171373, -44.28411094576001261 ) ) ;
#22691=CARTESIAN_POINT ( 'NONE',  ( 5.107860025160634088, -60.88642786446147426, 23.30380398316933110 ) ) ;
#22697=CARTESIAN_POINT ( 'NONE',  ( 1.736494649845414795, 67.70200331863051701, 20.12302832235323180 ) ) ;
#22701=ORIENTED_EDGE ( 'NONE', *, *, #69117, .F. ) ;
#22703=CARTESIAN_POINT ( 'NONE',  ( 5.000000000000000888, 10.54112798502250214, 66.30787999718575065 ) ) ;
#22744=CARTESIAN_POINT ( 'NONE',  ( 5.126144196591232216, -16.23426282122703768, 69.90718656545267606 ) ) ;
#22755=ORIENTED_EDGE ( 'NONE', *, *, #25290, .F. ) ;
#22764=CARTESIAN_POINT ( 'NONE',  ( -2.069125466540922886, -10.11940336925128214, -70.25556669588459613 ) ) ;
#22778=CARTESIAN_POINT ( 'NONE',  ( 2.957351242930898602E-11, 51.14729664189404446, -48.52014062454985321 ) ) ;
#22797=EDGE_LOOP ( 'NONE', ( #24588, #15285, #68417, #65299 ) ) ;
#22817=AXIS2_PLACEMENT_3D ( 'NONE', #56207, #15071, #38105 ) ;
#22840=CARTESIAN_POINT ( 'NONE',  ( -5.126106709314333543, 52.42424824937320693, 49.01286957842763314 ) ) ;
#22851=CARTESIAN_POINT ( 'NONE',  ( 3.407298021510787311, -16.35582233947175013, -69.12343428065700834 ) ) ;
#22859=CARTESIAN_POINT ( 'NONE',  ( 5.000000000000001776, -63.46295559274096831, -24.14151313015386080 ) ) ;
#22866=CARTESIAN_POINT ( 'NONE',  ( -1.558072418987807239, -51.25713184919958110, 48.56213741370790160 ) ) ;
#22903=CARTESIAN_POINT ( 'NONE',  ( -5.000000000000000000, -16.24494643555759410, 69.83755725260752456 ) ) ;
#22914=ORIENTED_EDGE ( 'NONE', *, *, #64844, .F. ) ;
#22929=CARTESIAN_POINT ( 'NONE',  ( -4.999999999999999112, -10.60557809245594463, 66.49298242784793445 ) ) ;
#22978=CARTESIAN_POINT ( 'NONE',  ( -6.308070865149355555, 10.25011764679247328, 64.85270989085067583 ) ) ;
#23027=ORIENTED_EDGE ( 'NONE', *, *, #51410, .T. ) ;
#23058=CARTESIAN_POINT ( 'NONE',  ( 4.193070328474942876, 10.26769692241485643, 64.12609983179218887 ) ) ;
#23070=CARTESIAN_POINT ( 'NONE',  ( -5.000000000000000000, -52.15374455614144722, -42.28282461816569082 ) ) ;
#23082=CARTESIAN_POINT ( 'NONE',  ( 5.000000000000000000, 11.82742353449332917, 68.45184936927694253 ) ) ;
#23094=CARTESIAN_POINT ( 'NONE',  ( -5.000000000000001776, -67.10993666412726100, -23.06595724273644876 ) ) ;
#23124=CARTESIAN_POINT ( 'NONE',  ( -1.308779242298911516, -10.28008949575750641, 63.61387346696258049 ) ) ;
#23138=ORIENTED_EDGE ( 'NONE', *, *, #7790, .F. ) ;
#23183=EDGE_CURVE ( 'NONE', #5956, #2769, #45060, .T. ) ;
#23214=FACE_OUTER_BOUND ( 'NONE', #53605, .T. ) ;
#23237=CARTESIAN_POINT ( 'NONE',  ( 5.000000000000000000, -64.62379132009250782, -24.09319349500408691 ) ) ;
#23242=CARTESIAN_POINT ( 'NONE',  ( -3.496982156821212939, 68.06496700477899253, -20.41687962716563121 ) ) ;
#23297=DIRECTION ( 'NONE',  ( 1.000000000000000000, -0.000000000000000000, -0.000000000000000000 ) ) ;
#23299=CARTESIAN_POINT ( 'NONE',  ( -4.999999999999999112, -13.22058908515350062, 69.49198671174478648 ) ) ;
#23300=CARTESIAN_POINT ( 'NONE',  ( 4.999999999999999112, -64.62627855237444408, 24.10294814404683450 ) ) ;
#23309=VECTOR ( 'NONE', #32269, 1000.000000000000000 ) ;
#23310=EDGE_CURVE ( 'NONE', #63044, #71522, #64611, .T. ) ;
#23336=CARTESIAN_POINT ( 'NONE',  ( -5.000000000000000000, -53.34243969459512869, 47.33397984627169564 ) ) ;
#23357=CARTESIAN_POINT ( 'NONE',  ( -1.780377099649267381, 67.71330631781158615, 20.13219356122112913 ) ) ;
#23439=CARTESIAN_POINT ( 'NONE',  ( -5.000000000000000000, -52.84347807771128203, -43.21644271080234745 ) ) ;
#23452=ORIENTED_EDGE ( 'NONE', *, *, #40655, .T. ) ;
#23455=CARTESIAN_POINT ( 'NONE',  ( 4.999999999999999112, 68.02455775458950882, -22.06917953199437221 ) ) ;
#23480=ORIENTED_EDGE ( 'NONE', *, *, #58421, .F. ) ;
#23494=CARTESIAN_POINT ( 'NONE',  ( 4.465384415997275092, -10.10202268796506253, 70.97396818905022542 ) ) ;
#23525=CARTESIAN_POINT ( 'NONE',  ( 0.4320110153365238070, -49.91454558245994377, 40.68976686129099818 ) ) ;
#23576=DIRECTION ( 'NONE',  ( -1.000000000000000000, 0.000000000000000000, 0.000000000000000000 ) ) ;
#23607=CARTESIAN_POINT ( 'NONE',  ( 5.000000000000000888, -62.31673578527537671, -23.93255728291397944 ) ) ;
#23612=CARTESIAN_POINT ( 'NONE',  ( 0.3752463838824955378, 65.74564559952163734, -26.26824411940089021 ) ) ;
#23631=DIRECTION ( 'NONE',  ( 0.000000000000000000, 0.8536788251725985210, 0.5207998305029790664 ) ) ;
#23676=CARTESIAN_POINT ( 'NONE',  ( 5.000000000000000000, -62.32183698944616879, 23.94439461060377994 ) ) ;
#23686=CARTESIAN_POINT ( 'NONE',  ( 0.4320110153365303018, 60.19564456717396439, 22.88238106212169498 ) ) ;
#23716=CARTESIAN_POINT ( 'NONE',  ( -1.558072418983094343, 16.42747873774318990, 68.67104701338824668 ) ) ;
#23736=CARTESIAN_POINT ( 'NONE',  ( 0.000000000000000000, 0.000000000000000000, -17.50000000000000000 ) ) ;
#23763=CARTESIAN_POINT ( 'NONE',  ( 3.728321214226603786, 10.10963409588449835, -70.65936332831182654 ) ) ;
#23830=CARTESIAN_POINT ( 'NONE',  ( 5.000000000000000000, 63.46149047932947695, -24.14127879314006719 ) ) ;
#23832=( BOUNDED_SURFACE ( )  B_SPLINE_SURFACE ( 3, 2, ( 
 ( #50545, #2758, #27160 ),
 ( #61874, #44899, #54072 ),
 ( #67905, #44150, #16199 ),
 ( #37088, #61500, #4538 ),
 ( #15834, #55856, #33225 ),
 ( #38868, #15461, #31424 ),
 ( #2380, #67537, #25377 ),
 ( #38498, #10195, #48394 ),
 ( #21503, #8409, #71773 ),
 ( #60091, #39238, #62238 ),
 ( #44522, #8040, #71397 ),
 ( #31046, #48765, #32849 ),
 ( #56224, #73561, #19723 ),
 ( #50177, #10565, #9823 ),
 ( #27912, #45267, #42734 ),
 ( #33596, #56602, #14050 ),
 ( #4918, #54449, #50922 ),
 ( #65748, #4173, #73934 ) ),
 .UNSPECIFIED., .F., .F., .F. ) 
 B_SPLINE_SURFACE_WITH_KNOTS ( ( 4, 2, 2, 2, 2, 2, 2, 2, 4 ),
 ( 3, 3 ),
 ( 0.04202945594034795951, 0.04396162471218430234, 0.04589379348402064518, 0.04782596225585698801, 0.04975813102769333085, 0.05169029979952967369, 0.05265638418544784510, 0.05362246857136601652, 0.05748680611503870913 ),
 ( 0.000000000000000000, 1.000000000000000000 ),
 .UNSPECIFIED. ) 
 GEOMETRIC_REPRESENTATION_ITEM ( )  RATIONAL_B_SPLINE_SURFACE ( (
 ( 1.000000000000000000, 0.6241276099607513395, 1.000000000000000000),
 ( 1.000000000000000000, 0.6218761496800012667, 1.000000000000000000),
 ( 1.000000000000000000, 0.6198047272363184090, 1.000000000000000000),
 ( 1.000000000000000000, 0.6161935119824332174, 1.000000000000000000),
 ( 1.000000000000000000, 0.6146642324076686537, 1.000000000000000000),
 ( 1.000000000000000000, 0.6121850116874761882, 1.000000000000000000),
 ( 1.000000000000000000, 0.6112350889399633669, 1.000000000000000000),
 ( 1.000000000000000000, 0.6099522725972716941, 1.000000000000000000),
 ( 1.000000000000000000, 0.6096208180308003710, 1.000000000000000000),
 ( 1.000000000000000000, 0.6096183796349364803, 1.000000000000000000),
 ( 1.000000000000000000, 0.6099422200104442915, 1.000000000000000000),
 ( 1.000000000000000000, 0.6109087447822132422, 1.000000000000000000),
 ( 1.000000000000000000, 0.6113123981686904296, 1.000000000000000000),
 ( 1.000000000000000000, 0.6122677719810877273, 1.000000000000000000),
 ( 1.000000000000000000, 0.6128199619020645583, 1.000000000000000000),
 ( 1.000000000000000000, 0.6159350830267519283, 1.000000000000000000),
 ( 1.000000000000000000, 0.6195556778514385021, 1.000000000000000000),
 ( 1.000000000000000000, 0.6241278272307897446, 1.000000000000000000) ) ) 
 REPRESENTATION_ITEM ( '' )  SURFACE ( )  );
#23884=LINE ( 'NONE', #52558, #4975 ) ;
#23891=CARTESIAN_POINT ( 'NONE',  ( -5.000000000000000000, -10.26105934116143281, 64.40045319026697257 ) ) ;
#23898=DIRECTION ( 'NONE',  ( 0.000000000000000000, 0.000000000000000000, -1.000000000000000000 ) ) ;
#23902=CARTESIAN_POINT ( 'NONE',  ( 1.736494649845410798, -67.70200331863067333, -20.12302832235276995 ) ) ;
#23946=ORIENTED_EDGE ( 'NONE', *, *, #19179, .T. ) ;
#23959=CARTESIAN_POINT ( 'NONE',  ( 2.069125466538506597, 55.78340383127927993, 43.89144373685476808 ) ) ;
#23980=CARTESIAN_POINT ( 'NONE',  ( -1.506524674532530916, -55.70638416847222629, 43.84942669317716479 ) ) ;
#24025=EDGE_LOOP ( 'NONE', ( #40370, #40525, #11545, #8176 ) ) ;
#24064=CARTESIAN_POINT ( 'NONE',  ( -5.000000000000000000, 64.42874436516143533, -24.11656705754108998 ) ) ;
#24078=CARTESIAN_POINT ( 'NONE',  ( -1.882291019709195545, 10.12018455450467869, 70.22327770540688618 ) ) ;
#24106=EDGE_CURVE ( 'NONE', #20547, #36985, #25721, .T. ) ;
#24120=AXIS2_PLACEMENT_3D ( 'NONE', #63573, #33816, #34933 ) ;
#24123=CARTESIAN_POINT ( 'NONE',  ( -3.074111742571038697, 16.37317034319774223, -69.01341173091250880 ) ) ;
#24165=CARTESIAN_POINT ( 'NONE',  ( 5.000000000000000000, 68.60357193678729004, -20.85024232999272087 ) ) ;
#24227=ORIENTED_EDGE ( 'NONE', *, *, #12788, .T. ) ;
#24245=VERTEX_POINT ( 'NONE', #62672 ) ;
#24267=CARTESIAN_POINT ( 'NONE',  ( 5.000000000000000000, 10.00000000000000000, -75.19090595827292134 ) ) ;
#24282=B_SPLINE_CURVE_WITH_KNOTS ( 'NONE', 3,
 ( #17762, #41517, #6082, #58883, #52474, #63409, #57778, #41155, #51723, #69081 ),
 .UNSPECIFIED., .F., .F.,
 ( 4, 2, 2, 2, 4 ),
 ( 0.000000000000000000, 0.001314083742615453250, 0.002628167485230906500, 0.003942251227846359750, 0.005256334970461813000 ),
 .UNSPECIFIED. ) ;
#24310=ORIENTED_EDGE ( 'NONE', *, *, #58337, .F. ) ;
#24341=ORIENTED_EDGE ( 'NONE', *, *, #3858, .F. ) ;
#24355=EDGE_LOOP ( 'NONE', ( #13522, #51084, #36928, #21700 ) ) ;
#24363=CARTESIAN_POINT ( 'NONE',  ( 4.999999999999999112, -10.28276986844625718, 65.17752827135362281 ) ) ;
#24375=EDGE_CURVE ( 'NONE', #4853, #45416, #51358, .T. ) ;
#24378=DIRECTION ( 'NONE',  ( 0.000000000000000000, 0.000000000000000000, -1.000000000000000000 ) ) ;
#24400=EDGE_LOOP ( 'NONE', ( #62563, #57077, #61257, #61589 ) ) ;
#24405=CARTESIAN_POINT ( 'NONE',  ( -5.000000000000000000, 11.43937387734372813, 68.01947305042941139 ) ) ;
#24453=CARTESIAN_POINT ( 'NONE',  ( -2.266287154880006316, 10.27715108473168470, 63.73532778936321108 ) ) ;
#24497=ORIENTED_EDGE ( 'NONE', *, *, #34232, .T. ) ;
#24498=CARTESIAN_POINT ( 'NONE',  ( 2.589639417653364806, 10.27590863719303904, -63.78668228762732184 ) ) ;
#24520=CARTESIAN_POINT ( 'NONE',  ( -4.104248244559628667, -56.27889056305081539, -44.16174987545170438 ) ) ;
#24528=CARTESIAN_POINT ( 'NONE',  ( 0.4368895104719971445, -16.44602605510715065, 68.55492853905350614 ) ) ;
#24561=CARTESIAN_POINT ( 'NONE',  ( 5.000000000000000000, 65.00666015986205082, -24.03732210400486125 ) ) ;
#24578=VERTEX_POINT ( 'NONE', #24165 ) ;
#24588=ORIENTED_EDGE ( 'NONE', *, *, #17162, .F. ) ;
#24609=DIRECTION ( 'NONE',  ( 0.000000000000000000, 0.000000000000000000, -1.000000000000000000 ) ) ;
#24632=PLANE ( 'NONE',  #20595 ) ;
#24673=ORIENTED_EDGE ( 'NONE', *, *, #52876, .F. ) ;
#24694=CARTESIAN_POINT ( 'NONE',  ( -3.034644841523098859E-11, -67.59332269700080076, 20.03478791450305962 ) ) ;
#24699=CARTESIAN_POINT ( 'NONE',  ( -2.170320029210516033, -51.35721532638450526, 48.60044191894271393 ) ) ;
#24702=ORIENTED_EDGE ( 'NONE', *, *, #48158, .T. ) ;
#24746=CARTESIAN_POINT ( 'NONE',  ( 5.000000000000000000, 32.28817737728141424, 3.295974604355933479E-13 ) ) ;
#24826=ORIENTED_EDGE ( 'NONE', *, *, #49426, .F. ) ;
#24827=CARTESIAN_POINT ( 'NONE',  ( 2.591411123066388100, 60.37037679141896973, 22.98897912931846932 ) ) ;
#24851=ORIENTED_EDGE ( 'NONE', *, *, #71883, .F. ) ;
#24852=EDGE_CURVE ( 'NONE', #5956, #3856, #19031, .T. ) ;
#24855=CARTESIAN_POINT ( 'NONE',  ( -3.369429374625380280, 50.21921270641865220, -40.85597392306764419 ) ) ;
#24857=EDGE_LOOP ( 'NONE', ( #28540, #9854 ) ) ;
#24957=EDGE_CURVE ( 'NONE', #32715, #70301, #14689, .T. ) ;
#24993=VERTEX_POINT ( 'NONE', #43749 ) ;
#25025=ADVANCED_FACE ( 'NONE', ( #37349 ), #32447, .F. ) ;
#25067=CARTESIAN_POINT ( 'NONE',  ( 5.000000000000000000, 29.68417822476651580, 4.268394125863321342 ) ) ;
#25068=CARTESIAN_POINT ( 'NONE',  ( 4.104248244540173118, -10.10575198619682524, -70.81982386214420444 ) ) ;
#25097=ORIENTED_EDGE ( 'NONE', *, *, #40655, .F. ) ;
#25127=CARTESIAN_POINT ( 'NONE',  ( 5.000000000000000000, 11.68639849891297366, -68.31608016562482533 ) ) ;
#25140=EDGE_LOOP ( 'NONE', ( #8687, #37467, #25600, #3248 ) ) ;
#25151=CARTESIAN_POINT ( 'NONE',  ( 2.666560895877943341E-14, -16.44602605510714355, 68.55492853905353456 ) ) ;
#25179=VERTEX_POINT ( 'NONE', #50820 ) ;
#25199=CARTESIAN_POINT ( 'NONE',  ( 5.000000000000000000, 50.64189880742059557, 41.08656465431948845 ) ) ;
#25221=EDGE_LOOP ( 'NONE', ( #72660, #37206, #9362, #59045 ) ) ;
#25222=CARTESIAN_POINT ( 'NONE',  ( 4.999999999999999112, -14.70234347858786705, -69.93881661156081009 ) ) ;
#25290=EDGE_CURVE ( 'NONE', #42334, #4853, #16594, .T. ) ;
#25377=CARTESIAN_POINT ( 'NONE',  ( 2.591411123053213750, 50.09422832877228871, -40.78779037274974684 ) ) ;
#25416=VECTOR ( 'NONE', #69389, 1000.000000000000227 ) ;
#25441=CARTESIAN_POINT ( 'NONE',  ( 3.734423912254536848, -10.10901040137823514, -70.68514270129527688 ) ) ;
#25446=( GEOMETRIC_REPRESENTATION_CONTEXT ( 3 ) GLOBAL_UNCERTAINTY_ASSIGNED_CONTEXT ( ( #52880 ) ) GLOBAL_UNIT_ASSIGNED_CONTEXT ( ( #11761, #29488, #836 ) ) REPRESENTATION_CONTEXT ( 'NONE', 'WORKASPACE' ) );
#25449=CARTESIAN_POINT ( 'NONE',  ( 0.8912353796323385646, 67.61603573606910800, -20.05324848891999068 ) ) ;
#25543=CARTESIAN_POINT ( 'NONE',  ( -5.000000000000000888, -53.32026166094896524, 44.27875806161925709 ) ) ;
#25576=EDGE_CURVE ( 'NONE', #72156, #30597, #74453, .T. ) ;
#25597=CARTESIAN_POINT ( 'NONE',  ( 5.000000000000000000, 50.64189880742144823, -41.08656465431842975 ) ) ;
#25600=ORIENTED_EDGE ( 'NONE', *, *, #18276, .T. ) ;
#25621=DIRECTION ( 'NONE',  ( 0.000000000000000000, -1.000000000000000000, 0.000000000000000000 ) ) ;
#25721=LINE ( 'NONE', #60815, #74336 ) ;
#25745=CARTESIAN_POINT ( 'NONE',  ( 5.000000000000000000, -16.14408868864072844, 27.96238185062368586 ) ) ;
#25803=CARTESIAN_POINT ( 'NONE',  ( -5.000000000000000000, 50.64189880742059557, 41.08656465431948845 ) ) ;
#25823=CARTESIAN_POINT ( 'NONE',  ( -5.000000000000000888, -63.46295559274116016, 24.14151313015344158 ) ) ;
#25845=CARTESIAN_POINT ( 'NONE',  ( -2.584176286468218287, 67.83040016931262528, -20.22720298431334029 ) ) ;
#25865=CARTESIAN_POINT ( 'NONE',  ( 5.000000000000000888, 14.70421557449305716, -69.92631206022691970 ) ) ;
#25911=CARTESIAN_POINT ( 'NONE',  ( -5.000000000000000000, -53.50771145605706636, 45.03482491321309311 ) ) ;
#25937=CARTESIAN_POINT ( 'NONE',  ( -5.000000000000000000, -60.90295814858238543, -23.31388853594834032 ) ) ;
#25984=FACE_OUTER_BOUND ( 'NONE', #7946, .T. ) ;
#25991=CARTESIAN_POINT ( 'NONE',  ( 2.160335347077980472, 16.41093803200691070, 68.77481055341485217 ) ) ;
#25999=CARTESIAN_POINT ( 'NONE',  ( -0.8721677472748857740, -67.61512445009864791, -20.05250736213550056 ) ) ;
#26018=DIRECTION ( 'NONE',  ( 0.000000000000000000, 0.000000000000000000, -1.000000000000000000 ) ) ;
#26083=CARTESIAN_POINT ( 'NONE',  ( -5.000000000000000000, 11.14555136602166741, -27.84144949604398889 ) ) ;
#26099=CIRCLE ( 'NONE', #35769, 70.50000000000000000 ) ;
#26100=ADVANCED_FACE ( 'NONE', ( #27533 ), #23832, .F. ) ;
#26143=EDGE_CURVE ( 'NONE', #30587, #6891, #42034, .T. ) ;
#26152=CARTESIAN_POINT ( 'NONE',  ( -1.347111479062088207E-15, 0.000000000000000000, 0.000000000000000000 ) ) ;
#26187=CYLINDRICAL_SURFACE ( 'NONE', #13432, 5.000000000000000000 ) ;
#26258=CARTESIAN_POINT ( 'NONE',  ( -1.506524674528165075, -65.82790954191020205, -26.31843049628427877 ) ) ;
#26264=CARTESIAN_POINT ( 'NONE',  ( -4.999999999999999112, -13.21930962315088998, -69.49101004078880806 ) ) ;
#26302=EDGE_CURVE ( 'NONE', #12328, #55139, #11311, .T. ) ;
#26311=CARTESIAN_POINT ( 'NONE',  ( 5.000000000000000000, 65.74990953739953170, 23.82322416715377855 ) ) ;
#26324=ADVANCED_FACE ( 'NONE', ( #33975 ), #12414, .F. ) ;
#26334=CARTESIAN_POINT ( 'NONE',  ( 5.000000000000000000, -10.43216530810821219, -65.93415491242824089 ) ) ;
#26363=CARTESIAN_POINT ( 'NONE',  ( 7.456209740496410276, -51.58726928745755202, -41.60229883573035892 ) ) ;
#26369=FACE_OUTER_BOUND ( 'NONE', #36177, .T. ) ;
#26445=ORIENTED_EDGE ( 'NONE', *, *, #51410, .F. ) ;
#26540=CARTESIAN_POINT ( 'NONE',  ( -2.620431783921197244, -10.11675809139960869, 70.36490484706814641 ) ) ;
#26562=DIRECTION ( 'NONE',  ( 1.000000000000000000, 0.000000000000000000, 0.000000000000000000 ) ) ;
#26573=EDGE_LOOP ( 'NONE', ( #52673, #16602, #51295, #4509, #60252, #18454, #13896, #16134, #42569, #27455, #51944, #33152, #40726, #66221, #41580, #67791, #14156, #37991, #68161, #47052, #44427, #65138, #55348, #24851, #31127, #26445, #69877, #7015, #51323, #56150, #12471, #16307, #11796, #31317, #72711, #50566, #65321, #14774, #21878 ) ) ;
#26582=AXIS2_PLACEMENT_3D ( 'NONE', #24746, #48869, #59834 ) ;
#26626=CARTESIAN_POINT ( 'NONE',  ( 5.000000000000000000, 53.36732872257336169, -44.46877392682712582 ) ) ;
#26640=CARTESIAN_POINT ( 'NONE',  ( 3.734423912262952783, -66.26963445014256138, -26.58791153593539036 ) ) ;
#26714=B_SPLINE_CURVE_WITH_KNOTS ( 'NONE', 3,
 ( #7477, #30482, #35421, #53499, #355, #23336, #29382, #34683, #14595, #2552, #25911, #25543, #47818, #42533, #2178, #1816, #60632, #8954, #31218, #19151 ),
 .UNSPECIFIED., .F., .F.,
 ( 4, 2, 2, 2, 2, 2, 2, 2, 2, 4 ),
 ( 0.000000000000000000, 0.001156441540184021885, 0.001734662310276033044, 0.002312883080368043770, 0.003469324620552040501, 0.004625766160736037233, 0.005782207700920033965, 0.006938649241104030696, 0.008095090781288028295, 0.009251532321472025894 ),
 .UNSPECIFIED. ) ;
#26752=CARTESIAN_POINT ( 'NONE',  ( 6.308070865158109441, -51.03903544633450906, -41.30321721932262591 ) ) ;
#26761=EDGE_LOOP ( 'NONE', ( #22755, #46208, #24826, #60900 ) ) ;
#26937=AXIS2_PLACEMENT_3D ( 'NONE', #11357, #29081, #64151 ) ;
#26941=CARTESIAN_POINT ( 'NONE',  ( -7.456209740496309024, -10.23501300384518053, -65.47703513267214248 ) ) ;
#26954=CARTESIAN_POINT ( 'NONE',  ( -5.000000000000001776, -62.69487254116422292, 24.02505537902018773 ) ) ;
#27013=( BOUNDED_SURFACE ( )  B_SPLINE_SURFACE ( 3, 2, ( 
 ( #56576, #21479, #5633 ),
 ( #56946, #4889, #10170 ),
 ( #21109, #15437, #34318 ),
 ( #33206, #73172, #22590 ),
 ( #45610, #9801, #27885 ),
 ( #57322, #27510, #50896 ),
 ( #4150, #49786, #32824 ),
 ( #73911, #22215, #45242 ),
 ( #68254, #16549, #5262 ),
 ( #27140, #39587, #62582 ),
 ( #47462, #58437, #70485 ),
 ( #23716, #28633, #24453 ),
 ( #63330, #51647, #64085 ),
 ( #52398, #24078, #70125 ),
 ( #46720, #34690, #69746 ),
 ( #17307, #28522, #57698 ),
 ( #7116, #47087, #22978 ),
 ( #29750, #45984, #69000 ) ),
 .UNSPECIFIED., .F., .F., .F. ) 
 B_SPLINE_SURFACE_WITH_KNOTS ( ( 4, 2, 2, 2, 2, 2, 2, 2, 4 ),
 ( 3, 3 ),
 ( 0.04202945594032935633, 0.04396162471216807227, 0.04589379348400678821, 0.04782596225584550415, 0.04975813102768422008, 0.05169029979952293602, 0.05265638418544229399, 0.05362246857136165196, 0.05748680611503908383 ),
 ( 0.000000000000000000, 1.000000000000000000 ),
 .UNSPECIFIED. ) 
 GEOMETRIC_REPRESENTATION_ITEM ( )  RATIONAL_B_SPLINE_SURFACE ( (
 ( 1.000000000000000000, 0.6241276099608165095, 1.000000000000000000),
 ( 1.000000000000000000, 0.6218761496800117028, 1.000000000000000000),
 ( 1.000000000000000000, 0.6198047272364380911, 1.000000000000000000),
 ( 1.000000000000000000, 0.6161935119824036855, 1.000000000000000000),
 ( 1.000000000000000000, 0.6146642324079838460, 1.000000000000000000),
 ( 1.000000000000000000, 0.6121850116872165071, 1.000000000000000000),
 ( 1.000000000000000000, 0.6112350889399397191, 1.000000000000000000),
 ( 1.000000000000000000, 0.6099522725973182125, 1.000000000000000000),
 ( 1.000000000000000000, 0.6096208180308724245, 1.000000000000000000),
 ( 1.000000000000000000, 0.6096183796348639827, 1.000000000000000000),
 ( 1.000000000000000000, 0.6099422200103279401, 1.000000000000000000),
 ( 1.000000000000000000, 0.6109087447822609818, 1.000000000000000000),
 ( 1.000000000000000000, 0.6113123981687891284, 1.000000000000000000),
 ( 1.000000000000000000, 0.6122677719809712649, 1.000000000000000000),
 ( 1.000000000000000000, 0.6128199619021086342, 1.000000000000000000),
 ( 1.000000000000000000, 0.6159350830265309940, 1.000000000000000000),
 ( 1.000000000000000000, 0.6195556778515928231, 1.000000000000000000),
 ( 1.000000000000000000, 0.6241278272307890784, 1.000000000000000000) ) ) 
 REPRESENTATION_ITEM ( '' )  SURFACE ( )  );
#27014=EDGE_LOOP ( 'NONE', ( #28223, #12004, #17208, #20029, #49808 ) ) ;
#27126=CARTESIAN_POINT ( 'NONE',  ( -0.8997857291006282621, -51.17549659652937777, -48.53090770943286714 ) ) ;
#27140=CARTESIAN_POINT ( 'NONE',  ( -0.4451317748865747936, 16.44604352396224911, 68.55481936398530252 ) ) ;
#27152=CARTESIAN_POINT ( 'NONE',  ( 5.000000000000000000, 50.64189880742059557, 41.08656465431948845 ) ) ;
#27160=CARTESIAN_POINT ( 'NONE',  ( 7.456155213531542536, 51.58724325107107944, -41.60228463192800774 ) ) ;
#27168=VERTEX_POINT ( 'NONE', #45281 ) ;
#27239=CARTESIAN_POINT ( 'NONE',  ( 4.999999999999998224, 52.84634075987080593, 43.22150062466589304 ) ) ;
#27257=VERTEX_POINT ( 'NONE', #6415 ) ;
#27292=CARTESIAN_POINT ( 'NONE',  ( -1.781595147088172792, -16.42277972781904083, 68.70049804031401663 ) ) ;
#27294=CARTESIAN_POINT ( 'NONE',  ( -5.000000000000000888, 64.62627855237413144, 24.10294814404773334 ) ) ;
#27299=CARTESIAN_POINT ( 'NONE',  ( -5.000000000000000000, -16.24494643555759410, -69.83755725260751035 ) ) ;
#27302=DIRECTION ( 'NONE',  ( 1.000000000000000000, -0.000000000000000000, -0.000000000000000000 ) ) ;
#27310=CARTESIAN_POINT ( 'NONE',  ( 0.6547826978328875613, -10.28110016890869893, -63.57209897671329912 ) ) ;
#27324=VECTOR ( 'NONE', #38731, 1000.000000000000000 ) ;
#27367=ORIENTED_EDGE ( 'NONE', *, *, #7528, .F. ) ;
#27369=FACE_OUTER_BOUND ( 'NONE', #10013, .T. ) ;
#27370=CARTESIAN_POINT ( 'NONE',  ( 5.000000000000000000, 53.57153130924530871, -46.19535935661008352 ) ) ;
#27377=EDGE_LOOP ( 'NONE', ( #54043, #5858, #46842, #50185 ) ) ;
#27384=CARTESIAN_POINT ( 'NONE',  ( -1.296342370383604559, -60.23018777774399268, -22.90345467631826182 ) ) ;
#27403=EDGE_CURVE ( 'NONE', #41883, #17647, #61922, .T. ) ;
#27429=CARTESIAN_POINT ( 'NONE',  ( 5.000000000000000000, -53.21762015693898462, 47.70201125340187787 ) ) ;
#27455=ORIENTED_EDGE ( 'NONE', *, *, #43593, .T. ) ;
#27465=CARTESIAN_POINT ( 'NONE',  ( 5.000000000000000000, -60.90295814858255596, 23.31388853594792110 ) ) ;
#27488=VECTOR ( 'NONE', #42057, 1000.000000000000000 ) ;
#27510=CARTESIAN_POINT ( 'NONE',  ( 1.877992804784251124, 10.12031740952137859, 70.21778636471140089 ) ) ;
#27523=ORIENTED_EDGE ( 'NONE', *, *, #58852, .T. ) ;
#27528=CARTESIAN_POINT ( 'NONE',  ( -5.000000000000000000, -11.14555136602165675, -27.84144949604441166 ) ) ;
#27533=FACE_OUTER_BOUND ( 'NONE', #48961, .T. ) ;
#27614=B_SPLINE_CURVE_WITH_KNOTS ( 'NONE', 3,
 ( #25937, #9355, #9733, #55389, #14993, #32755, #48954, #14621, #21035, #55016, #13865, #32374 ),
 .UNSPECIFIED., .F., .F.,
 ( 4, 2, 2, 2, 2, 4 ),
 ( 2.602085213965210642E-18, 0.002547658444427999564, 0.005095316888855995659, 0.006369146111069992622, 0.007642975333283990452, 0.01019063377771198264 ),
 .UNSPECIFIED. ) ;
#27669=CARTESIAN_POINT ( 'NONE',  ( 4.336811714529327233, -16.30209246797837608, 69.46462972173030437 ) ) ;
#27671=CARTESIAN_POINT ( 'NONE',  ( -5.000000000000000000, 68.60357193678683529, 20.85024232999420946 ) ) ;
#27686=CARTESIAN_POINT ( 'NONE',  ( -0.4320110153365275818, 10.28109898471437766, -63.57214792341211762 ) ) ;
#27696=ORIENTED_EDGE ( 'NONE', *, *, #11971, .F. ) ;
#27757=CARTESIAN_POINT ( 'NONE',  ( -0.8997857291014387249, 51.17549659652912908, 48.53090770943328636 ) ) ;
#27759=CARTESIAN_POINT ( 'NONE',  ( 3.496982156820216403, -68.06496700477795514, -20.41687962716770599 ) ) ;
#27781=CARTESIAN_POINT ( 'NONE',  ( 2.216418498311605312, -51.36626494304428547, 48.60390812669808724 ) ) ;
#27807=EDGE_CURVE ( 'NONE', #40460, #56676, #32482, .T. ) ;
#27810=CARTESIAN_POINT ( 'NONE',  ( 5.000000000000000000, -51.30314553820225854, 41.49361401976497632 ) ) ;
#27824=DIRECTION ( 'NONE',  ( -0.000000000000000000, 0.000000000000000000, 1.000000000000000000 ) ) ;
#27845=CARTESIAN_POINT ( 'NONE',  ( -5.000000000000000000, -10.26105934116143281, 64.40045319026697257 ) ) ;
#27885=CARTESIAN_POINT ( 'NONE',  ( 4.471435261918252024, 10.26549131683129445, 64.21726486257941247 ) ) ;
#27902=CARTESIAN_POINT ( 'NONE',  ( 0.000000000000000000, 0.000000000000000000, -81.50000000000000000 ) ) ;
#27906=CARTESIAN_POINT ( 'NONE',  ( 4.231687259402287182, -68.27410168872741281, 20.58597903916479055 ) ) ;
#27912=CARTESIAN_POINT ( 'NONE',  ( -2.436599634633916711, 51.42120007173274132, -48.62500384162247968 ) ) ;
#27928=EDGE_CURVE ( 'NONE', #9105, #40460, #37266, .T. ) ;
#27992=CARTESIAN_POINT ( 'NONE',  ( -5.000000000000000888, 53.57132521838762074, -46.19376297453450775 ) ) ;
#27994=CARTESIAN_POINT ( 'NONE',  ( -0.7581620860326259148, -65.76154746681233121, 26.27794529687887604 ) ) ;
#28043=DIRECTION ( 'NONE',  ( 1.000000000000000000, -0.000000000000000000, -0.000000000000000000 ) ) ;
#28044=CARTESIAN_POINT ( 'NONE',  ( -4.104248244567244797, -66.38464254922357100, 26.65807398666778738 ) ) ;
#28063=CARTESIAN_POINT ( 'NONE',  ( -2.436599634634027289, -16.39988855009439561, -68.84456747601407756 ) ) ;
#28079=CARTESIAN_POINT ( 'NONE',  ( -5.000000000000000000, 10.38759426015435139, -65.74583990312709147 ) ) ;
#28093=VERTEX_POINT ( 'NONE', #28268 ) ;
#28139=CARTESIAN_POINT ( 'NONE',  ( 5.000000000000000888, -53.12474899268170248, -47.87640533067879289 ) ) ;
#28142=CARTESIAN_POINT ( 'NONE',  ( 1.736494649845409910, -16.42394793108440254, -68.69316892220882664 ) ) ;
#28157=CARTESIAN_POINT ( 'NONE',  ( -2.997005883571752349, -55.94527535363520343, 43.97975057405725607 ) ) ;
#28159=DIRECTION ( 'NONE',  ( 0.000000000000000000, -0.02418647091589873691, -0.9997074645238147594 ) ) ;
#28186=B_SPLINE_CURVE_WITH_KNOTS ( 'NONE', 3,
 ( #41385, #34255, #57257, #48133, #71880, #59112, #7420, #30427, #66231, #31910 ),
 .UNSPECIFIED., .F., .F.,
 ( 4, 2, 2, 2, 4 ),
 ( 0.000000000000000000, 0.001314083742615275224, 0.002628167485230550448, 0.003942251227845825455, 0.005256334970461100896 ),
 .UNSPECIFIED. ) ;
#28191=CARTESIAN_POINT ( 'NONE',  ( -5.000000000000000000, -60.90295814858257017, 23.31388853594792820 ) ) ;
#28206=DIRECTION ( 'NONE',  ( 0.000000000000000000, -3.469446951953613400E-15, 1.000000000000000000 ) ) ;
#28223=ORIENTED_EDGE ( 'NONE', *, *, #48223, .T. ) ;
#28237=VECTOR ( 'NONE', #62739, 1000.000000000000227 ) ;
#28268=CARTESIAN_POINT ( 'NONE',  ( -5.000000000000000000, 10.26105934116143281, -64.40045319026697257 ) ) ;
#28278=ORIENTED_EDGE ( 'NONE', *, *, #43593, .F. ) ;
#28290=CARTESIAN_POINT ( 'NONE',  ( -2.926785083138225622E-14, 16.44602605510714355, 68.55492853905353456 ) ) ;
#28310=CARTESIAN_POINT ( 'NONE',  ( -6.891449706540977438, 10.24244278380984774, -65.16993756079918398 ) ) ;
#28341=DIRECTION ( 'NONE',  ( 1.000000000000000000, -0.000000000000000000, -0.000000000000000000 ) ) ;
#28360=CARTESIAN_POINT ( 'NONE',  ( -5.000000000000000000, -53.17721328501337297, -43.91924822456289235 ) ) ;
#28386=EDGE_CURVE ( 'NONE', #53910, #20164, #50557, .T. ) ;
#28436=CARTESIAN_POINT ( 'NONE',  ( 4.193030820682222881, 10.26769724739507872, -64.12608639927633192 ) ) ;
#28446=B_SPLINE_CURVE_WITH_KNOTS ( 'NONE', 3,
 ( #32356, #72712, #44040, #34598, #51549, #12666, #51934, #64364, #34970, #28917, #74567, #69654, #39863, #57987, #57605, #46263, #6657, #24363, #63238, #11939 ),
 .UNSPECIFIED., .F., .F.,
 ( 4, 2, 2, 2, 2, 2, 2, 2, 2, 4 ),
 ( 0.000000000000000000, 0.001156441540183998683, 0.001734662310276000301, 0.002312883080368001703, 0.003469324620552004506, 0.004625766160736007743, 0.005782207700920009678, 0.006938649241104013349, 0.008095090781288016152, 0.009251532321472018955 ),
 .UNSPECIFIED. ) ;
#28449=CARTESIAN_POINT ( 'NONE',  ( -1.704527592502770306, -49.99193291617143586, -40.73198448289709717 ) ) ;
#28461=ORIENTED_EDGE ( 'NONE', *, *, #12788, .F. ) ;
#28496=CARTESIAN_POINT ( 'NONE',  ( 2.124081043562863869, -10.27770035960974759, -63.71262442773669221 ) ) ;
#28506=CARTESIAN_POINT ( 'NONE',  ( -3.074111742570588834, 51.58078258920524206, 48.68628732315647767 ) ) ;
#28522=CARTESIAN_POINT ( 'NONE',  ( -2.997005883563423012, 10.11494357241938147, 70.43990496500997267 ) ) ;
#28529=CARTESIAN_POINT ( 'NONE',  ( -2.216418498321459207, 67.77535163244979799, -20.18253627484908463 ) ) ;
#28540=ORIENTED_EDGE ( 'NONE', *, *, #10463, .F. ) ;
#28562=ORIENTED_EDGE ( 'NONE', *, *, #20706, .T. ) ;
#28566=CARTESIAN_POINT ( 'NONE',  ( -3.018451720292563716E-14, -16.44602605510714355, -68.55492853905353456 ) ) ;
#28588=CARTESIAN_POINT ( 'NONE',  ( -4.999999999999999112, -13.57248045702108818, 69.64920683919132216 ) ) ;
#28589=CARTESIAN_POINT ( 'NONE',  ( 4.999999999999998224, -62.69792629052213329, 24.03557775816873487 ) ) ;
#28609=DIRECTION ( 'NONE',  ( 0.000000000000000000, 0.000000000000000000, -1.000000000000000000 ) ) ;
#28633=CARTESIAN_POINT ( 'NONE',  ( -1.317228840344603968, 10.12208498181967364, 70.14472670972865842 ) ) ;
#28649=DIRECTION ( 'NONE',  ( 1.000000000000000000, -0.000000000000000000, -0.000000000000000000 ) ) ;
#28681=B_SPLINE_CURVE_WITH_KNOTS ( 'NONE', 3,
 ( #42543, #70850, #19163, #59538, #7850, #13850, #32740, #48939 ),
 .UNSPECIFIED., .F., .F.,
 ( 4, 2, 2, 4 ),
 ( 0.005256334970490776810, 0.006570121696662009278, 0.007883908422833242613, 0.01051148187517571622 ),
 .UNSPECIFIED. ) ;
#28727=CARTESIAN_POINT ( 'NONE',  ( -4.999999999999999112, -51.74377041917529851, -41.86884046506285273 ) ) ;
#28785=CARTESIAN_POINT ( 'NONE',  ( 2.589639417659363563, -10.27590863719301062, 63.78668228762852976 ) ) ;
#28787=CARTESIAN_POINT ( 'NONE',  ( -5.000000000000000888, 65.75515815785517759, 23.82162496270711216 ) ) ;
#28870=CARTESIAN_POINT ( 'NONE',  ( 4.193030820682221993, -10.26769724739507872, 64.12608639927633192 ) ) ;
#28877=CARTESIAN_POINT ( 'NONE',  ( 1.882291019709844582, 55.75505015263103559, 43.87597576789043785 ) ) ;
#28903=CARTESIAN_POINT ( 'NONE',  ( -6.298842414731080197, 61.32333038069598530, -23.57034304878899533 ) ) ;
#28917=CARTESIAN_POINT ( 'NONE',  ( 5.000000000000000888, -12.55543720214775760, 69.09376167622102116 ) ) ;
#28939=CARTESIAN_POINT ( 'NONE',  ( -5.000000000000000000, 0.000000000000000000, 0.000000000000000000 ) ) ;
#28942=CARTESIAN_POINT ( 'NONE',  ( -1.739508062077476325, -16.42388987907938613, -68.69353258878828683 ) ) ;
#28954=CIRCLE ( 'NONE', #21717, 10.99999999999999645 ) ;
#28957=EDGE_LOOP ( 'NONE', ( #70437, #11840 ) ) ;
#28964=CARTESIAN_POINT ( 'NONE',  ( 5.000000000000000000, -63.46149047932930642, 24.14127879314051839 ) ) ;
#28976=CARTESIAN_POINT ( 'NONE',  ( 2.124081043562908722, 60.31560147600158217, 22.95556260996253783 ) ) ;
#29021=CARTESIAN_POINT ( 'NONE',  ( 2.990854866095820075, 66.07503719301756462, 26.46919450145244568 ) ) ;
#29059=EDGE_LOOP ( 'NONE', ( #56389, #60586, #56570, #46822 ) ) ;
#29078=CARTESIAN_POINT ( 'NONE',  ( 5.000000000000000000, 0.000000000000000000, 0.000000000000000000 ) ) ;
#29081=DIRECTION ( 'NONE',  ( 0.000000000000000000, 0.4789076340208558435, -0.8778652960884979484 ) ) ;
#29109=CARTESIAN_POINT ( 'NONE',  ( -4.999999999999999112, -52.62657404299689290, -48.70092614269891129 ) ) ;
#29124=CARTESIAN_POINT ( 'NONE',  ( 5.000000000000000000, 60.90295814858271939, -23.31388853594749833 ) ) ;
#29167=CARTESIAN_POINT ( 'NONE',  ( 0.000000000000000000, 0.000000000000000000, 0.000000000000000000 ) ) ;
#29168=CARTESIAN_POINT ( 'NONE',  ( -0.8997857290927073759, -16.44125064681654891, 68.58473395859566324 ) ) ;
#29178=DIRECTION ( 'NONE',  ( 0.000000000000000000, 0.000000000000000000, 1.000000000000000000 ) ) ;
#29193=AXIS2_PLACEMENT_3D ( 'NONE', #22079, #45105, #56806 ) ;
#29224=VECTOR ( 'NONE', #71774, 1000.000000000000114 ) ;
#29230=AXIS2_PLACEMENT_3D ( 'NONE', #41617, #35960, #19329 ) ;
#29247=VERTEX_POINT ( 'NONE', #52282 ) ;
#29260=CARTESIAN_POINT ( 'NONE',  ( 6.308070865150001261, 51.03903544634584222, 41.30321721932931922 ) ) ;
#29267=CARTESIAN_POINT ( 'NONE',  ( 5.000000000000000000, -53.57132521838697414, -46.19376297453524671 ) ) ;
#29277=EDGE_CURVE ( 'NONE', #37240, #72436, #41750, .T. ) ;
#29285=CARTESIAN_POINT ( 'NONE',  ( -4.330454160167791500, 68.33163558029933426, -20.63184982502332687 ) ) ;
#29291=LINE ( 'NONE', #11933, #62915 ) ;
#29307=VERTEX_POINT ( 'NONE', #63213 ) ;
#29308=B_SPLINE_CURVE_WITH_KNOTS ( 'NONE', 3,
 ( #49400, #32063, #25999, #72420, #36608, #20348, #49024, #72032 ),
 .UNSPECIFIED., .F., .F.,
 ( 4, 2, 2, 4 ),
 ( 0.005256334970490779412, 0.006570121696662016217, 0.007883908422833253021, 0.01051148187517571969 ),
 .UNSPECIFIED. ) ;
#29382=CARTESIAN_POINT ( 'NONE',  ( -4.999999999999999112, -53.39837237779295265, 47.14918772354921828 ) ) ;
#29413=AXIS2_PLACEMENT_3D ( 'NONE', #72269, #14541, #38325 ) ;
#29425=ORIENTED_EDGE ( 'NONE', *, *, #54136, .F. ) ;
#29431=CARTESIAN_POINT ( 'NONE',  ( 3.228176881614038596, 10.27295505383825791, -63.90876373295822788 ) ) ;
#29488=( NAMED_UNIT ( * ) PLANE_ANGLE_UNIT ( ) SI_UNIT ( $, .RADIAN. ) );
#29497=CARTESIAN_POINT ( 'NONE',  ( 5.000000000000000000, 68.60357193678729004, -20.85024232999272087 ) ) ;
#29549=ORIENTED_EDGE ( 'NONE', *, *, #71893, .T. ) ;
#29550=B_SPLINE_CURVE_WITH_KNOTS ( 'NONE', 3,
 ( #53891, #8233, #61031, #38406, #42921, #32375, #31619, #21036, #72732, #15369, #36909, #3323, #9356, #26311, #72350, #55390, #61408, #54640, #14248, #3699, #2579, #59917 ),
 .UNSPECIFIED., .F., .F.,
 ( 4, 2, 2, 2, 2, 2, 2, 2, 2, 2, 4 ),
 ( 0.000000000000000000, 0.001156727053362440957, 0.001735090580043662954, 0.002313454106724884950, 0.003470181160087330678, 0.004048544686768553759, 0.004626908213449776840, 0.005783635266812262032, 0.006940362320174748960, 0.008097089373537234153, 0.009253816426899720213 ),
 .UNSPECIFIED. ) ;
#29566=ORIENTED_EDGE ( 'NONE', *, *, #52876, .T. ) ;
#29605=EDGE_CURVE ( 'NONE', #2210, #40213, #48174, .T. ) ;
#29616=LINE ( 'NONE', #70705, #12339 ) ;
#29617=CARTESIAN_POINT ( 'NONE',  ( 1.704527592502717459, -10.27896685065643290, -63.66027613114049188 ) ) ;
#29639=CARTESIAN_POINT ( 'NONE',  ( -3.428378827827393227, -51.66489094708095564, 48.71857030467474914 ) ) ;
#29648=CARTESIAN_POINT ( 'NONE',  ( -1.877992804783608305, 65.87054549412373206, -26.34444121135337369 ) ) ;
#29653=CARTESIAN_POINT ( 'NONE',  ( 4.999999999999999112, 0.000000000000000000, 0.000000000000000000 ) ) ;
#29684=EDGE_CURVE ( 'NONE', #42285, #3856, #68732, .T. ) ;
#29709=DIRECTION ( 'NONE',  ( 0.000000000000000000, 0.000000000000000000, -1.000000000000000000 ) ) ;
#29712=CARTESIAN_POINT ( 'NONE',  ( 5.000000000000000000, -60.90295814858255596, 23.31388853594792110 ) ) ;
#29750=CARTESIAN_POINT ( 'NONE',  ( -5.126144196591292612, 16.23426282122703057, 69.90718656545274712 ) ) ;
#29757=DIRECTION ( 'NONE',  ( 0.000000000000000000, 0.02418647091589873691, -0.9997074645238147594 ) ) ;
#29763=CARTESIAN_POINT ( 'NONE',  ( 4.465349678524218824, 66.51625814178468943, 26.73836809291932326 ) ) ;
#29798=CARTESIAN_POINT ( 'NONE',  ( -0.4501631047671846297, 16.44600848780500257, -68.55503832938671849 ) ) ;
#29821=DIRECTION ( 'NONE',  ( 0.000000000000000000, 0.8778652960885012790, 0.4789076340208496818 ) ) ;
#29846=VECTOR ( 'NONE', #37432, 1000.000000000000000 ) ;
#29903=EDGE_CURVE ( 'NONE', #46734, #37508, #30097, .T. ) ;
#29963=LINE ( 'NONE', #42747, #69062 ) ;
#29981=DIRECTION ( 'NONE',  ( 0.000000000000000000, 0.000000000000000000, -1.000000000000000000 ) ) ;
#29985=AXIS2_PLACEMENT_3D ( 'NONE', #385, #69026, #68648 ) ;
#29991=ORIENTED_EDGE ( 'NONE', *, *, #11324, .F. ) ;
#30013=ADVANCED_FACE ( 'NONE', ( #9325 ), #33111, .F. ) ;
#30014=CARTESIAN_POINT ( 'NONE',  ( 4.193030820682221105, -60.66866849074666135, 23.17095654502632840 ) ) ;
#30021=CARTESIAN_POINT ( 'NONE',  ( 6.308070865130366300, 61.28915309316995774, -23.54949267154435688 ) ) ;
#30052=ORIENTED_EDGE ( 'NONE', *, *, #45656, .T. ) ;
#30071=CARTESIAN_POINT ( 'NONE',  ( -5.000000000000000000, 14.13320814749880583, 69.81894086168458102 ) ) ;
#30096=ORIENTED_EDGE ( 'NONE', *, *, #48158, .F. ) ;
#30097=CIRCLE ( 'NONE', #9647, 8.000000000000000000 ) ;
#30098=ADVANCED_FACE ( 'NONE', ( #39850 ), #40798, .F. ) ;
#30165=CARTESIAN_POINT ( 'NONE',  ( 2.219371606097434224, 16.40787039054625041, -68.79427927095591144 ) ) ;
#30255=SHAPE_REPRESENTATION_RELATIONSHIP ( 'NONE' , 'NONE' ,  #5031, #54364 ) ;
#30268=CARTESIAN_POINT ( 'NONE',  ( 5.000000000000000888, -52.35862550122958936, 48.98731492261398301 ) ) ;
#30285=CARTESIAN_POINT ( 'NONE',  ( -1.347111479062088207E-15, 0.000000000000000000, 0.000000000000000000 ) ) ;
#30317=DIRECTION ( 'NONE',  ( 1.000000000000000000, -0.000000000000000000, -0.000000000000000000 ) ) ;
#30350=ORIENTED_EDGE ( 'NONE', *, *, #41105, .F. ) ;
#30385=CIRCLE ( 'NONE', #72556, 17.50000000000000000 ) ;
#30400=CARTESIAN_POINT ( 'NONE',  ( 4.999999999999999112, 0.000000000000000000, -17.50000000000000000 ) ) ;
#30427=CARTESIAN_POINT ( 'NONE',  ( 0.8761883848947588094, 51.17400877215430199, -48.53033992007421915 ) ) ;
#30476=CARTESIAN_POINT ( 'NONE',  ( -4.999999999999999112, 68.48952624890550567, -21.22548696402827773 ) ) ;
#30482=CARTESIAN_POINT ( 'NONE',  ( -5.000000000000000000, -52.62579568235233296, 48.70175807017984937 ) ) ;
#30536=CARTESIAN_POINT ( 'NONE',  ( 7.456209740496399618, 10.23501300384517876, -65.47703513267221354 ) ) ;
#30540=EDGE_LOOP ( 'NONE', ( #49723, #46296, #62844, #61310 ) ) ;
#30587=VERTEX_POINT ( 'NONE', #34126 ) ;
#30588=CARTESIAN_POINT ( 'NONE',  ( 5.000000000000000000, 0.000000000000000000, 0.000000000000000000 ) ) ;
#30597=VERTEX_POINT ( 'NONE', #8394 ) ;
#30653=DIRECTION ( 'NONE',  ( 0.000000000000000000, 0.000000000000000000, -1.000000000000000000 ) ) ;
#30654=CARTESIAN_POINT ( 'NONE',  ( 5.000000000000000000, 0.000000000000000000, 0.000000000000000000 ) ) ;
#30754=CARTESIAN_POINT ( 'NONE',  ( 3.228176881614462701, 60.48309044411729474, -23.05774181791798227 ) ) ;
#30813=LINE ( 'NONE', #54583, #14469 ) ;
#30835=VECTOR ( 'NONE', #32239, 1000.000000000000000 ) ;
#30845=B_SPLINE_CURVE_WITH_KNOTS ( 'NONE', 3,
 ( #46314, #40658, #45567, #52354, #63662, #62541, #16505, #51600 ),
 .UNSPECIFIED., .F., .F.,
 ( 4, 2, 2, 4 ),
 ( 0.005256334970461813000, 0.006570121696640287938, 0.007883908422818762876, 0.01051148187517571102 ),
 .UNSPECIFIED. ) ;
#30920=PLANE ( 'NONE',  #59484 ) ;
#31039=DIRECTION ( 'NONE',  ( 0.000000000000000000, -0.8536788251725986321, -0.5207998305029790664 ) ) ;
#31046=CARTESIAN_POINT ( 'NONE',  ( -1.558072418987822783, 51.25713184919987953, -48.56213741370757475 ) ) ;
#31061=VECTOR ( 'NONE', #28159, 1000.000000000000000 ) ;
#31098=CARTESIAN_POINT ( 'NONE',  ( -4.615726161709600817, -68.43878643976945853, 20.71807028113862970 ) ) ;
#31119=CARTESIAN_POINT ( 'NONE',  ( 5.107860025163145856, 60.88642786445311827, -23.30380398316370716 ) ) ;
#31127=ORIENTED_EDGE ( 'NONE', *, *, #52585, .T. ) ;
#31173=CARTESIAN_POINT ( 'NONE',  ( 5.000000000000000000, 14.13320814749867615, -69.81894086168455260 ) ) ;
#31218=CARTESIAN_POINT ( 'NONE',  ( -5.000000000000000000, -50.98458432551155539, 41.27351214092421827 ) ) ;
#31243=CARTESIAN_POINT ( 'NONE',  ( -2.124081043562906501, 50.03790111639161609, 40.75706181777542270 ) ) ;
#31252=CARTESIAN_POINT ( 'NONE',  ( -3.373128826976388162, 60.49298623944847719, -23.06377889928770486 ) ) ;
#31263=CARTESIAN_POINT ( 'NONE',  ( 5.000000000000000888, -10.54112798502250570, -66.30787999718575065 ) ) ;
#31309=DIRECTION ( 'NONE',  ( 1.000000000000000000, -0.000000000000000000, -0.000000000000000000 ) ) ;
#31317=ORIENTED_EDGE ( 'NONE', *, *, #22614, .T. ) ;
#31318=CARTESIAN_POINT ( 'NONE',  ( 4.217983994790212243, -68.29231466825473262, -20.60018752343863824 ) ) ;
#31322=CARTESIAN_POINT ( 'NONE',  ( -5.000000000000000000, 8.780967503833453037E-15, 71.70204102886728492 ) ) ;
#31328=CARTESIAN_POINT ( 'NONE',  ( 4.999999999999995559, -16.24494643555759410, -69.83755725260751035 ) ) ;
#31424=CARTESIAN_POINT ( 'NONE',  ( 3.223881452091114763, 50.20043732028305783, -40.84573126306947444 ) ) ;
#31435=ORIENTED_EDGE ( 'NONE', *, *, #56462, .T. ) ;
#31448=ORIENTED_EDGE ( 'NONE', *, *, #48477, .F. ) ;
#31500=CARTESIAN_POINT ( 'NONE',  ( 7.456209740496425376, 61.82228229130313224, -23.87473629694153132 ) ) ;
#31619=CARTESIAN_POINT ( 'NONE',  ( 5.000000000000000000, 62.88740100213628637, 24.06179116403814078 ) ) ;
#31625=ORIENTED_EDGE ( 'NONE', *, *, #38104, .F. ) ;
#31631=CARTESIAN_POINT ( 'NONE',  ( 3.369429374625368734, 60.49191766694088557, -23.06312700027788765 ) ) ;
#31632=VERTEX_POINT ( 'NONE', #49516 ) ;
#31643=CARTESIAN_POINT ( 'NONE',  ( 4.999999999999998224, -11.32881245867858944, -67.85521288293395514 ) ) ;
#31769=CARTESIAN_POINT ( 'NONE',  ( -5.000000000000002665, 0.000000000000000000, 0.000000000000000000 ) ) ;
#31822=CIRCLE ( 'NONE', #71535, 71.70204102886728492 ) ;
#31856=CARTESIAN_POINT ( 'NONE',  ( 0.000000000000000000, 0.000000000000000000, 0.000000000000000000 ) ) ;
#31857=CARTESIAN_POINT ( 'NONE',  ( -5.000000000000000000, 53.55895565990245899, 45.41404144516120311 ) ) ;
#31864=CARTESIAN_POINT ( 'NONE',  ( 2.620431783921701285, -10.11675809139960691, -70.36490484706366999 ) ) ;
#31877=CARTESIAN_POINT ( 'NONE',  ( -4.999999999999999112, -63.84827628760526608, 24.15557308422303961 ) ) ;
#31910=CARTESIAN_POINT ( 'NONE',  ( 2.957351242930898602E-11, 51.14729664189404446, -48.52014062454985321 ) ) ;
#31933=CARTESIAN_POINT ( 'NONE',  ( 5.000000000000000000, -11.14555136602165675, -27.84144949604441166 ) ) ;
#31939=CARTESIAN_POINT ( 'NONE',  ( -0.6474643998351045093, -60.19533971085457580, -22.88219507985856538 ) ) ;
#31978=CARTESIAN_POINT ( 'NONE',  ( -3.428378827827395892, 16.35907404636618878, 69.10239319626211341 ) ) ;
#32047=CARTESIAN_POINT ( 'NONE',  ( -2.591411123065558986, -50.09422832877655907, -40.78779037275307928 ) ) ;
#32063=CARTESIAN_POINT ( 'NONE',  ( -0.4368895104720016409, -67.59332269700065865, -20.03478791450352858 ) ) ;
#32213=ORIENTED_EDGE ( 'NONE', *, *, #17273, .T. ) ;
#32226=CARTESIAN_POINT ( 'NONE',  ( -3.496982156811836440, -16.35094707925444624, 69.15443034746803619 ) ) ;
#32233=EDGE_CURVE ( 'NONE', #74331, #60459, #49466, .T. ) ;
#32238=CARTESIAN_POINT ( 'NONE',  ( -5.000000000000000000, 51.74377041917500009, 41.86884046506322932 ) ) ;
#32239=DIRECTION ( 'NONE',  ( 1.000000000000000000, -0.000000000000000000, -0.000000000000000000 ) ) ;
#32269=DIRECTION ( 'NONE',  ( 0.000000000000000000, -0.8778652960884978373, -0.4789076340208558435 ) ) ;
#32303=ADVANCED_FACE ( 'NONE', ( #42832, #65851 ), #43210, .F. ) ;
#32324=CARTESIAN_POINT ( 'NONE',  ( 1.506680654954019039, -65.82403019918146470, -26.31606384388913611 ) ) ;
#32345=CARTESIAN_POINT ( 'NONE',  ( 4.330454160156406829, -52.03352386568032983, 48.86100738216652672 ) ) ;
#32349=ORIENTED_EDGE ( 'NONE', *, *, #61345, .T. ) ;
#32356=CARTESIAN_POINT ( 'NONE',  ( 5.000000000000000000, -16.24494643555759410, 69.83755725260752456 ) ) ;
#32367=CARTESIAN_POINT ( 'NONE',  ( 5.000000000000000888, -52.35862550122958936, 48.98731492261398301 ) ) ;
#32374=CARTESIAN_POINT ( 'NONE',  ( 5.000000000000000000, -60.90295814858238543, -23.31388853594834032 ) ) ;
#32375=CARTESIAN_POINT ( 'NONE',  ( 5.000000000000000888, 62.69487254116386055, 24.02505537902103683 ) ) ;
#32401=CARTESIAN_POINT ( 'NONE',  ( 3.407298021510795749, -51.68473891413731991, 48.72627478609596352 ) ) ;
#32430=CARTESIAN_POINT ( 'NONE',  ( 2.266287154879883303, -50.05783744175294459, -40.76793781259145533 ) ) ;
#32447=PLANE ( 'NONE',  #33510 ) ;
#32482=CIRCLE ( 'NONE', #5979, 71.70204102886728492 ) ;
#32515=AXIS2_PLACEMENT_3D ( 'NONE', #26152, #49170, #21249 ) ;
#32551=ORIENTED_EDGE ( 'NONE', *, *, #73767, .F. ) ;
#32594=ORIENTED_EDGE ( 'NONE', *, *, #18926, .F. ) ;
#32598=CARTESIAN_POINT ( 'NONE',  ( -4.999999999999952927, -68.60357193678709109, 20.85024232999324667 ) ) ;
#32641=CARTESIAN_POINT ( 'NONE',  ( -5.000000000000000888, -68.32828612846157057, 21.58087353894127247 ) ) ;
#32664=EDGE_LOOP ( 'NONE', ( #40320, #40590, #15079, #71074 ) ) ;
#32686=DIRECTION ( 'NONE',  ( 0.000000000000000000, 0.02418647091589873691, 0.9997074645238147594 ) ) ;
#32703=CARTESIAN_POINT ( 'NONE',  ( 0.8997857291013038328, -67.61674724335156839, -20.05382624916256518 ) ) ;
#32715=VERTEX_POINT ( 'NONE', #26083 ) ;
#32724=CARTESIAN_POINT ( 'NONE',  ( 6.298842414714818538, -51.07418104650420787, 41.32239042994850564 ) ) ;
#32727=DIRECTION ( 'NONE',  ( 0.000000000000000000, -0.4789076340208496818, 0.8778652960885012790 ) ) ;
#32740=CARTESIAN_POINT ( 'NONE',  ( -4.231687259407060253, 68.27410168872913232, 20.58597903916736627 ) ) ;
#32748=CARTESIAN_POINT ( 'NONE',  ( 13.99999999999999822, 0.000000000000000000, -8.000000000000000000 ) ) ;
#32755=CARTESIAN_POINT ( 'NONE',  ( 0.4320110153365262495, -60.19564456717412071, -22.88238106212127576 ) ) ;
#32765=CARTESIAN_POINT ( 'NONE',  ( 0.8419854211626177642, 60.19512794652395371, -22.88206588978716383 ) ) ;
#32824=CARTESIAN_POINT ( 'NONE',  ( 2.591411123065536781, 10.27614846265000637, 63.77676950207272455 ) ) ;
#32849=CARTESIAN_POINT ( 'NONE',  ( -2.266287154886474919, 50.05783744175423777, -40.76793781259114979 ) ) ;
#32905=CARTESIAN_POINT ( 'NONE',  ( 5.000000000000000000, -60.11723469343116477, 46.25570701698070764 ) ) ;
#32932=CARTESIAN_POINT ( 'NONE',  ( 1.558072418983288632, -67.68461058694124688, 20.10890959968006797 ) ) ;
#32934=CARTESIAN_POINT ( 'NONE',  ( 5.000000000000000000, 53.50771145605643397, 45.03482491321383918 ) ) ;
#32988=CARTESIAN_POINT ( 'NONE',  ( -2.591411123055096688, -10.27614846265026038, 63.77676950206216588 ) ) ;
#32998=FACE_OUTER_BOUND ( 'NONE', #40165, .T. ) ;
#32999=CARTESIAN_POINT ( 'NONE',  ( -5.000000000000000000, 53.21762015693831671, 47.70201125340263104 ) ) ;
#33007=CARTESIAN_POINT ( 'NONE',  ( -3.511653767258354986, -16.35475815726549342, -69.12977678000822834 ) ) ;
#33026=CARTESIAN_POINT ( 'NONE',  ( -4.999999999999999112, 14.70234347858786528, -69.93881661156081009 ) ) ;
#33072=CARTESIAN_POINT ( 'NONE',  ( 4.999999999999999112, 52.84347807771189309, -43.21644271080158717 ) ) ;
#33085=DIRECTION ( 'NONE',  ( 0.000000000000000000, 0.000000000000000000, -1.000000000000000000 ) ) ;
#33111=( BOUNDED_SURFACE ( )  B_SPLINE_SURFACE ( 3, 2, ( 
 ( #21002, #21744, #16448 ),
 ( #56472, #62480, #15336 ),
 ( #32345, #4788, #32724 ),
 ( #49300, #33844, #44028 ),
 ( #67037, #56842, #15710 ),
 ( #27781, #61752, #55358 ),
 ( #55732, #44772, #4049 ),
 ( #50052, #73068, #44398 ),
 ( #73807, #67786, #16078 ),
 ( #22115, #45139, #74554 ),
 ( #11926, #51168, #34212 ),
 ( #22866, #58341, #52663 ),
 ( #57973, #23980, #45880 ),
 ( #6645, #63981, #70021 ),
 ( #68894, #74177, #17956 ),
 ( #259, #28157, #18327 ),
 ( #631, #57214, #41342 ),
 ( #5528, #40974, #69269 ) ),
 .UNSPECIFIED., .F., .F., .F. ) 
 B_SPLINE_SURFACE_WITH_KNOTS ( ( 4, 2, 2, 2, 2, 2, 2, 2, 4 ),
 ( 3, 3 ),
 ( 0.04202945594034800114, 0.04396162471218434398, 0.04589379348402068681, 0.04782596225585702965, 0.04975813102769337248, 0.05169029979952971532, 0.05265638418544788674, 0.05362246857136605815, 0.05748680611503874383 ),
 ( 0.000000000000000000, 1.000000000000000000 ),
 .UNSPECIFIED. ) 
 GEOMETRIC_REPRESENTATION_ITEM ( )  RATIONAL_B_SPLINE_SURFACE ( (
 ( 1.000000000000000000, 0.6241276099607500072, 1.000000000000000000),
 ( 1.000000000000000000, 0.6218761496802208688, 1.000000000000000000),
 ( 1.000000000000000000, 0.6198047272360279747, 1.000000000000000000),
 ( 1.000000000000000000, 0.6161935119827212093, 1.000000000000000000),
 ( 1.000000000000000000, 0.6146642324083134712, 1.000000000000000000),
 ( 1.000000000000000000, 0.6121850116868342573, 1.000000000000000000),
 ( 1.000000000000000000, 0.6112350889398914244, 1.000000000000000000),
 ( 1.000000000000000000, 0.6099522725973434145, 1.000000000000000000),
 ( 1.000000000000000000, 0.6096208180309086178, 1.000000000000000000),
 ( 1.000000000000000000, 0.6096183796348277895, 1.000000000000000000),
 ( 1.000000000000000000, 0.6099422200098292279, 1.000000000000000000),
 ( 1.000000000000000000, 0.6109087447825207740, 1.000000000000000000),
 ( 1.000000000000000000, 0.6113123981689779773, 1.000000000000000000),
 ( 1.000000000000000000, 0.6122677719807979591, 1.000000000000000000),
 ( 1.000000000000000000, 0.6128199619019198963, 1.000000000000000000),
 ( 1.000000000000000000, 0.6159350830273242483, 1.000000000000000000),
 ( 1.000000000000000000, 0.6195556778510084017, 1.000000000000000000),
 ( 1.000000000000000000, 0.6241278272307887454, 1.000000000000000000) ) ) 
 REPRESENTATION_ITEM ( '' )  SURFACE ( )  );
#33113=CARTESIAN_POINT ( 'NONE',  ( -5.000000000000000000, 0.000000000000000000, 0.000000000000000000 ) ) ;
#33131=CARTESIAN_POINT ( 'NONE',  ( 5.000000000000000888, -52.63864145287922014, 42.88977517748058688 ) ) ;
#33141=CARTESIAN_POINT ( 'NONE',  ( 13.99999999999999822, 0.000000000000000000, -17.50000000000000000 ) ) ;
#33152=ORIENTED_EDGE ( 'NONE', *, *, #9142, .T. ) ;
#33192=CARTESIAN_POINT ( 'NONE',  ( -4.471435261918684567, -50.48103707412959551, -40.99880869399324723 ) ) ;
#33201=CARTESIAN_POINT ( 'NONE',  ( -5.000000000000000000, -10.00000000000000000, -75.19090595827292134 ) ) ;
#33206=CARTESIAN_POINT ( 'NONE',  ( 3.496982156820435783, 16.35094707925456348, 69.15443034747086415 ) ) ;
#33225=CARTESIAN_POINT ( 'NONE',  ( 4.471435261904963987, 50.48103707412082031, -40.99880869398744210 ) ) ;
#33248=PLANE ( 'NONE',  #44228 ) ;
#33282=ORIENTED_EDGE ( 'NONE', *, *, #15774, .T. ) ;
#33288=EDGE_CURVE ( 'NONE', #22076, #21755, #8033, .T. ) ;
#33304=CARTESIAN_POINT ( 'NONE',  ( 5.000000000000000888, 53.57132521838664729, 46.19376297453561619 ) ) ;
#33353=CARTESIAN_POINT ( 'NONE',  ( 2.069125466541355873, -10.11940336925128214, 70.25556669588236502 ) ) ;
#33355=CARTESIAN_POINT ( 'NONE',  ( -5.000000000000000000, 60.90295814858222201, 23.31388853594875599 ) ) ;
#33372=CARTESIAN_POINT ( 'NONE',  ( -3.544144923088220711, -10.27124247550359826, -63.97955030412420996 ) ) ;
#33389=ORIENTED_EDGE ( 'NONE', *, *, #62565, .F. ) ;
#33434=CARTESIAN_POINT ( 'NONE',  ( 5.000000000000000000, 50.64189880742144823, -41.08656465431842975 ) ) ;
#33447=CARTESIAN_POINT ( 'NONE',  ( -6.891449706549017229, 51.31760009878102835, 41.45518442798194059 ) ) ;
#33449=CARTESIAN_POINT ( 'NONE',  ( 13.99999999999999822, 0.000000000000000000, 0.000000000000000000 ) ) ;
#33472=DIRECTION ( 'NONE',  ( -1.000000000000000000, 0.000000000000000000, -0.000000000000000000 ) ) ;
#33510=AXIS2_PLACEMENT_3D ( 'NONE', #66763, #60348, #54710 ) ;
#33559=CARTESIAN_POINT ( 'NONE',  ( -0.4501631047669842345, -51.14740050675992222, -48.52018030598949139 ) ) ;
#33596=CARTESIAN_POINT ( 'NONE',  ( -3.511653767258854586, 51.69076377080494922, -48.72852442694383512 ) ) ;
#33658=CARTESIAN_POINT ( 'NONE',  ( -1.688721909672441956, 10.27943647337372468, 63.64086505882563216 ) ) ;
#33671=CARTESIAN_POINT ( 'NONE',  ( -5.000000000000000000, -53.55895565990277163, -45.41404144516085495 ) ) ;
#33673=CARTESIAN_POINT ( 'NONE',  ( 4.336811714534362316, -68.30918023750064094, 20.61428864871788846 ) ) ;
#33726=ORIENTED_EDGE ( 'NONE', *, *, #33981, .F. ) ;
#33728=CARTESIAN_POINT ( 'NONE',  ( -7.456155213548125715, -61.82225697226411398, 23.87472085067487271 ) ) ;
#33730=CARTESIAN_POINT ( 'NONE',  ( -5.000000000000000000, 68.33088307291085073, 21.57589723056566910 ) ) ;
#33745=CARTESIAN_POINT ( 'NONE',  ( -1.558072418987778152, -16.42747873774261080, -68.67104701338908512 ) ) ;
#33758=CARTESIAN_POINT ( 'NONE',  ( -0.8588954341815023819, -49.93020820668186133, -40.69831139579137869 ) ) ;
#33800=ORIENTED_EDGE ( 'NONE', *, *, #34510, .T. ) ;
#33809=PLANE ( 'NONE',  #29193 ) ;
#33816=DIRECTION ( 'NONE',  ( -0.000000000000000000, 0.5207998305029671871, 0.8536788251726059595 ) ) ;
#33821=CARTESIAN_POINT ( 'NONE',  ( 0.3752463838824043885, 55.62178951997592691, 43.80327721769204885 ) ) ;
#33828=CARTESIAN_POINT ( 'NONE',  ( 5.000000000000000888, -51.89737250574506078, -42.00009673807131350 ) ) ;
#33844=CARTESIAN_POINT ( 'NONE',  ( 2.990854866091075870, -55.96051345247121134, 43.98806351442848950 ) ) ;
#33856=EDGE_CURVE ( 'NONE', #72830, #42285, #70056, .T. ) ;
#33857=CARTESIAN_POINT ( 'NONE',  ( -5.000000000000000000, 0.000000000000000000, 0.000000000000000000 ) ) ;
#33892=DIRECTION ( 'NONE',  ( 1.000000000000000000, 0.000000000000000000, 0.000000000000000000 ) ) ;
#33893=EDGE_CURVE ( 'NONE', #44073, #74219, #29550, .T. ) ;
#33975=FACE_OUTER_BOUND ( 'NONE', #22797, .T. ) ;
#33981=EDGE_CURVE ( 'NONE', #25179, #53910, #57498, .T. ) ;
#34053=CARTESIAN_POINT ( 'NONE',  ( -0.3794862803196089041, -65.74576272852164038, 26.26831557574494624 ) ) ;
#34067=VERTEX_POINT ( 'NONE', #33141 ) ;
#34073=CARTESIAN_POINT ( 'NONE',  ( -5.000000000000000000, -63.46149047932912879, -24.14127879314093761 ) ) ;
#34102=CARTESIAN_POINT ( 'NONE',  ( -2.990854866096253950, -66.07503719301790568, 26.46919450145037445 ) ) ;
#34119=CARTESIAN_POINT ( 'NONE',  ( -0.7509181236822947136, -10.12341933770111879, -70.08957333326543448 ) ) ;
#34126=CARTESIAN_POINT ( 'NONE',  ( 5.000000000000000000, -11.14555136602166208, 27.84144949604419494 ) ) ;
#34187=CARTESIAN_POINT ( 'NONE',  ( -1.308779242312746893, 49.95118570763212773, 40.70975538998155940 ) ) ;
#34197=CARTESIAN_POINT ( 'NONE',  ( 0.4369882809721241101, -16.44602605510714710, -68.55492853905353456 ) ) ;
#34207=CARTESIAN_POINT ( 'NONE',  ( 5.000000000000000000, -66.79212039439826754, -23.29662735513450400 ) ) ;
#34212=CARTESIAN_POINT ( 'NONE',  ( -1.296342370391162069, -49.95006747299220251, 40.70914535207602825 ) ) ;
#34232=EDGE_CURVE ( 'NONE', #3989, #72569, #67315, .T. ) ;
#34255=CARTESIAN_POINT ( 'NONE',  ( 4.615726161709589270, 52.16176840074273002, -48.91069252044838578 ) ) ;
#34270=CARTESIAN_POINT ( 'NONE',  ( -2.967813307894019431E-11, 16.44602605510714355, -68.55492853905352035 ) ) ;
#34274=DIRECTION ( 'NONE',  ( 0.000000000000000000, 0.8778652960885012790, 0.4789076340208496818 ) ) ;
#34279=PRODUCT_CONTEXT ( 'NONE', #73674, 'mechanical' ) ;
#34293=EDGE_CURVE ( 'NONE', #56998, #45708, #73344, .T. ) ;
#34318=CARTESIAN_POINT ( 'NONE',  ( 6.298842414732200190, 10.24914933418224194, 64.89273347874026854 ) ) ;
#34367=CYLINDRICAL_SURFACE ( 'NONE', #10503, 17.50000000000000000 ) ;
#34407=CARTESIAN_POINT ( 'NONE',  ( -5.000000000000000000, 10.26105934116142215, 64.40045319026754100 ) ) ;
#34433=CIRCLE ( 'NONE', #48877, 5.000000000000000888 ) ;
#34435=CARTESIAN_POINT ( 'NONE',  ( 5.000000000000000000, 67.10993666412761627, -23.06595724273550374 ) ) ;
#34459=DIRECTION ( 'NONE',  ( 1.000000000000000000, 0.000000000000000000, 0.000000000000000000 ) ) ;
#34476=CARTESIAN_POINT ( 'NONE',  ( -5.126106709314337095, -68.65851429197823563, 20.89429596904591691 ) ) ;
#34481=DIRECTION ( 'NONE',  ( 1.000000000000000000, -0.000000000000000000, 0.000000000000000000 ) ) ;
#34498=CARTESIAN_POINT ( 'NONE',  ( 0.3794862803135433671, -10.12385276104027199, -70.07165850195889334 ) ) ;
#34510=EDGE_CURVE ( 'NONE', #72569, #9105, #52823, .T. ) ;
#34560=CARTESIAN_POINT ( 'NONE',  ( 5.000000000000000000, -10.26105934116143459, 64.40045319026695836 ) ) ;
#34565=CARTESIAN_POINT ( 'NONE',  ( -0.3794862803192503020, 55.62190996747682448, 43.80334292620992187 ) ) ;
#34579=CARTESIAN_POINT ( 'NONE',  ( -1.704527592502768307, -60.27089976682808015, 22.92829164824352262 ) ) ;
#34580=PRODUCT_DEFINITION_FORMATION_WITH_SPECIFIED_SOURCE ( 'ANY', '', #61975, .NOT_KNOWN. ) ;
#34587=CARTESIAN_POINT ( 'NONE',  ( -0.4501631047670816010, 67.59340899456853435, -20.03485802339563193 ) ) ;
#34594=DIRECTION ( 'NONE',  ( 1.000000000000000000, -0.000000000000000000, -0.000000000000000000 ) ) ;
#34598=CARTESIAN_POINT ( 'NONE',  ( 5.000000000000000000, -14.89980876190738179, 69.94558486267358433 ) ) ;
#34626=CARTESIAN_POINT ( 'NONE',  ( -3.407298021510761998, -51.68473891413697174, -48.72627478609629037 ) ) ;
#34647=CARTESIAN_POINT ( 'NONE',  ( -4.999999999999992006, -10.25159769123454900, 64.79153472057838314 ) ) ;
#34649=CARTESIAN_POINT ( 'NONE',  ( 4.999999999999999112, -63.85408791058082301, 24.15552328276479699 ) ) ;
#34663=CARTESIAN_POINT ( 'NONE',  ( 3.373128826976390826, 60.49298623944800823, 23.06377889928895186 ) ) ;
#34668=VERTEX_POINT ( 'NONE', #15041 ) ;
#34683=CARTESIAN_POINT ( 'NONE',  ( -5.000000000000001776, -53.53067326687894933, 46.58593137613084423 ) ) ;
#34690=CARTESIAN_POINT ( 'NONE',  ( -2.069125466538952907, 10.11940336925101924, 70.25556669587955128 ) ) ;
#34698=DIRECTION ( 'NONE',  ( 1.000000000000000000, 0.000000000000000000, 0.000000000000000000 ) ) ;
#34719=DIRECTION ( 'NONE',  ( 0.000000000000000000, 0.000000000000000000, -1.000000000000000000 ) ) ;
#34737=AXIS2_PLACEMENT_3D ( 'NONE', #41731, #65474, #13768 ) ;
#34742=FACE_OUTER_BOUND ( 'NONE', #5682, .T. ) ;
#34792=CARTESIAN_POINT ( 'NONE',  ( -5.000000000000000000, -53.35645474066778604, -47.33026262608771617 ) ) ;
#34816=DIRECTION ( 'NONE',  ( -1.000000000000000000, 0.000000000000000000, 0.000000000000000000 ) ) ;
#34846=VECTOR ( 'NONE', #68678, 1000.000000000000000 ) ;
#34848=CARTESIAN_POINT ( 'NONE',  ( -1.877992804784410330, -65.87054549411909932, 26.34444121134937333 ) ) ;
#34850=DIRECTION ( 'NONE',  ( 0.000000000000000000, -0.8778652960885044987, 0.4789076340208435756 ) ) ;
#34862=AXIS2_PLACEMENT_3D ( 'NONE', #25745, #16573, #39610 ) ;
#34880=CARTESIAN_POINT ( 'NONE',  ( -3.373128826976394823, -50.22031155377506195, -40.85657338450078413 ) ) ;
#34900=ORIENTED_EDGE ( 'NONE', *, *, #29277, .F. ) ;
#34933=DIRECTION ( 'NONE',  ( 0.000000000000000000, -0.8536788251726059595, 0.5207998305029671871 ) ) ;
#34937=CARTESIAN_POINT ( 'NONE',  ( 7.456209740496436034, 51.58726928745726070, 41.60229883573070708 ) ) ;
#34947=CARTESIAN_POINT ( 'NONE',  ( 2.160335347077970702, -16.41093803200690715, -68.77481055341485217 ) ) ;
#34952=CARTESIAN_POINT ( 'NONE',  ( -2.124081043562907833, -60.31560147600191613, 22.95556260996172782 ) ) ;
#34970=CARTESIAN_POINT ( 'NONE',  ( 5.000000000000000000, -13.21930962315071767, 69.49101004078875121 ) ) ;
#34997=PLANE ( 'NONE',  #39090 ) ;
#35006=B_SPLINE_CURVE_WITH_KNOTS ( 'NONE', 3,
 ( #73640, #60447, #8777, #17782, #62681, #92, #56675, #4992, #27992, #57047, #51743, #461, #62316, #50999, #40057, #5358, #46079, #10642, #40795, #40428 ),
 .UNSPECIFIED., .F., .F.,
 ( 4, 2, 2, 2, 2, 2, 2, 2, 2, 4 ),
 ( 0.000000000000000000, 0.001156441540183978300, 0.001734662310275972546, 0.002312883080367967008, 0.003469324620551975016, 0.004625766160735983457, 0.005782207700919991464, 0.006938649241103999471, 0.008095090781288007478, 0.009251532321472015485 ),
 .UNSPECIFIED. ) ;
#35020=CARTESIAN_POINT ( 'NONE',  ( -4.999999999999999112, -12.24343743989404310, 68.85270403949348861 ) ) ;
#35021=CARTESIAN_POINT ( 'NONE',  ( 4.999999999999692690, -68.48985753891565764, 21.22439692019619883 ) ) ;
#35037=DIRECTION ( 'NONE',  ( 1.000000000000000000, -0.000000000000000000, -0.000000000000000000 ) ) ;
#35047=CARTESIAN_POINT ( 'NONE',  ( -5.000000000000000888, 63.84827628760543661, -24.15557308422260263 ) ) ;
#35074=CARTESIAN_POINT ( 'NONE',  ( 2.216418498320175345, 67.77535163244897376, 20.18253627485079349 ) ) ;
#35077=CARTESIAN_POINT ( 'NONE',  ( 1.739508062057428139, -67.70228923712181768, 20.12326043015085730 ) ) ;
#35106=CARTESIAN_POINT ( 'NONE',  ( 1.780377099648907224, 16.42166210098345758, -68.70754022607248146 ) ) ;
#35171=CARTESIAN_POINT ( 'NONE',  ( 5.000000000000000000, 10.28295106684163684, 65.17663434001590872 ) ) ;
#35205=AXIS2_PLACEMENT_3D ( 'NONE', #19427, #1372, #36428 ) ;
#35303=DIRECTION ( 'NONE',  ( -0.000000000000000000, -0.000000000000000000, 1.000000000000000000 ) ) ;
#35304=CARTESIAN_POINT ( 'NONE',  ( -5.126144196591281954, -68.65853088339370913, -20.89430926783084885 ) ) ;
#35317=CARTESIAN_POINT ( 'NONE',  ( -0.4368895104720019740, -51.14729664189371761, 48.52014062455020138 ) ) ;
#35321=CARTESIAN_POINT ( 'NONE',  ( 0.8419854211626226492, -60.19512794652378318, 22.88206588978759015 ) ) ;
#35324=CARTESIAN_POINT ( 'NONE',  ( 4.999999999999999112, -64.42874436516109427, -24.11656705754197816 ) ) ;
#35329=CARTESIAN_POINT ( 'NONE',  ( -3.074111742569602956, 67.95395293240338219, -20.32712440775815210 ) ) ;
#35334=DIRECTION ( 'NONE',  ( 1.000000000000000000, -0.000000000000000000, -0.000000000000000000 ) ) ;
#35362=DIRECTION ( 'NONE',  ( 0.000000000000000000, 0.000000000000000000, -1.000000000000000000 ) ) ;
#35421=CARTESIAN_POINT ( 'NONE',  ( -4.999999999999999112, -52.85071664756715393, 48.38833198888253406 ) ) ;
#35468=CARTESIAN_POINT ( 'NONE',  ( -2.620431783929222824, 10.11675809140012561, -70.36490484707876192 ) ) ;
#35502=VERTEX_POINT ( 'NONE', #16440 ) ;
#35532=CARTESIAN_POINT ( 'NONE',  ( 4.999999999999999112, 13.57248045702108818, 69.64920683919132216 ) ) ;
#35587=ORIENTED_EDGE ( 'NONE', *, *, #57922, .T. ) ;
#35639=EDGE_CURVE ( 'NONE', #4298, #3455, #39862, .T. ) ;
#35675=CARTESIAN_POINT ( 'NONE',  ( -3.107148544787702027E-14, -51.14729664189371761, 48.52014062455021559 ) ) ;
#35686=CARTESIAN_POINT ( 'NONE',  ( -4.465349678524273003, 66.51625814178524365, -26.73836809291795191 ) ) ;
#35737=CARTESIAN_POINT ( 'NONE',  ( -5.000000000000000888, 14.70421557449314953, 69.92631206022693391 ) ) ;
#35756=ORIENTED_EDGE ( 'NONE', *, *, #38494, .F. ) ;
#35769=AXIS2_PLACEMENT_3D ( 'NONE', #11682, #10571, #34719 ) ;
#35801=ORIENTED_EDGE ( 'NONE', *, *, #27807, .T. ) ;
#35802=CARTESIAN_POINT ( 'NONE',  ( 0.8997857291008781733, 67.61674724335057363, 20.05382624916572709 ) ) ;
#35832=CARTESIAN_POINT ( 'NONE',  ( 0.3752463838827005405, 10.12385607954436573, -70.07152133708838448 ) ) ;
#35840=LINE ( 'NONE', #45663, #34846 ) ;
#35899=EDGE_CURVE ( 'NONE', #74219, #45651, #41749, .T. ) ;
#35901=CARTESIAN_POINT ( 'NONE',  ( 5.000000000000000000, 66.11467145570921389, -23.67355326542971383 ) ) ;
#35921=CARTESIAN_POINT ( 'NONE',  ( -5.000000000000000000, 18.53862685874501537, 23.57305537018163477 ) ) ;
#35933=DIRECTION ( 'NONE',  ( 0.000000000000000000, 0.8536788251726059595, -0.5207998305029671871 ) ) ;
#35960=DIRECTION ( 'NONE',  ( 1.000000000000000000, 0.000000000000000000, 0.000000000000000000 ) ) ;
#36056=CARTESIAN_POINT ( 'NONE',  ( 2.436599634630261413, 67.82108862182671771, -20.21956363439073101 ) ) ;
#36115=DIRECTION ( 'NONE',  ( 1.000000000000000000, -0.000000000000000000, -0.000000000000000000 ) ) ;
#36167=ORIENTED_EDGE ( 'NONE', *, *, #70525, .F. ) ;
#36168=CARTESIAN_POINT ( 'NONE',  ( -0.3752463838826867737, 65.74564559951204501, 26.26824411940225446 ) ) ;
#36177=EDGE_LOOP ( 'NONE', ( #70579, #45660, #12675, #43307 ) ) ;
#36201=CARTESIAN_POINT ( 'NONE',  ( -1.506680654954751120, 10.12163528317106120, -70.16331425390788468 ) ) ;
#36224=CARTESIAN_POINT ( 'NONE',  ( -3.734423912265953938, -56.16062404875297887, -44.09723116535785437 ) ) ;
#36234=CARTESIAN_POINT ( 'NONE',  ( -5.000000000000002665, 2.143131898507868248E-15, 17.50000000000000000 ) ) ;
#36257=DIRECTION ( 'NONE',  ( 0.000000000000000000, 0.000000000000000000, -1.000000000000000000 ) ) ;
#36292=VECTOR ( 'NONE', #6672, 1000.000000000000000 ) ;
#36298=CIRCLE ( 'NONE', #15761, 71.70204102886728492 ) ;
#36358=ORIENTED_EDGE ( 'NONE', *, *, #38112, .T. ) ;
#36370=ORIENTED_EDGE ( 'NONE', *, *, #41210, .T. ) ;
#36405=CARTESIAN_POINT ( 'NONE',  ( -4.217983994794788138, -68.29231466825659425, 20.60018752343953707 ) ) ;
#36428=DIRECTION ( 'NONE',  ( 0.000000000000000000, 0.000000000000000000, 1.000000000000000000 ) ) ;
#36447=CARTESIAN_POINT ( 'NONE',  ( -5.000000000000002665, 0.000000000000000000, 0.000000000000000000 ) ) ;
#36462=CARTESIAN_POINT ( 'NONE',  ( 13.99999999999999822, 0.000000000000000000, 0.000000000000000000 ) ) ;
#36473=CARTESIAN_POINT ( 'NONE',  ( -5.000000000000000000, 10.42446448370097656, 65.94449134867544160 ) ) ;
#36478=AXIS2_PLACEMENT_3D ( 'NONE', #36447, #37183, #24378 ) ;
#36505=B_SPLINE_CURVE_WITH_KNOTS ( 'NONE', 3,
 ( #10725, #39399, #51454, #68807, #22035, #50709, #33758, #28449, #11843, #34880, #17498, #16362 ),
 .UNSPECIFIED., .F., .F.,
 ( 4, 2, 2, 2, 2, 4 ),
 ( 3.469446951953614189E-18, 0.002547658444427999130, 0.005095316888855994791, 0.006369146111069992622, 0.007642975333283991320, 0.01019063377771198438 ),
 .UNSPECIFIED. ) ;
#36539=CARTESIAN_POINT ( 'NONE',  ( -2.069125466537580227, 65.90280720053385721, 26.36412295902896830 ) ) ;
#36568=CARTESIAN_POINT ( 'NONE',  ( 0.8588954341814997173, 49.93020820668242266, -40.69831139579068235 ) ) ;
#36608=CARTESIAN_POINT ( 'NONE',  ( -2.170320029210516921, -67.76782500014672905, -20.17643218080532108 ) ) ;
#36626=CARTESIAN_POINT ( 'NONE',  ( -1.736494649864694706, 16.42394793108385898, -68.69316892221223725 ) ) ;
#36657=( LENGTH_UNIT ( ) NAMED_UNIT ( * ) SI_UNIT ( .MILLI., .METRE. ) );
#36784=CARTESIAN_POINT ( 'NONE',  ( 6.891449706524926277, -10.24244278381002005, -65.16993756079213540 ) ) ;
#36844=CARTESIAN_POINT ( 'NONE',  ( 5.000000000000000000, 10.42446448370085577, -65.94449134867498685 ) ) ;
#36847=B_SPLINE_CURVE_WITH_KNOTS ( 'NONE', 3,
 ( #1548, #24528, #18508, #70559, #58153, #6819, #46801, #1176 ),
 .UNSPECIFIED., .F., .F.,
 ( 4, 2, 2, 4 ),
 ( 0.005256334970490775943, 0.006570121696662012747, 0.007883908422833249552, 0.01051148187517572316 ),
 .UNSPECIFIED. ) ;
#36907=CARTESIAN_POINT ( 'NONE',  ( -2.589639417653282649, 60.37884160280883350, 22.99414321703751440 ) ) ;
#36909=CARTESIAN_POINT ( 'NONE',  ( 5.000000000000001776, 64.62379132009235150, 24.09319349500452034 ) ) ;
#36921=EDGE_CURVE ( 'NONE', #74219, #14457, #60412, .T. ) ;
#36928=ORIENTED_EDGE ( 'NONE', *, *, #52915, .T. ) ;
#36985=VERTEX_POINT ( 'NONE', #99 ) ;
#36986=CARTESIAN_POINT ( 'NONE',  ( 4.615726161707419450, -68.43878643976833587, -20.71807028113835614 ) ) ;
#36992=CARTESIAN_POINT ( 'NONE',  ( -5.000000000000000000, -16.14408868864072844, 22.96238185062368586 ) ) ;
#36999=ORIENTED_EDGE ( 'NONE', *, *, #50098, .T. ) ;
#37024=( NAMED_UNIT ( * ) PLANE_ANGLE_UNIT ( ) SI_UNIT ( $, .RADIAN. ) );
#37088=CARTESIAN_POINT ( 'NONE',  ( 3.496982156811288434, 51.71401992552112148, -48.73755072030355251 ) ) ;
#37159=CARTESIAN_POINT ( 'NONE',  ( 4.465384415997327494, 66.51627080308891493, -26.73837581714001033 ) ) ;
#37183=DIRECTION ( 'NONE',  ( 1.000000000000000000, -0.000000000000000000, -0.000000000000000000 ) ) ;
#37190=CARTESIAN_POINT ( 'NONE',  ( -4.999999999999944045, 68.60357193678724741, -20.85024232999276350 ) ) ;
#37206=ORIENTED_EDGE ( 'NONE', *, *, #11971, .T. ) ;
#37212=CARTESIAN_POINT ( 'NONE',  ( 4.999999999999999112, 10.82378452496227261, -67.02990231369372509 ) ) ;
#37232=DIRECTION ( 'NONE',  ( 0.000000000000000000, -0.000000000000000000, 1.000000000000000000 ) ) ;
#37240=VERTEX_POINT ( 'NONE', #31328 ) ;
#37266=CIRCLE ( 'NONE', #22817, 10.99999999999999645 ) ;
#37283=CARTESIAN_POINT ( 'NONE',  ( -3.728321214213454748, 66.24762070553359194, 26.57448171416459459 ) ) ;
#37304=DIRECTION ( 'NONE',  ( 0.000000000000000000, -0.8536788251726096233, 0.5207998305029611918 ) ) ;
#37334=CARTESIAN_POINT ( 'NONE',  ( -14.00000000000000178, -2.250000000005106138, 7.677076266390546522 ) ) ;
#37340=CARTESIAN_POINT ( 'NONE',  ( 4.615726161707415898, 16.27701803902727917, 69.62876280158647546 ) ) ;
#37349=FACE_OUTER_BOUND ( 'NONE', #3586, .T. ) ;
#37432=DIRECTION ( 'NONE',  ( 0.000000000000000000, 0.02418647091589873691, -0.9997074645238147594 ) ) ;
#37467=ORIENTED_EDGE ( 'NONE', *, *, #29903, .F. ) ;
#37472=B_SPLINE_CURVE_WITH_KNOTS ( 'NONE', 3,
 ( #68212, #16508, #38060, #32401, #9383, #4106, #22177, #55042, #62174, #4851 ),
 .UNSPECIFIED., .F., .F.,
 ( 4, 2, 2, 2, 4 ),
 ( 0.000000000000000000, 0.001314083742622695287, 0.002628167485245389273, 0.003942251227868082825, 0.005256334970490777678 ),
 .UNSPECIFIED. ) ;
#37508=VERTEX_POINT ( 'NONE', #41093 ) ;
#37522=CARTESIAN_POINT ( 'NONE',  ( -5.000000000000000000, 52.15374455614115590, 42.28282461816605320 ) ) ;
#37527=ADVANCED_FACE ( 'NONE', ( #69392 ), #64102, .F. ) ;
#37541=CARTESIAN_POINT ( 'NONE',  ( -4.999999999999999112, -64.62379132009267835, 24.09319349500363217 ) ) ;
#37586=CARTESIAN_POINT ( 'NONE',  ( 5.000000000000000000, 10.53354221205055907, -66.31578581128081851 ) ) ;
#37604=LINE ( 'NONE', #44377, #27324 ) ;
#37611=PRODUCT_DEFINITION ( 'UNKNOWN', '', #34580, #5579 ) ;
#37636=DIRECTION ( 'NONE',  ( 1.000000000000000000, -0.000000000000000000, 0.000000000000000000 ) ) ;
#37673=EDGE_CURVE ( 'NONE', #48525, #16897, #47848, .T. ) ;
#37683=ORIENTED_EDGE ( 'NONE', *, *, #56789, .F. ) ;
#37720=CARTESIAN_POINT ( 'NONE',  ( 0.8761883848702608502, 16.44150283900216181, 68.58316157020807680 ) ) ;
#37723=VERTEX_POINT ( 'NONE', #42924 ) ;
#37840=ORIENTED_EDGE ( 'NONE', *, *, #13068, .T. ) ;
#37864=ORIENTED_EDGE ( 'NONE', *, *, #44247, .F. ) ;
#37886=CARTESIAN_POINT ( 'NONE',  ( -6.891449706524621632, -10.24244278381001472, 65.16993756079229172 ) ) ;
#37917=VERTEX_POINT ( 'NONE', #22424 ) ;
#37980=CARTESIAN_POINT ( 'NONE',  ( 4.330454160168685895, -68.33163558029976059, -20.63184982502311371 ) ) ;
#37991=ORIENTED_EDGE ( 'NONE', *, *, #20706, .F. ) ;
#38029=ORIENTED_EDGE ( 'NONE', *, *, #19109, .T. ) ;
#38030=CARTESIAN_POINT ( 'NONE',  ( -4.465384415997326606, 66.51627080308836071, 26.73837581714138878 ) ) ;
#38032=CARTESIAN_POINT ( 'NONE',  ( -0.4320110153365296912, 49.91454558245937534, 40.68976686129168741 ) ) ;
#38055=CARTESIAN_POINT ( 'NONE',  ( 5.000000000000000000, -11.00479820989369983, -67.37201579502529114 ) ) ;
#38060=CARTESIAN_POINT ( 'NONE',  ( 4.217983994790209579, -51.98644305214834560, 48.84278562423003933 ) ) ;
#38086=CARTESIAN_POINT ( 'NONE',  ( -2.216418498320683828, -51.36626494304695711, -48.60390812669793803 ) ) ;
#38104=EDGE_CURVE ( 'NONE', #53358, #14457, #26099, .T. ) ;
#38105=DIRECTION ( 'NONE',  ( 0.000000000000000000, 1.224646799147353700E-16, 1.000000000000000000 ) ) ;
#38112=EDGE_CURVE ( 'NONE', #17726, #19443, #46385, .T. ) ;
#38194=DIRECTION ( 'NONE',  ( -0.000000000000000000, -0.000000000000000000, 1.000000000000000000 ) ) ;
#38252=CARTESIAN_POINT ( 'NONE',  ( 5.000000000000000000, -52.35862550122924830, -48.98731492261435250 ) ) ;
#38289=CARTESIAN_POINT ( 'NONE',  ( -5.000000000000000888, -66.79212039439843807, 23.29662735513404925 ) ) ;
#38325=DIRECTION ( 'NONE',  ( 0.000000000000000000, 0.000000000000000000, 1.000000000000000000 ) ) ;
#38348=CARTESIAN_POINT ( 'NONE',  ( -2.219371606097689131, -67.78152867896241673, -20.18750705526169043 ) ) ;
#38354=CARTESIAN_POINT ( 'NONE',  ( -5.000000000000000000, -14.32120916179462711, -69.86289779849464310 ) ) ;
#38406=CARTESIAN_POINT ( 'NONE',  ( 5.000000000000001776, 62.13136467932960016, 23.87699943806516245 ) ) ;
#38426=CARTESIAN_POINT ( 'NONE',  ( 3.428378827818292951, 16.35907404636675366, -69.10239319625853227 ) ) ;
#38437=VECTOR ( 'NONE', #617, 1000.000000000000000 ) ;
#38494=EDGE_CURVE ( 'NONE', #6205, #22530, #51332, .T. ) ;
#38498=CARTESIAN_POINT ( 'NONE',  ( 0.8997857290934923036, 51.17549659653047200, -48.53090770943093446 ) ) ;
#38511=AXIS2_PLACEMENT_3D ( 'NONE', #4070, #4432, #61773 ) ;
#38524=CARTESIAN_POINT ( 'NONE',  ( 5.000000000000000000, -10.00000000000000000, -75.19090595827292134 ) ) ;
#38658=VECTOR ( 'NONE', #43427, 1000.000000000000000 ) ;
#38667=CARTESIAN_POINT ( 'NONE',  ( -5.000000000000000000, -62.13136467932989859, 23.87699943806431335 ) ) ;
#38672=EDGE_LOOP ( 'NONE', ( #46012, #36999 ) ) ;
#38726=ORIENTED_EDGE ( 'NONE', *, *, #48999, .F. ) ;
#38731=DIRECTION ( 'NONE',  ( -0.000000000000000000, -0.02418647091589873691, 0.9997074645238147594 ) ) ;
#38732=CARTESIAN_POINT ( 'NONE',  ( 5.126106709314299792, -68.65851429197805089, -20.89429596904636099 ) ) ;
#38739=CARTESIAN_POINT ( 'NONE',  ( -5.000000000000000888, -10.25161785469022035, -64.79070129774558495 ) ) ;
#38786=EDGE_LOOP ( 'NONE', ( #45543, #63955, #60694, #9294 ) ) ;
#38797=VERTEX_POINT ( 'NONE', #42299 ) ;
#38833=CARTESIAN_POINT ( 'NONE',  ( 5.107860025164819184, -50.62490018645517154, -41.07729128472065838 ) ) ;
#38862=CARTESIAN_POINT ( 'NONE',  ( 5.000000000000000000, -16.14408868864072844, 27.96238185062368586 ) ) ;
#38868=CARTESIAN_POINT ( 'NONE',  ( 2.216418498311663487, 51.36626494304667290, -48.60390812669556482 ) ) ;
#38888=VERTEX_POINT ( 'NONE', #35921 ) ;
#38946=CARTESIAN_POINT ( 'NONE',  ( -1.781595147096710186, -67.70776641946466157, 20.12770457511388855 ) ) ;
#38948=CARTESIAN_POINT ( 'NONE',  ( 4.999999999999999112, 52.85071664756648602, 48.38833198888325882 ) ) ;
#38978=ADVANCED_FACE ( 'NONE', ( #9100 ), #33248, .F. ) ;
#38981=AXIS2_PLACEMENT_3D ( 'NONE', #30588, #52495, #36257 ) ;
#38987=ORIENTED_EDGE ( 'NONE', *, *, #70951, .T. ) ;
#38999=CARTESIAN_POINT ( 'NONE',  ( -0.4501631047602908664, -16.44600848780494218, 68.55503832938644848 ) ) ;
#39001=CARTESIAN_POINT ( 'NONE',  ( -5.000000000000003553, 68.48985753891551553, 21.22439692019726820 ) ) ;
#39020=CARTESIAN_POINT ( 'NONE',  ( -0.4451317748925319173, -16.44604352396231661, -68.55481936398555831 ) ) ;
#39038=CARTESIAN_POINT ( 'NONE',  ( -5.000000000000001776, 11.69579520003552098, -68.31051037013783400 ) ) ;
#39090=AXIS2_PLACEMENT_3D ( 'NONE', #58014, #6319, #27824 ) ;
#39091=CARTESIAN_POINT ( 'NONE',  ( -3.496982156821625498, 51.71401992552586080, 48.73755072030351698 ) ) ;
#39093=CARTESIAN_POINT ( 'NONE',  ( -4.336811714530219852, -68.30918023749046597, -20.61428864874384104 ) ) ;
#39133=ADVANCED_FACE ( 'NONE', ( #11333 ), #34367, .T. ) ;
#39150=CIRCLE ( 'NONE', #16223, 71.70204102886728492 ) ;
#39168=CARTESIAN_POINT ( 'NONE',  ( -5.000000000000000000, -15.86295220590816513, 69.92641310672760824 ) ) ;
#39200=CARTESIAN_POINT ( 'NONE',  ( 1.506524674528859187, -55.70638416847143048, -43.84942669317729980 ) ) ;
#39224=DIRECTION ( 'NONE',  ( 0.000000000000000000, -0.9997074645238147594, -0.02418647091589873691 ) ) ;
#39238=CARTESIAN_POINT ( 'NONE',  ( -0.3752463838875753632, 55.62178951997461240, -43.80327721769091198 ) ) ;
#39245=EDGE_LOOP ( 'NONE', ( #2765, #13586, #66616, #33389, #10060, #38726, #29566, #70732, #57287, #31625, #14062, #73008, #58301, #52864, #10413, #49597 ) ) ;
#39320=CARTESIAN_POINT ( 'NONE',  ( 1.882291019709147140, -65.87523470714363327, 26.34730193751357419 ) ) ;
#39329=CARTESIAN_POINT ( 'NONE',  ( 5.000000000000000000, 11.00479820989369806, 67.37201579502529114 ) ) ;
#39371=CARTESIAN_POINT ( 'NONE',  ( -5.000000000000000888, 67.66364885638930105, 22.52891795222361893 ) ) ;
#39388=CARTESIAN_POINT ( 'NONE',  ( -5.126144196591213564, -16.23426282122703768, -69.90718656545267606 ) ) ;
#39399=CARTESIAN_POINT ( 'NONE',  ( 4.193030820682224658, -50.40097124335133572, -40.95512985425011010 ) ) ;
#39405=CARTESIAN_POINT ( 'NONE',  ( -4.999999999999999112, 10.60557809245594463, -66.49298242784793445 ) ) ;
#39458=CARTESIAN_POINT ( 'NONE',  ( 1.317228840344865981, 55.68607278122992454, 43.83834608838541413 ) ) ;
#39460=CARTESIAN_POINT ( 'NONE',  ( 4.104248244554821845, -66.38464254924988950, -26.65807398668032491 ) ) ;
#39467=CARTESIAN_POINT ( 'NONE',  ( 4.999999999999999112, -53.39837237779262580, -47.14918772354958065 ) ) ;
#39473=CARTESIAN_POINT ( 'NONE',  ( -5.000000000000000000, 68.60357193678683529, 20.85024232999420946 ) ) ;
#39486=CARTESIAN_POINT ( 'NONE',  ( -5.000000000000000000, -10.00000000000000000, 75.19090595827292134 ) ) ;
#39512=CARTESIAN_POINT ( 'NONE',  ( 5.000000000000000000, -52.84347807771159466, 43.21644271080197086 ) ) ;
#39544=CARTESIAN_POINT ( 'NONE',  ( -5.000000000000000888, -11.44657803507906024, 68.01244171956641082 ) ) ;
#39587=CARTESIAN_POINT ( 'NONE',  ( -0.3752463838827032050, 10.12385607954549371, 70.07152133708838448 ) ) ;
#39605=CARTESIAN_POINT ( 'NONE',  ( 5.000000000000000000, 52.35862550122891435, 48.98731492261470777 ) ) ;
#39610=DIRECTION ( 'NONE',  ( 0.000000000000000000, 0.000000000000000000, 1.000000000000000000 ) ) ;
#39683=CARTESIAN_POINT ( 'NONE',  ( 1.780377099648655870, -67.71330631781141562, 20.13219356122130677 ) ) ;
#39688=VECTOR ( 'NONE', #4221, 1000.000000000000227 ) ;
#39704=CARTESIAN_POINT ( 'NONE',  ( -5.000000000000000000, -68.60357193678697740, -20.85024232999374050 ) ) ;
#39728=AXIS2_PLACEMENT_3D ( 'NONE', #3944, #9601, #9217 ) ;
#39734=CARTESIAN_POINT ( 'NONE',  ( -3.734423912265183887, -66.26963445013821286, 26.58791153593155343 ) ) ;
#39736=CARTESIAN_POINT ( 'NONE',  ( -5.000000000000000888, 61.23620218020138140, 23.51718915682135957 ) ) ;
#39739=CARTESIAN_POINT ( 'NONE',  ( 5.000000000000000000, -70.11723469343094450, -28.93519894129240910 ) ) ;
#39752=CARTESIAN_POINT ( 'NONE',  ( -1.317228840348697361, -10.12208498181994543, -70.14472670972902790 ) ) ;
#39760=CARTESIAN_POINT ( 'NONE',  ( 2.124081043562912718, -50.03790111639220584, 40.75706181777475479 ) ) ;
#39812=CARTESIAN_POINT ( 'NONE',  ( -13.99999999999999822, 2.249999999994893862, 7.677076266393539683 ) ) ;
#39817=CARTESIAN_POINT ( 'NONE',  ( -0.4320110153365241401, -10.28109898471437589, 63.57214792341211762 ) ) ;
#39825=CARTESIAN_POINT ( 'NONE',  ( -2.990854866100027820, 55.96051345247528985, 43.98806351443512597 ) ) ;
#39832=CARTESIAN_POINT ( 'NONE',  ( 4.999999999999999112, -51.30401030464736323, -41.49390406302068612 ) ) ;
#39835=CARTESIAN_POINT ( 'NONE',  ( 4.999999999999995559, -16.24494643555759410, -69.83755725260751035 ) ) ;
#39850=FACE_OUTER_BOUND ( 'NONE', #56629, .T. ) ;
#39858=DIRECTION ( 'NONE',  ( 0.000000000000000000, -0.4789076340208436311, -0.8778652960885046097 ) ) ;
#39862=B_SPLINE_CURVE_WITH_KNOTS ( 'NONE', 3,
 ( #51912, #30014, #1357, #70377, #35321, #51529, #45871, #34579, #34952, #74546, #63219, #46980 ),
 .UNSPECIFIED., .F., .F.,
 ( 4, 2, 2, 2, 2, 4 ),
 ( 0.000000000000000000, 0.002547658444427998263, 0.005095316888855995659, 0.006369146111069994357, 0.007642975333283993054, 0.01019063377771198611 ),
 .UNSPECIFIED. ) ;
#39863=CARTESIAN_POINT ( 'NONE',  ( 5.000000000000000000, -11.43937387734352029, 68.01947305042915559 ) ) ;
#39901=CARTESIAN_POINT ( 'NONE',  ( -5.000000000000000000, 13.21930962315089353, 69.49101004078882227 ) ) ;
#39910=CARTESIAN_POINT ( 'NONE',  ( -5.000000000000000000, -11.00479820989369806, 67.37201579502529114 ) ) ;
#39911=CARTESIAN_POINT ( 'NONE',  ( 4.999999999999998224, -68.02455775458935250, 22.06917953199485183 ) ) ;
#39918=EDGE_CURVE ( 'NONE', #10343, #29247, #44206, .T. ) ;
#39924=ORIENTED_EDGE ( 'NONE', *, *, #41210, .F. ) ;
#39932=CIRCLE ( 'NONE', #8743, 17.50000000000000000 ) ;
#40055=CARTESIAN_POINT ( 'NONE',  ( 5.000000000000000000, 68.60357193678729004, -20.85024232999272087 ) ) ;
#40057=CARTESIAN_POINT ( 'NONE',  ( -5.000000000000000000, 52.63770595436734823, -42.88862352055258498 ) ) ;
#40059=CARTESIAN_POINT ( 'NONE',  ( 3.544144923084093790, -60.54353712382357600, 23.09461823984349849 ) ) ;
#40065=CARTESIAN_POINT ( 'NONE',  ( 4.615726161707420339, 68.43878643976823639, 20.71807028113882510 ) ) ;
#40069=EDGE_CURVE ( 'NONE', #20164, #57466, #46865, .T. ) ;
#40102=CARTESIAN_POINT ( 'NONE',  ( 5.000000000000000000, -10.00000000000000000, 75.19090595827292134 ) ) ;
#40147=CARTESIAN_POINT ( 'NONE',  ( -5.000000000000000000, 52.35862550122993042, -48.98731492261362064 ) ) ;
#40165=EDGE_LOOP ( 'NONE', ( #41646, #48139, #24341, #29991 ) ) ;
#40200=CARTESIAN_POINT ( 'NONE',  ( -4.471435261918103699, 50.48103707413024210, 40.99880869399409988 ) ) ;
#40206=CARTESIAN_POINT ( 'NONE',  ( 4.999999999999999112, -52.63770595436673716, -42.88862352055331684 ) ) ;
#40213=VERTEX_POINT ( 'NONE', #65806 ) ;
#40219=CARTESIAN_POINT ( 'NONE',  ( 5.000000000000000000, -62.88740100213644268, -24.06179116403768958 ) ) ;
#40223=CARTESIAN_POINT ( 'NONE',  ( -4.104248244544275614, 66.38464254927804120, -26.65807398668060912 ) ) ;
#40265=LINE ( 'NONE', #6687, #13565 ) ;
#40320=ORIENTED_EDGE ( 'NONE', *, *, #66198, .F. ) ;
#40370=ORIENTED_EDGE ( 'NONE', *, *, #65766, .F. ) ;
#40426=CARTESIAN_POINT ( 'NONE',  ( 13.99999999999999822, -2.250000000005106138, 7.677076266390546522 ) ) ;
#40428=CARTESIAN_POINT ( 'NONE',  ( -5.000000000000000000, 50.64189880742145533, -41.08656465431843685 ) ) ;
#40453=CARTESIAN_POINT ( 'NONE',  ( -5.000000000000000000, -62.32183698944596983, -23.94439461060419916 ) ) ;
#40460=VERTEX_POINT ( 'NONE', #11454 ) ;
#40468=ORIENTED_EDGE ( 'NONE', *, *, #63735, .T. ) ;
#40482=CARTESIAN_POINT ( 'NONE',  ( -4.330454160168802247, -68.33163558030018692, 20.63184982502184184 ) ) ;
#40490=EDGE_CURVE ( 'NONE', #41883, #63044, #15983, .T. ) ;
#40513=CARTESIAN_POINT ( 'NONE',  ( -0.8419854211626197626, -49.91401432488752477, 40.68947704085019978 ) ) ;
#40525=ORIENTED_EDGE ( 'NONE', *, *, #38494, .T. ) ;
#40568=CARTESIAN_POINT ( 'NONE',  ( -5.000000000000000000, -10.26105934116143281, 64.40045319026697257 ) ) ;
#40590=ORIENTED_EDGE ( 'NONE', *, *, #17656, .T. ) ;
#40598=CARTESIAN_POINT ( 'NONE',  ( -5.086519500889289169, 60.91611154180230869, -23.32191296475761533 ) ) ;
#40655=EDGE_CURVE ( 'NONE', #10343, #72436, #69591, .T. ) ;
#40658=CARTESIAN_POINT ( 'NONE',  ( 0.4368895104455872702, 51.14729664189188441, 48.52014062455049270 ) ) ;
#40691=DIRECTION ( 'NONE',  ( 1.000000000000000000, -0.000000000000000000, -0.000000000000000000 ) ) ;
#40712=FACE_OUTER_BOUND ( 'NONE', #46759, .T. ) ;
#40726=ORIENTED_EDGE ( 'NONE', *, *, #38112, .F. ) ;
#40743=CARTESIAN_POINT ( 'NONE',  ( -0.8997857291008479752, 16.44125064681836790, -68.58473395859590482 ) ) ;
#40761=EDGE_CURVE ( 'NONE', #4853, #21807, #72506, .T. ) ;
#40795=CARTESIAN_POINT ( 'NONE',  ( -5.000000000000000888, 50.98458432551188224, -41.27351214092388432 ) ) ;
#40798=( BOUNDED_SURFACE ( )  B_SPLINE_SURFACE ( 3, 2, ( 
 ( #46250, #35686, #22481 ),
 ( #5163, #40223, #17580 ),
 ( #29285, #45502, #28903 ),
 ( #23242, #52295, #40598 ),
 ( #35329, #68520, #63226 ),
 ( #28529, #29648, #999 ),
 ( #63599, #62851, #11187 ),
 ( #69642, #57593, #51537 ),
 ( #34587, #46988, #5903 ),
 ( #51921, #23612, #46622 ),
 ( #25449, #65818, #64722 ),
 ( #19795, #48093, #66193 ),
 ( #53035, #13748, #70386 ),
 ( #13018, #48837, #30754 ),
 ( #36056, #71843, #54521 ),
 ( #14125, #65072, #31119 ),
 ( #59073, #48464, #30021 ),
 ( #53408, #37159, #31500 ) ),
 .UNSPECIFIED., .F., .F., .F. ) 
 B_SPLINE_SURFACE_WITH_KNOTS ( ( 4, 2, 2, 2, 2, 2, 2, 2, 4 ),
 ( 3, 3 ),
 ( 0.04202945594032907878, 0.04396162471216779472, 0.04589379348400651065, 0.04782596225584522659, 0.04975813102768394253, 0.05169029979952265846, 0.05265638418544201643, 0.05362246857136137440, 0.05748680611503880628 ),
 ( 0.000000000000000000, 1.000000000000000000 ),
 .UNSPECIFIED. ) 
 GEOMETRIC_REPRESENTATION_ITEM ( )  RATIONAL_B_SPLINE_SURFACE ( (
 ( 1.000000000000000000, 0.6241276099608162875, 1.000000000000000000),
 ( 1.000000000000000000, 0.6218761496799840582, 1.000000000000000000),
 ( 1.000000000000000000, 0.6198047272364743954, 1.000000000000000000),
 ( 1.000000000000000000, 0.6161935119823676033, 1.000000000000000000),
 ( 1.000000000000000000, 0.6146642324081269537, 1.000000000000000000),
 ( 1.000000000000000000, 0.6121850116870736214, 1.000000000000000000),
 ( 1.000000000000000000, 0.6112350889400831599, 1.000000000000000000),
 ( 1.000000000000000000, 0.6099522725971745496, 1.000000000000000000),
 ( 1.000000000000000000, 0.6096208180306917912, 1.000000000000000000),
 ( 1.000000000000000000, 0.6096183796350446160, 1.000000000000000000),
 ( 1.000000000000000000, 0.6099422200101833891, 1.000000000000000000),
 ( 1.000000000000000000, 0.6109087447823334793, 1.000000000000000000),
 ( 1.000000000000000000, 0.6113123981688253217, 1.000000000000000000),
 ( 1.000000000000000000, 0.6122677719809350716, 1.000000000000000000),
 ( 1.000000000000000000, 0.6128199619021440503, 1.000000000000000000),
 ( 1.000000000000000000, 0.6159350830263871091, 1.000000000000000000),
 ( 1.000000000000000000, 0.6195556778517007368, 1.000000000000000000),
 ( 1.000000000000000000, 0.6241278272307889674, 1.000000000000000000) ) ) 
 REPRESENTATION_ITEM ( '' )  SURFACE ( )  );
#40852=CARTESIAN_POINT ( 'NONE',  ( 5.000000000000000000, -16.24494643555759410, 69.83755725260752456 ) ) ;
#40891=CARTESIAN_POINT ( 'NONE',  ( -4.231687259402721502, 51.96503165405514579, -48.83411696341705266 ) ) ;
#40952=CARTESIAN_POINT ( 'NONE',  ( -4.465384415997324830, -66.51627080308854545, -26.73837581714093403 ) ) ;
#40953=CARTESIAN_POINT ( 'NONE',  ( 13.99999999999999822, -2.250000000005106138, 10.23492587299426404 ) ) ;
#40957=CARTESIAN_POINT ( 'NONE',  ( 5.000000000000000000, -52.35862550122924830, -48.98731492261435250 ) ) ;
#40974=CARTESIAN_POINT ( 'NONE',  ( -4.465384415997270651, -56.41424811512369786, 44.23559237190949034 ) ) ;
#41014=CARTESIAN_POINT ( 'NONE',  ( -0.4369882809721231665, -51.14729664189338365, -48.52014062455058507 ) ) ;
#41017=AXIS2_PLACEMENT_3D ( 'NONE', #59498, #36115, #2519 ) ;
#41093=CARTESIAN_POINT ( 'NONE',  ( -13.99999999999999822, 0.000000000000000000, -8.000000000000000000 ) ) ;
#41097=VECTOR ( 'NONE', #50515, 1000.000000000000000 ) ;
#41105=EDGE_CURVE ( 'NONE', #31632, #3, #57029, .T. ) ;
#41107=B_SPLINE_CURVE_WITH_KNOTS ( 'NONE', 3,
 ( #34270, #51597, #56528, #74612, #45940, #38426, #61430, #18756 ),
 .UNSPECIFIED., .F., .F.,
 ( 4, 2, 2, 4 ),
 ( 0.005256334970460992476, 0.006570121696639674713, 0.007883908422818356951, 0.01051148187517570928 ),
 .UNSPECIFIED. ) ;
#41155=CARTESIAN_POINT ( 'NONE',  ( -0.8761883848941678377, 51.17400877215322197, 48.53033992007524944 ) ) ;
#41194=ORIENTED_EDGE ( 'NONE', *, *, #50993, .F. ) ;
#41198=EDGE_CURVE ( 'NONE', #53910, #56676, #36847, .T. ) ;
#41210=EDGE_CURVE ( 'NONE', #3856, #21239, #24282, .T. ) ;
#41307=VERTEX_POINT ( 'NONE', #36234 ) ;
#41319=CARTESIAN_POINT ( 'NONE',  ( 2.997005883565903250, 55.94527535364343862, 43.97975057406247146 ) ) ;
#41325=DIRECTION ( 'NONE',  ( 1.000000000000000000, -0.000000000000000000, -0.000000000000000000 ) ) ;
#41342=CARTESIAN_POINT ( 'NONE',  ( -6.308070865134226324, -51.03903544637460499, 41.30321721934398482 ) ) ;
#41385=CARTESIAN_POINT ( 'NONE',  ( 5.000000000000000000, 52.35862550122993042, -48.98731492261362064 ) ) ;
#41416=CARTESIAN_POINT ( 'NONE',  ( -5.000000000000000000, 60.90295814858222201, 23.31388853594875599 ) ) ;
#41459=CARTESIAN_POINT ( 'NONE',  ( 1.781595147095992537, 67.70776641946450525, 20.12770457511415501 ) ) ;
#41487=CARTESIAN_POINT ( 'NONE',  ( 0.4451317748865717405, 16.44604352396224911, -68.55481936398530252 ) ) ;
#41517=CARTESIAN_POINT ( 'NONE',  ( -4.615726161709537756, 52.16176840074169974, 48.91069252044945870 ) ) ;
#41566=AXIS2_PLACEMENT_3D ( 'NONE', #51598, #45941, #29709 ) ;
#41580=ORIENTED_EDGE ( 'NONE', *, *, #54301, .F. ) ;
#41585=CARTESIAN_POINT ( 'NONE',  ( -5.000000000000000000, -70.11723469343111503, 28.93519894129190817 ) ) ;
#41614=ADVANCED_FACE ( 'NONE', ( #11555, #57595 ), #261, .F. ) ;
#41617=CARTESIAN_POINT ( 'NONE',  ( -5.000000000000000000, 32.28817737728141424, 3.295974604355933479E-13 ) ) ;
#41646=ORIENTED_EDGE ( 'NONE', *, *, #25576, .T. ) ;
#41704=EDGE_CURVE ( 'NONE', #44017, #46951, #52297, .T. ) ;
#41721=DIRECTION ( 'NONE',  ( 0.000000000000000000, 0.000000000000000000, -1.000000000000000000 ) ) ;
#41731=CARTESIAN_POINT ( 'NONE',  ( 4.999999999999999112, 0.000000000000000000, 0.000000000000000000 ) ) ;
#41749=CIRCLE ( 'NONE', #5573, 71.70204102886728492 ) ;
#41750=B_SPLINE_CURVE_WITH_KNOTS ( 'NONE', 3,
 ( #39835, #11914, #62839, #22851, #74164, #34947, #28142, #17566, #34197, #45488 ),
 .UNSPECIFIED., .F., .F.,
 ( 4, 2, 2, 2, 4 ),
 ( 0.000000000000000000, 0.001314083742622691817, 0.002628167485245383635, 0.003942251227868075886, 0.005256334970490767269 ),
 .UNSPECIFIED. ) ;
#41761=EDGE_LOOP ( 'NONE', ( #53366, #477, #52884, #55305, #72138 ) ) ;
#41794=CARTESIAN_POINT ( 'NONE',  ( -5.000000000000000000, 66.79212039439858017, -23.29662735513358385 ) ) ;
#41820=CARTESIAN_POINT ( 'NONE',  ( 4.330454160169023403, 68.33163558030062745, 20.63184982502072984 ) ) ;
#41851=CARTESIAN_POINT ( 'NONE',  ( 5.126144196591270408, 16.23426282122703057, -69.90718656545273291 ) ) ;
#41872=CARTESIAN_POINT ( 'NONE',  ( -7.456155213548131933, -51.58724325107842645, -41.60228463193305970 ) ) ;
#41883=VERTEX_POINT ( 'NONE', #19064 ) ;
#41895=VECTOR ( 'NONE', #28341, 1000.000000000000000 ) ;
#42034=CIRCLE ( 'NONE', #34862, 5.000000000000000888 ) ;
#42042=LINE ( 'NONE', #63960, #49018 ) ;
#42057=DIRECTION ( 'NONE',  ( 1.000000000000000000, -0.000000000000000000, -0.000000000000000000 ) ) ;
#42115=CARTESIAN_POINT ( 'NONE',  ( -5.000000000000000000, 12.24744670179871164, 68.85644987591972210 ) ) ;
#42124=FACE_OUTER_BOUND ( 'NONE', #68126, .T. ) ;
#42126=AXIS2_PLACEMENT_3D ( 'NONE', #29167, #28043, #46878 ) ;
#42164=CARTESIAN_POINT ( 'NONE',  ( -0.8721677472748838866, 16.44158143986581777, 68.58266913489940464 ) ) ;
#42188=AXIS2_PLACEMENT_3D ( 'NONE', #44935, #61906, #67574 ) ;
#42207=AXIS2_PLACEMENT_3D ( 'NONE', #47146, #64872, #64513 ) ;
#42211=CARTESIAN_POINT ( 'NONE',  ( -2.990854866096085640, 10.11452374054098335, -70.45725801588044135 ) ) ;
#42228=VECTOR ( 'NONE', #35933, 1000.000000000000000 ) ;
#42264=ORIENTED_EDGE ( 'NONE', *, *, #25576, .F. ) ;
#42265=CARTESIAN_POINT ( 'NONE',  ( 3.407298021510797525, -68.04056125360885687, -20.39715949456126154 ) ) ;
#42285=VERTEX_POINT ( 'NONE', #15511 ) ;
#42299=CARTESIAN_POINT ( 'NONE',  ( 5.000000000000000000, 10.26105934116143459, -64.40045319026695836 ) ) ;
#42331=DIRECTION ( 'NONE',  ( 1.000000000000000000, -0.000000000000000000, -0.000000000000000000 ) ) ;
#42334=VERTEX_POINT ( 'NONE', #9505 ) ;
#42439=ORIENTED_EDGE ( 'NONE', *, *, #24957, .T. ) ;
#42442=TOROIDAL_SURFACE ( 'NONE', #1551, 81.50000000000000000, 10.99999999999999822 ) ;
#42463=B_SPLINE_CURVE_WITH_KNOTS ( 'NONE', 3,
 ( #41416, #47058, #6716, #5605, #52737, #23686, #64428, #11258, #28976, #34663, #58043, #51614 ),
 .UNSPECIFIED., .F., .F.,
 ( 4, 2, 2, 2, 2, 4 ),
 ( 0.000000000000000000, 0.002547658444427995661, 0.005095316888855991322, 0.006369146111069989152, 0.007642975333283986983, 0.01019063377771198264 ),
 .UNSPECIFIED. ) ;
#42507=CARTESIAN_POINT ( 'NONE',  ( -14.00000000000000178, -2.250000000005106138, 10.23492587299426404 ) ) ;
#42533=CARTESIAN_POINT ( 'NONE',  ( -5.000000000000000000, -52.84634075987140278, 43.22150062466516118 ) ) ;
#42543=CARTESIAN_POINT ( 'NONE',  ( -2.986204309486589110E-14, 67.59332269700053075, 20.03478791450399399 ) ) ;
#42569=ORIENTED_EDGE ( 'NONE', *, *, #69448, .F. ) ;
#42579=CARTESIAN_POINT ( 'NONE',  ( 4.999999999999995559, -16.24494643555759410, -69.83755725260751035 ) ) ;
#42587=B_SPLINE_CURVE_WITH_KNOTS ( 'NONE', 3,
 ( #17620, #17244, #1408, #34626, #51964, #673, #301, #52706, #41014, #12336 ),
 .UNSPECIFIED., .F., .F.,
 ( 4, 2, 2, 2, 4 ),
 ( 0.000000000000000000, 0.001314083742622679674, 0.002628167485245360650, 0.003942251227868041191, 0.005256334970490722167 ),
 .UNSPECIFIED. ) ;
#42700=CARTESIAN_POINT ( 'NONE',  ( -14.00000000000000178, -2.250000000005106138, 10.23492587299426404 ) ) ;
#42734=CARTESIAN_POINT ( 'NONE',  ( -3.544144923088096366, 50.27229464832369388, -40.88493206427705928 ) ) ;
#42747=CARTESIAN_POINT ( 'NONE',  ( 5.000000000000000000, 18.53862685874501537, 23.57305537018163832 ) ) ;
#42795=FACE_OUTER_BOUND ( 'NONE', #70041, .T. ) ;
#42830=CARTESIAN_POINT ( 'NONE',  ( -14.00000000000000178, 0.000000000000000000, 0.000000000000000000 ) ) ;
#42832=FACE_OUTER_BOUND ( 'NONE', #24857, .T. ) ;
#42841=AXIS2_PLACEMENT_3D ( 'NONE', #46672, #33892, #28206 ) ;
#42848=EDGE_CURVE ( 'NONE', #27168, #42334, #801, .T. ) ;
#42921=CARTESIAN_POINT ( 'NONE',  ( 5.000000000000000000, 62.31673578527522750, 23.93255728291440931 ) ) ;
#42924=CARTESIAN_POINT ( 'NONE',  ( -5.000000000000000000, -68.60357193678697740, -20.85024232999374050 ) ) ;
#42942=CARTESIAN_POINT ( 'NONE',  ( 4.999999999999999112, -15.86295220590816868, -69.92641310672759403 ) ) ;
#42949=AXIS2_PLACEMENT_3D ( 'NONE', #17701, #383, #12045 ) ;
#42952=ORIENTED_EDGE ( 'NONE', *, *, #10463, .T. ) ;
#42953=B_SPLINE_CURVE_WITH_KNOTS ( 'NONE', 3,
 ( #22778, #183, #17122, #921, #11846, #6195, #40891, #40147 ),
 .UNSPECIFIED., .F., .F.,
 ( 4, 2, 2, 4 ),
 ( 0.005256334970461100896, 0.006570121696639755378, 0.007883908422818408993, 0.01051148187517571796 ),
 .UNSPECIFIED. ) ;
#43093=ORIENTED_EDGE ( 'NONE', *, *, #2307, .F. ) ;
#43210=PLANE ( 'NONE',  #3712 ) ;
#43230=CARTESIAN_POINT ( 'NONE',  ( 5.000000000000000000, 11.43937387734352029, -68.01947305042915559 ) ) ;
#43241=EDGE_LOOP ( 'NONE', ( #46955, #11255, #11889, #35587, #3895, #17800, #44604, #35801, #29549, #57066, #12507, #44380, #64995, #59505, #64572, #14020, #48384, #54485, #24227, #64203, #10520, #38029, #67245, #15582, #12131, #7978, #63379, #69292, #70257, #4180, #32349, #30052, #47851, #40468, #45443, #10113, #74361, #49410, #52846 ) ) ;
#43274=FACE_OUTER_BOUND ( 'NONE', #26761, .T. ) ;
#43307=ORIENTED_EDGE ( 'NONE', *, *, #50098, .F. ) ;
#43310=CARTESIAN_POINT ( 'NONE',  ( -5.000000000000000000, 60.90295814858271939, -23.31388853594749833 ) ) ;
#43322=CARTESIAN_POINT ( 'NONE',  ( 4.999999999999997335, -12.24343743989403777, -68.85270403949347440 ) ) ;
#43350=CARTESIAN_POINT ( 'NONE',  ( -5.126106709314337984, -52.42424824937356220, -49.01286957842727077 ) ) ;
#43366=CARTESIAN_POINT ( 'NONE',  ( -5.000000000000000000, 0.000000000000000000, 0.000000000000000000 ) ) ;
#43403=TOROIDAL_SURFACE ( 'NONE', #3686, 81.50000000000000000, 10.99999999999999822 ) ;
#43416=DIRECTION ( 'NONE',  ( -1.000000000000000000, -0.000000000000000000, -0.000000000000000000 ) ) ;
#43427=DIRECTION ( 'NONE',  ( -0.000000000000000000, -0.02418647091589873691, 0.9997074645238147594 ) ) ;
#43510=ORIENTED_EDGE ( 'NONE', *, *, #55105, .F. ) ;
#43522=CARTESIAN_POINT ( 'NONE',  ( -4.104248244541351731, -10.10575198619676129, 70.81982386214673397 ) ) ;
#43584=AXIS2_PLACEMENT_3D ( 'NONE', #14596, #8955, #3670 ) ;
#43593=EDGE_CURVE ( 'NONE', #22530, #45708, #15188, .T. ) ;
#43623=CARTESIAN_POINT ( 'NONE',  ( 7.456155213548071536, -61.82225697226390793, -23.87472085067526706 ) ) ;
#43700=DIRECTION ( 'NONE',  ( -1.000000000000000000, -0.000000000000000000, -0.000000000000000000 ) ) ;
#43710=CARTESIAN_POINT ( 'NONE',  ( 2.124081043562907833, 50.03790111639249005, -40.75706181777439951 ) ) ;
#43749=CARTESIAN_POINT ( 'NONE',  ( -5.000000000000000000, 29.68417822476661527, -4.268394125862720934 ) ) ;
#43762=CARTESIAN_POINT ( 'NONE',  ( -14.00000000000000178, -2.250000000005106138, 7.677076266390546522 ) ) ;
#43802=DIRECTION ( 'NONE',  ( 0.000000000000000000, 0.000000000000000000, 1.000000000000000000 ) ) ;
#43929=CARTESIAN_POINT ( 'NONE',  ( 4.465349678513698350, -10.10202304668585604, -70.97395336192410298 ) ) ;
#44006=CARTESIAN_POINT ( 'NONE',  ( 0.4501631047672336461, -67.59340899456768170, -20.03485802339844568 ) ) ;
#44011=CARTESIAN_POINT ( 'NONE',  ( -5.000000000000000888, -14.89980876190747061, -69.94558486267359854 ) ) ;
#44017=VERTEX_POINT ( 'NONE', #23891 ) ;
#44028=CARTESIAN_POINT ( 'NONE',  ( 5.086519500874516986, -50.65542486323015225, 41.09394361258718220 ) ) ;
#44031=DIRECTION ( 'NONE',  ( 0.000000000000000000, -0.8778652960885011680, -0.4789076340208496263 ) ) ;
#44040=CARTESIAN_POINT ( 'NONE',  ( 5.000000000000000000, -15.48016642534403253, 69.96422921944753170 ) ) ;
#44060=CARTESIAN_POINT ( 'NONE',  ( -3.373128826976389938, 50.22031155377479195, 40.85657338450112519 ) ) ;
#44067=EDGE_CURVE ( 'NONE', #17960, #24993, #56910, .T. ) ;
#44071=CARTESIAN_POINT ( 'NONE',  ( -4.193070328474951758, 60.66867996115669825, -23.17096354272497649 ) ) ;
#44073=VERTEX_POINT ( 'NONE', #54428 ) ;
#44086=DIRECTION ( 'NONE',  ( 0.000000000000000000, 0.000000000000000000, -1.000000000000000000 ) ) ;
#44117=CARTESIAN_POINT ( 'NONE',  ( 3.228176881613692206, -50.21013539028081851, -40.85102191503939650 ) ) ;
#44150=CARTESIAN_POINT ( 'NONE',  ( 3.734423912254124733, 56.16062404875547287, -44.09723116535789700 ) ) ;
#44206=B_SPLINE_CURVE_WITH_KNOTS ( 'NONE', 3,
 ( #66916, #48806, #72190, #14093, #71814, #14467, #71071, #38252 ),
 .UNSPECIFIED., .F., .F.,
 ( 4, 2, 2, 4 ),
 ( 0.005256334970490722167, 0.006570121696661957236, 0.007883908422833192306, 0.01051148187517566418 ),
 .UNSPECIFIED. ) ;
#44221=DIRECTION ( 'NONE',  ( 1.000000000000000000, -0.000000000000000000, -0.000000000000000000 ) ) ;
#44228=AXIS2_PLACEMENT_3D ( 'NONE', #38524, #3067, #66056 ) ;
#44235=CARTESIAN_POINT ( 'NONE',  ( 0.7509181236782381808, -65.76106071587273050, 26.27764834702160712 ) ) ;
#44247=EDGE_CURVE ( 'NONE', #14457, #5956, #28681, .T. ) ;
#44254=ORIENTED_EDGE ( 'NONE', *, *, #71554, .F. ) ;
#44262=DIRECTION ( 'NONE',  ( 1.000000000000000000, -0.000000000000000000, -0.000000000000000000 ) ) ;
#44285=CARTESIAN_POINT ( 'NONE',  ( -4.471435261902951375, -10.26549131683149163, 64.21726486257125543 ) ) ;
#44304=CARTESIAN_POINT ( 'NONE',  ( -4.193070328474943764, 10.26769692241485643, -64.12609983179220308 ) ) ;
#44317=CARTESIAN_POINT ( 'NONE',  ( -5.000000000000000000, -66.10919140997998511, 23.67639547905989161 ) ) ;
#44364=CARTESIAN_POINT ( 'NONE',  ( 5.000000000000000000, 53.17721328501398403, -43.91924822456213917 ) ) ;
#44377=CARTESIAN_POINT ( 'NONE',  ( 5.000000000000000000, 10.00000000000000000, 75.19090595827292134 ) ) ;
#44380=ORIENTED_EDGE ( 'NONE', *, *, #69117, .T. ) ;
#44384=CARTESIAN_POINT ( 'NONE',  ( -5.000000000000000888, -10.53354221205070473, -66.31578581128121641 ) ) ;
#44398=CARTESIAN_POINT ( 'NONE',  ( 1.308779242300525114, -49.95118570763320776, 40.70975538998114729 ) ) ;
#44427=ORIENTED_EDGE ( 'NONE', *, *, #49426, .T. ) ;
#44430=CARTESIAN_POINT ( 'NONE',  ( 2.666560895877943341E-14, -16.44602605510714355, 68.55492853905353456 ) ) ;
#44486=CARTESIAN_POINT ( 'NONE',  ( 2.069125466536428259, -55.78340383128517743, -43.89144373685886791 ) ) ;
#44522=CARTESIAN_POINT ( 'NONE',  ( -0.8912353796372728398, 51.17464048784120223, -48.53058040617283098 ) ) ;
#44561=LINE ( 'NONE', #20411, #38658 ) ;
#44586=CARTESIAN_POINT ( 'NONE',  ( 5.000000000000000000, -29.68417822476656553, 4.268394125862919886 ) ) ;
#44604=ORIENTED_EDGE ( 'NONE', *, *, #62565, .T. ) ;
#44607=CARTESIAN_POINT ( 'NONE',  ( 4.999999999999999112, 52.62579568235167216, 48.70175807018058123 ) ) ;
#44660=CARTESIAN_POINT ( 'NONE',  ( -5.000000000000000888, 67.10993666412713310, 23.06595724273690351 ) ) ;
#44669=CARTESIAN_POINT ( 'NONE',  ( -5.000000000000000888, 53.31073972600139399, 44.28411094576038209 ) ) ;
#44672=DIRECTION ( 'NONE',  ( 1.000000000000000000, -0.000000000000000000, -0.000000000000000000 ) ) ;
#44677=CARTESIAN_POINT ( 'NONE',  ( 1.688721909672338040, 10.27943647337372290, -63.64086505882561795 ) ) ;
#44694=CARTESIAN_POINT ( 'NONE',  ( -4.999999999999992006, 10.25159769123454900, -64.79153472057838314 ) ) ;
#44720=ORIENTED_EDGE ( 'NONE', *, *, #69261, .F. ) ;
#44724=FACE_BOUND ( 'NONE', #50514, .T. ) ;
#44748=VECTOR ( 'NONE', #59999, 1000.000000000000000 ) ;
#44749=CARTESIAN_POINT ( 'NONE',  ( -2.216418498320457786, 51.36626494304663026, 48.60390812669818672 ) ) ;
#44751=CARTESIAN_POINT ( 'NONE',  ( -2.997005883566162154, -66.06021892606753454, -26.46015439093728361 ) ) ;
#44772=CARTESIAN_POINT ( 'NONE',  ( 1.506680654948051590, -55.70239491600889892, 43.84725041001744472 ) ) ;
#44796=CARTESIAN_POINT ( 'NONE',  ( 5.000000000000000000, -53.17721328501367850, 43.91924822456251576 ) ) ;
#44804=CARTESIAN_POINT ( 'NONE',  ( -2.160335347077982249, -16.41093803200690715, 68.77481055341485217 ) ) ;
#44835=EDGE_LOOP ( 'NONE', ( #20257, #74627, #38987, #48795, #69115, #5062, #70956, #23946, #20383, #6859, #1930, #11053, #23452, #9202, #28562, #72456 ) ) ;
#44861=CARTESIAN_POINT ( 'NONE',  ( -0.7581620860327765721, -55.63814191976648971, -43.81219805000106504 ) ) ;
#44899=CARTESIAN_POINT ( 'NONE',  ( 4.104248244544244528, 56.27889056305702553, -44.16174987545804242 ) ) ;
#44935=CARTESIAN_POINT ( 'NONE',  ( 13.99999999999999822, 0.000000000000000000, 0.000000000000000000 ) ) ;
#44978=CARTESIAN_POINT ( 'NONE',  ( 0.6474643998350866347, -60.19533971085802904, 22.88219507986015699 ) ) ;
#45050=CARTESIAN_POINT ( 'NONE',  ( 1.308779242298710344, -10.28008949575750641, -63.61387346696258049 ) ) ;
#45060=B_SPLINE_CURVE_WITH_KNOTS ( 'NONE', 3,
 ( #27671, #39001, #33730, #74068, #45767, #39371, #68042, #44660, #16333, #62367, #28787, #56732, #27294, #11442, #50310, #17088, #68778, #73331, #39736, #33355 ),
 .UNSPECIFIED., .F., .F.,
 ( 4, 2, 2, 2, 2, 2, 2, 2, 2, 4 ),
 ( 0.000000000000000000, 0.001156441540183992178, 0.001734662310275988158, 0.002312883080367984356, 0.003469324620551976317, 0.004625766160735968711, 0.005782207700919960239, 0.006938649241103952633, 0.008095090781287984927, 0.009251532321472018955 ),
 .UNSPECIFIED. ) ;
#45066=CARTESIAN_POINT ( 'NONE',  ( -5.000000000000001776, 10.82431413986196134, -67.03128830763429846 ) ) ;
#45097=VECTOR ( 'NONE', #23297, 1000.000000000000000 ) ;
#45105=DIRECTION ( 'NONE',  ( -0.000000000000000000, 0.4789076340208374138, 0.8778652960885079404 ) ) ;
#45118=CARTESIAN_POINT ( 'NONE',  ( 0.8912353796319145705, 51.17464048784069064, 48.53058040617271729 ) ) ;
#45120=CARTESIAN_POINT ( 'NONE',  ( 0.6547826978432315093, -60.19560277018764083, -22.88235556323010300 ) ) ;
#45139=CARTESIAN_POINT ( 'NONE',  ( -0.3752463838874934843, -55.62178951997881882, 43.80327721769354810 ) ) ;
#45198=CARTESIAN_POINT ( 'NONE',  ( 5.000000000000000000, -68.60357193678713372, 20.85024232999320404 ) ) ;
#45242=CARTESIAN_POINT ( 'NONE',  ( 1.308779242311841839, 10.28008949575769293, 63.61387346695496348 ) ) ;
#45253=FACE_OUTER_BOUND ( 'NONE', #32664, .T. ) ;
#45267=CARTESIAN_POINT ( 'NONE',  ( -2.069125466540701286, 55.78340383128293212, -43.89144373685724787 ) ) ;
#45274=ORIENTED_EDGE ( 'NONE', *, *, #69261, .T. ) ;
#45281=CARTESIAN_POINT ( 'NONE',  ( 5.000000000000000000, -50.64189880742087269, -41.08656465431914029 ) ) ;
#45289=CARTESIAN_POINT ( 'NONE',  ( -4.737866951562140549, 16.26762833210766956, -69.68949229523444444 ) ) ;
#45339=CARTESIAN_POINT ( 'NONE',  ( 0.4451317748866334134, -67.59323688304569089, 20.03471819849699997 ) ) ;
#45342=CARTESIAN_POINT ( 'NONE',  ( 5.000000000000000000, 50.64189880742059557, 41.08656465431948845 ) ) ;
#45407=CARTESIAN_POINT ( 'NONE',  ( -1.882291019712477143, -10.12018455450522580, -70.22327770540287872 ) ) ;
#45416=VERTEX_POINT ( 'NONE', #27528 ) ;
#45443=ORIENTED_EDGE ( 'NONE', *, *, #18166, .T. ) ;
#45478=CARTESIAN_POINT ( 'NONE',  ( -4.330454160167357180, 52.03352386568316490, 48.86100738217030681 ) ) ;
#45485=CARTESIAN_POINT ( 'NONE',  ( 5.000000000000001776, -53.32026166094865971, -44.27875806161964789 ) ) ;
#45488=CARTESIAN_POINT ( 'NONE',  ( -3.018451720292563716E-14, -16.44602605510714355, -68.55492853905353456 ) ) ;
#45502=CARTESIAN_POINT ( 'NONE',  ( -3.734423912264015932, 66.26963445014290244, -26.58791153592997247 ) ) ;
#45511=PLANE ( 'NONE',  #7325 ) ;
#45543=ORIENTED_EDGE ( 'NONE', *, *, #23310, .T. ) ;
#45567=CARTESIAN_POINT ( 'NONE',  ( 0.8721677472509306028, 51.17354301023034679, 48.53016177276406040 ) ) ;
#45601=EDGE_CURVE ( 'NONE', #74324, #48525, #39932, .T. ) ;
#45610=CARTESIAN_POINT ( 'NONE',  ( 3.074111742571302042, 16.37317034319775644, 69.01341173091257986 ) ) ;
#45651=VERTEX_POINT ( 'NONE', #39605 ) ;
#45656=EDGE_CURVE ( 'NONE', #27257, #4330, #46001, .T. ) ;
#45660=ORIENTED_EDGE ( 'NONE', *, *, #45601, .T. ) ;
#45663=CARTESIAN_POINT ( 'NONE',  ( 5.000000000000000000, -70.11723469343111503, 28.93519894129190817 ) ) ;
#45708=VERTEX_POINT ( 'NONE', #17697 ) ;
#45709=CARTESIAN_POINT ( 'NONE',  ( -1.308779242311917335, -60.23127520339022567, 22.90411807697330104 ) ) ;
#45720=CARTESIAN_POINT ( 'NONE',  ( 4.999999999999999112, 10.60557809245594463, 66.49298242784793445 ) ) ;
#45730=CARTESIAN_POINT ( 'NONE',  ( -4.999999999999998224, -68.02455775458921039, -22.06917953199535276 ) ) ;
#45759=EDGE_CURVE ( 'NONE', #15493, #3120, #49341, .T. ) ;
#45765=CARTESIAN_POINT ( 'NONE',  ( -3.074111742570127426, -67.95395293240403589, 20.32712440775640772 ) ) ;
#45767=CARTESIAN_POINT ( 'NONE',  ( -5.000000000000000888, 67.91007042436096697, 22.22893179988047763 ) ) ;
#45808=ORIENTED_EDGE ( 'NONE', *, *, #29277, .T. ) ;
#45843=CARTESIAN_POINT ( 'NONE',  ( -5.000000000000000000, -10.26105934116142215, -64.40045319026754100 ) ) ;
#45853=CARTESIAN_POINT ( 'NONE',  ( 1.558072418983279750, 51.25713184919774079, 48.56213741370889636 ) ) ;
#45855=CARTESIAN_POINT ( 'NONE',  ( -7.456209740496416494, -61.82228229130281250, -23.87473629694239463 ) ) ;
#45871=CARTESIAN_POINT ( 'NONE',  ( -0.8588954341814998283, -60.21087566322590590, 22.89167302533720871 ) ) ;
#45875=CARTESIAN_POINT ( 'NONE',  ( 5.000000000000000000, -63.84827628760507423, -24.15557308422348015 ) ) ;
#45880=CARTESIAN_POINT ( 'NONE',  ( -2.589639417659010068, -50.10293296561829379, 40.79253907059205631 ) ) ;
#45940=CARTESIAN_POINT ( 'NONE',  ( 2.170320029193673506, 16.41060967376299473, -68.77687409974411992 ) ) ;
#45941=DIRECTION ( 'NONE',  ( 1.000000000000000000, -0.000000000000000000, -0.000000000000000000 ) ) ;
#45984=CARTESIAN_POINT ( 'NONE',  ( -4.465384415997333711, 10.10202268796506431, 70.97396818905025384 ) ) ;
#46001=LINE ( 'NONE', #62983, #25416 ) ;
#46006=DIRECTION ( 'NONE',  ( -0.000000000000000000, -0.000000000000000000, -1.000000000000000000 ) ) ;
#46012=ORIENTED_EDGE ( 'NONE', *, *, #70709, .T. ) ;
#46067=CARTESIAN_POINT ( 'NONE',  ( 5.000000000000000000, 10.26105934116143281, 64.40045319026697257 ) ) ;
#46069=DIRECTION ( 'NONE',  ( -1.000000000000000000, 0.000000000000000000, 0.000000000000000000 ) ) ;
#46079=CARTESIAN_POINT ( 'NONE',  ( -5.000000000000000000, 51.89737250574564342, -42.00009673807059585 ) ) ;
#46087=CARTESIAN_POINT ( 'NONE',  ( 2.584176044310538600, 67.83040087281460728, 20.22720375976279072 ) ) ;
#46094=CARTESIAN_POINT ( 'NONE',  ( 5.000000000000001776, 61.58678017309407693, -23.68362420833262405 ) ) ;
#46097=ORIENTED_EDGE ( 'NONE', *, *, #6917, .T. ) ;
#46105=CARTESIAN_POINT ( 'NONE',  ( -5.000000000000000000, -66.79063484153778063, -23.29724706625406228 ) ) ;
#46136=CARTESIAN_POINT ( 'NONE',  ( 1.558072418987630714, -16.42747873774311884, 68.67104701338894301 ) ) ;
#46204=CIRCLE ( 'NONE', #38981, 71.70204102886728492 ) ;
#46208=ORIENTED_EDGE ( 'NONE', *, *, #60460, .F. ) ;
#46229=CARTESIAN_POINT ( 'NONE',  ( -2.591411123064620181, 50.09422832877455534, 40.78779037275248243 ) ) ;
#46250=CARTESIAN_POINT ( 'NONE',  ( -5.126106709314346865, 68.65851429197836353, -20.89429596904543018 ) ) ;
#46263=CARTESIAN_POINT ( 'NONE',  ( 5.000000000000000000, -10.53354221205055907, 66.31578581128081851 ) ) ;
#46296=ORIENTED_EDGE ( 'NONE', *, *, #53720, .T. ) ;
#46308=( BOUNDED_SURFACE ( )  B_SPLINE_SURFACE ( 3, 2, ( 
 ( #6759, #29763, #58818 ),
 ( #47842, #57711, #63717 ),
 ( #41820, #7128, #6017 ),
 ( #64473, #29021, #63343 ),
 ( #1115, #53152, #12040 ),
 ( #35074, #18445, #747 ),
 ( #41459, #58451, #24827 ),
 ( #35802, #1486, #70498 ),
 ( #18817, #11668, #64830 ),
 ( #13134, #36168, #59188 ),
 ( #7498, #1841, #70863 ),
 ( #19174, #52040, #376 ),
 ( #23357, #71218, #36907 ),
 ( #2947, #2201, #49716 ),
 ( #19538, #36539, #14246 ),
 ( #8603, #13864, #59550 ),
 ( #48579, #37283, #59915 ),
 ( #8231, #38030, #53889 ) ),
 .UNSPECIFIED., .F., .F., .F. ) 
 B_SPLINE_SURFACE_WITH_KNOTS ( ( 4, 2, 2, 2, 2, 2, 2, 2, 4 ),
 ( 3, 3 ),
 ( 0.04202945594032922449, 0.04396162471216792655, 0.04589379348400663555, 0.04782596225584534455, 0.04975813102768404661, 0.05169029979952274867, 0.05265638418544209970, 0.05362246857136145073, 0.05748680611503886179 ),
 ( 0.000000000000000000, 1.000000000000000000 ),
 .UNSPECIFIED. ) 
 GEOMETRIC_REPRESENTATION_ITEM ( )  RATIONAL_B_SPLINE_SURFACE ( (
 ( 1.000000000000000000, 0.6241276099608158434, 1.000000000000000000),
 ( 1.000000000000000000, 0.6218761496800927491, 1.000000000000000000),
 ( 1.000000000000000000, 0.6198047272363291782, 1.000000000000000000),
 ( 1.000000000000000000, 0.6161935119825117102, 1.000000000000000000),
 ( 1.000000000000000000, 0.6146642324080550113, 1.000000000000000000),
 ( 1.000000000000000000, 0.6121850116871446756, 1.000000000000000000),
 ( 1.000000000000000000, 0.6112350889399391640, 1.000000000000000000),
 ( 1.000000000000000000, 0.6099522725973176573, 1.000000000000000000),
 ( 1.000000000000000000, 0.6096208180308001490, 1.000000000000000000),
 ( 1.000000000000000000, 0.6096183796349362582, 1.000000000000000000),
 ( 1.000000000000000000, 0.6099422200102193603, 1.000000000000000000),
 ( 1.000000000000000000, 0.6109087447823151606, 1.000000000000000000),
 ( 1.000000000000000000, 0.6113123981688073361, 1.000000000000000000),
 ( 1.000000000000000000, 0.6122677719809532793, 1.000000000000000000),
 ( 1.000000000000000000, 0.6128199619021084121, 1.000000000000000000),
 ( 1.000000000000000000, 0.6159350830265307719, 1.000000000000000000),
 ( 1.000000000000000000, 0.6195556778515927121, 1.000000000000000000),
 ( 1.000000000000000000, 0.6241278272307889674, 1.000000000000000000) ) ) 
 REPRESENTATION_ITEM ( '' )  SURFACE ( )  );
#46314=CARTESIAN_POINT ( 'NONE',  ( -2.886287813027996254E-11, 51.14729664189304970, 48.52014062455092613 ) ) ;
#46349=ORIENTED_EDGE ( 'NONE', *, *, #13878, .F. ) ;
#46385=LINE ( 'NONE', #56230, #69484 ) ;
#46513=DIRECTION ( 'NONE',  ( 0.000000000000000000, 0.000000000000000000, -1.000000000000000000 ) ) ;
#46593=DIRECTION ( 'NONE',  ( 1.000000000000000000, -0.000000000000000000, -0.000000000000000000 ) ) ;
#46609=CARTESIAN_POINT ( 'NONE',  ( -0.8721677472748865512, -51.17354301023302554, 48.53016177276413146 ) ) ;
#46622=CARTESIAN_POINT ( 'NONE',  ( 0.6474643998348341700, 60.19533971085920854, -22.88219507986035950 ) ) ;
#46672=CARTESIAN_POINT ( 'NONE',  ( -5.000000000000000000, 16.14408868864073554, -27.96238185062347981 ) ) ;
#46681=LINE ( 'NONE', #12353, #48584 ) ;
#46720=CARTESIAN_POINT ( 'NONE',  ( -2.436599634630690403, 16.39988855009608670, 68.84456747601289806 ) ) ;
#46734=VERTEX_POINT ( 'NONE', #6162 ) ;
#46759=EDGE_LOOP ( 'NONE', ( #49136, #37864, #53843, #9335, #67119 ) ) ;
#46766=CARTESIAN_POINT ( 'NONE',  ( 2.266287154880021859, 10.27715108473168648, -63.73532778936322529 ) ) ;
#46801=CARTESIAN_POINT ( 'NONE',  ( 4.231687259407054036, -16.30907003467246952, 69.42009600258495539 ) ) ;
#46822=ORIENTED_EDGE ( 'NONE', *, *, #52077, .T. ) ;
#46823=CARTESIAN_POINT ( 'NONE',  ( -3.407298021520050568, 16.35582233947122432, -69.12343428066031947 ) ) ;
#46837=EDGE_CURVE ( 'NONE', #29307, #34067, #8583, .T. ) ;
#46842=ORIENTED_EDGE ( 'NONE', *, *, #72604, .F. ) ;
#46858=ADVANCED_FACE ( 'NONE', ( #4767 ), #71519, .F. ) ;
#46865=B_SPLINE_CURVE_WITH_KNOTS ( 'NONE', 3,
 ( #35675, #35317, #46609, #6634, #24699, #29639, #53024, #2072 ),
 .UNSPECIFIED., .F., .F.,
 ( 4, 2, 2, 4 ),
 ( 0.005256334970490777678, 0.006570121696662012747, 0.007883908422833246082, 0.01051148187517571622 ),
 .UNSPECIFIED. ) ;
#46878=DIRECTION ( 'NONE',  ( 0.000000000000000000, 0.000000000000000000, -1.000000000000000000 ) ) ;
#46893=DIRECTION ( 'NONE',  ( 1.000000000000000000, -0.000000000000000000, -0.000000000000000000 ) ) ;
#46894=ORIENTED_EDGE ( 'NONE', *, *, #9142, .F. ) ;
#46951=VERTEX_POINT ( 'NONE', #12272 ) ;
#46955=ORIENTED_EDGE ( 'NONE', *, *, #35899, .T. ) ;
#46980=CARTESIAN_POINT ( 'NONE',  ( -5.000000000000000000, -60.90295814858257017, 23.31388853594792820 ) ) ;
#46988=CARTESIAN_POINT ( 'NONE',  ( -0.3794862803194996581, 65.74576272851732028, -26.26831557574448794 ) ) ;
#47040=FACE_OUTER_BOUND ( 'NONE', #307, .T. ) ;
#47052=ORIENTED_EDGE ( 'NONE', *, *, #15001, .F. ) ;
#47058=CARTESIAN_POINT ( 'NONE',  ( -4.193030820682219328, 60.66866849074632739, 23.17095654502715973 ) ) ;
#47074=CARTESIAN_POINT ( 'NONE',  ( -5.000000000000000000, 64.62379132009284888, -24.09319349500319163 ) ) ;
#47080=CARTESIAN_POINT ( 'NONE',  ( 0.000000000000000000, 0.000000000000000000, 0.000000000000000000 ) ) ;
#47087=CARTESIAN_POINT ( 'NONE',  ( -3.728321214232717562, 10.10963409588413953, 70.65936332829922151 ) ) ;
#47112=AXIS2_PLACEMENT_3D ( 'NONE', #69852, #18164, #69478 ) ;
#47136=CARTESIAN_POINT ( 'NONE',  ( -0.6547826978431597889, 10.28110016890869893, -63.57209897671331333 ) ) ;
#47146=CARTESIAN_POINT ( 'NONE',  ( -14.00000000000000178, 2.249999999994893862, 10.23492587299426404 ) ) ;
#47158=FACE_OUTER_BOUND ( 'NONE', #29059, .T. ) ;
#47190=CARTESIAN_POINT ( 'NONE',  ( -4.615726161709595488, 16.27701803902710154, -69.62876280158768338 ) ) ;
#47344=CARTESIAN_POINT ( 'NONE',  ( -0.8761883848953855303, -67.61551161115575326, 20.05282165013548834 ) ) ;
#47387=CARTESIAN_POINT ( 'NONE',  ( 0.000000000000000000, 0.000000000000000000, -8.000000000000000000 ) ) ;
#47426=VECTOR ( 'NONE', #44262, 1000.000000000000000 ) ;
#47462=CARTESIAN_POINT ( 'NONE',  ( -0.8912353796322802779, 16.44139524822730891, 68.58382889509240954 ) ) ;
#47502=CARTESIAN_POINT ( 'NONE',  ( 2.436599634630545630, 16.39988855009607605, -68.84456747601286963 ) ) ;
#47525=CARTESIAN_POINT ( 'NONE',  ( -6.891449706541976639, -51.31760009879133833, -41.45518442798706360 ) ) ;
#47539=EDGE_CURVE ( 'NONE', #36985, #52335, #52945, .T. ) ;
#47561=CIRCLE ( 'NONE', #15018, 71.70204102886728492 ) ;
#47603=ORIENTED_EDGE ( 'NONE', *, *, #32233, .F. ) ;
#47696=CARTESIAN_POINT ( 'NONE',  ( 5.126144196591297941, 52.42426806216620605, 49.01287729762282197 ) ) ;
#47773=CARTESIAN_POINT ( 'NONE',  ( 5.000000000000002665, 14.32120916179452230, -69.86289779849464310 ) ) ;
#47818=CARTESIAN_POINT ( 'NONE',  ( -5.000000000000000888, -53.18690467503099484, 43.91652490638204398 ) ) ;
#47842=CARTESIAN_POINT ( 'NONE',  ( 4.737866951562526907, 68.48668487056681897, 20.75656675268901097 ) ) ;
#47848=LINE ( 'NONE', #23736, #73091 ) ;
#47851=ORIENTED_EDGE ( 'NONE', *, *, #11808, .T. ) ;
#47865=CARTESIAN_POINT ( 'NONE',  ( 4.999999999999999112, -15.47455834364811267, -69.96446835377027185 ) ) ;
#47939=VERTEX_POINT ( 'NONE', #72322 ) ;
#47948=EDGE_CURVE ( 'NONE', #57466, #20924, #48364, .T. ) ;
#47992=DIRECTION ( 'NONE',  ( 1.000000000000000000, -0.000000000000000000, 0.000000000000000000 ) ) ;
#48048=ADVANCED_FACE ( 'NONE', ( #43274 ), #66290, .F. ) ;
#48085=LINE ( 'NONE', #19054, #27488 ) ;
#48093=CARTESIAN_POINT ( 'NONE',  ( 1.317228840344749186, 65.80815776305091447, -26.30638062134158872 ) ) ;
#48114=B_SPLINE_CURVE_WITH_KNOTS ( 'NONE', 3,
 ( #51757, #22324, #35171, #50633, #104, #22703, #45720, #68365, #39329, #10653, #11031, #68734, #23082, #69111, #17418, #19636, #35532, #53249, #58917, #59283, #6851, #64924 ),
 .UNSPECIFIED., .F., .F.,
 ( 4, 2, 2, 2, 2, 2, 2, 2, 2, 2, 4 ),
 ( 0.000000000000000000, 0.001156727053362482157, 0.001735090580043723235, 0.002313454106724964314, 0.003470181160087444303, 0.004048544686768682996, 0.004626908213449921689, 0.005783635266812366983, 0.006940362320174811410, 0.008097089373537256704, 0.009253816426899701131 ),
 .UNSPECIFIED. ) ;
#48127=DIRECTION ( 'NONE',  ( 0.000000000000000000, 0.000000000000000000, -1.000000000000000000 ) ) ;
#48133=CARTESIAN_POINT ( 'NONE',  ( 3.407298021520018594, 51.68473891414078025, -48.72627478609679486 ) ) ;
#48139=ORIENTED_EDGE ( 'NONE', *, *, #6602, .T. ) ;
#48145=CARTESIAN_POINT ( 'NONE',  ( 5.000000000000000000, 15.48016642534403253, -69.96422921944753170 ) ) ;
#48158=EDGE_CURVE ( 'NONE', #30597, #72156, #65287, .T. ) ;
#48160=CIRCLE ( 'NONE', #32515, 70.50000000000000000 ) ;
#48174=CIRCLE ( 'NONE', #39728, 71.70204102886728492 ) ;
#48197=DIRECTION ( 'NONE',  ( 0.000000000000000000, 0.000000000000000000, 1.000000000000000000 ) ) ;
#48205=CARTESIAN_POINT ( 'NONE',  ( 5.000000000000000000, -50.64189880742116401, 41.08656465431877791 ) ) ;
#48212=CARTESIAN_POINT ( 'NONE',  ( -0.8588954341814981630, 49.93020820668157000, 40.69831139579171264 ) ) ;
#48223=EDGE_CURVE ( 'NONE', #6191, #54592, #29291, .T. ) ;
#48249=CARTESIAN_POINT ( 'NONE',  ( -2.804140485925949776E-11, 67.59332269700094287, -20.03478791450258001 ) ) ;
#48309=CARTESIAN_POINT ( 'NONE',  ( -14.00000000000000178, -2.250000000005106138, 7.677076266390546522 ) ) ;
#48364=CIRCLE ( 'NONE', #72508, 71.70204102886728492 ) ;
#48384=ORIENTED_EDGE ( 'NONE', *, *, #53301, .T. ) ;
#48394=CARTESIAN_POINT ( 'NONE',  ( 1.308779242300813994, 49.95118570763349908, -40.70975538998080623 ) ) ;
#48464=CARTESIAN_POINT ( 'NONE',  ( 3.728321214196736566, 66.24762070555856042, -26.57448171418095484 ) ) ;
#48472=VECTOR ( 'NONE', #4628, 1000.000000000000000 ) ;
#48477=EDGE_CURVE ( 'NONE', #3, #37917, #73751, .T. ) ;
#48525=VERTEX_POINT ( 'NONE', #59078 ) ;
#48579=CARTESIAN_POINT ( 'NONE',  ( -4.336811714529519968, 68.30918023749056545, 20.61428864874217481 ) ) ;
#48584=VECTOR ( 'NONE', #34274, 999.9999999999998863 ) ;
#48597=EDGE_CURVE ( 'NONE', #3455, #20924, #68037, .T. ) ;
#48608=LINE ( 'NONE', #53911, #19792 ) ;
#48693=EDGE_CURVE ( 'NONE', #27168, #7738, #36505, .T. ) ;
#48736=ORIENTED_EDGE ( 'NONE', *, *, #71578, .F. ) ;
#48765=CARTESIAN_POINT ( 'NONE',  ( -1.317228840347983265, 55.68607278123570126, -43.83834608838444069 ) ) ;
#48767=CARTESIAN_POINT ( 'NONE',  ( -5.000000000000000000, 70.11723469343073134, 28.93519894129288517 ) ) ;
#48780=DIRECTION ( 'NONE',  ( 1.000000000000000000, 0.000000000000000000, 0.000000000000000000 ) ) ;
#48795=ORIENTED_EDGE ( 'NONE', *, *, #33981, .T. ) ;
#48806=CARTESIAN_POINT ( 'NONE',  ( 0.4368895104719984768, -51.14729664189336944, -48.52014062455057086 ) ) ;
#48837=CARTESIAN_POINT ( 'NONE',  ( 1.882291019709091628, 65.87523470713929896, -26.34730193751198968 ) ) ;
#48841=EDGE_LOOP ( 'NONE', ( #74151, #24702, #13008, #54300 ) ) ;
#48842=CARTESIAN_POINT ( 'NONE',  ( -5.000000000000000000, -67.91996363552676996, 22.23680535815869774 ) ) ;
#48865=CARTESIAN_POINT ( 'NONE',  ( -1.736494649863607131, 67.70200331863343024, -20.12302832235386418 ) ) ;
#48869=DIRECTION ( 'NONE',  ( -1.000000000000000000, -0.000000000000000000, -0.000000000000000000 ) ) ;
#48877=AXIS2_PLACEMENT_3D ( 'NONE', #54388, #43416, #43802 ) ;
#48885=CARTESIAN_POINT ( 'NONE',  ( 5.000000000000000000, 10.26105934116143459, -64.40045319026695836 ) ) ;
#48891=EDGE_CURVE ( 'NONE', #8905, #16375, #53617, .T. ) ;
#48939=CARTESIAN_POINT ( 'NONE',  ( -5.000000000000000000, 68.60357193678683529, 20.85024232999420946 ) ) ;
#48954=CARTESIAN_POINT ( 'NONE',  ( 0.8588954341814944993, -60.21087566322576379, -22.89167302533761728 ) ) ;
#48961=EDGE_LOOP ( 'NONE', ( #46894, #43093, #73149, #69934, #60851 ) ) ;
#48978=DIRECTION ( 'NONE',  ( -0.000000000000000000, -1.000000000000000000, -0.000000000000000000 ) ) ;
#48984=CARTESIAN_POINT ( 'NONE',  ( -4.193030820682226434, 50.40097124335192547, -40.95512985424939245 ) ) ;
#48999=EDGE_CURVE ( 'NONE', #21239, #18569, #52056, .T. ) ;
#49015=CARTESIAN_POINT ( 'NONE',  ( -2.926785083138225622E-14, 16.44602605510714355, 68.55492853905353456 ) ) ;
#49018=VECTOR ( 'NONE', #35303, 1000.000000000000000 ) ;
#49024=CARTESIAN_POINT ( 'NONE',  ( -4.231687259407060253, -68.27410168872928864, -20.58597903916688665 ) ) ;
#49106=DIRECTION ( 'NONE',  ( 0.000000000000000000, 0.000000000000000000, -1.000000000000000000 ) ) ;
#49136=ORIENTED_EDGE ( 'NONE', *, *, #23183, .F. ) ;
#49160=LINE ( 'NONE', #72167, #47426 ) ;
#49170=DIRECTION ( 'NONE',  ( 1.000000000000000000, -0.000000000000000000, -0.000000000000000000 ) ) ;
#49184=FACE_OUTER_BOUND ( 'NONE', #56764, .T. ) ;
#49206=DIRECTION ( 'NONE',  ( 0.000000000000000000, 0.000000000000000000, -1.000000000000000000 ) ) ;
#49223=ADVANCED_FACE ( 'NONE', ( #50907 ), #73547, .F. ) ;
#49278=CARTESIAN_POINT ( 'NONE',  ( -3.228176881614594596, -60.48309044411862345, -23.05774181791981547 ) ) ;
#49300=CARTESIAN_POINT ( 'NONE',  ( 3.496982156811260900, -51.71401992552191018, 48.73755072030270696 ) ) ;
#49316=DIRECTION ( 'NONE',  ( -1.000000000000000000, -0.000000000000000000, -0.000000000000000000 ) ) ;
#49326=CARTESIAN_POINT ( 'NONE',  ( 5.000000000000000000, -52.85372778481357869, 48.38359481482874713 ) ) ;
#49334=CARTESIAN_POINT ( 'NONE',  ( -1.704527592502766309, 49.99193291617112322, 40.73198448289741691 ) ) ;
#49341=B_SPLINE_CURVE_WITH_KNOTS ( 'NONE', 3,
 ( #12043, #4912, #6020, #35077, #58089, #6400, #27906, #50915 ),
 .UNSPECIFIED., .F., .F.,
 ( 4, 2, 2, 4 ),
 ( 0.005256334970460276035, 0.006570121696639122204, 0.007883908422817968373, 0.01051148187517565204 ),
 .UNSPECIFIED. ) ;
#49391=CARTESIAN_POINT ( 'NONE',  ( 1.736494649845416349, 16.42394793108440254, 68.69316892220884085 ) ) ;
#49400=CARTESIAN_POINT ( 'NONE',  ( -2.978189300774432354E-14, -67.59332269700065865, -20.03478791450352858 ) ) ;
#49410=ORIENTED_EDGE ( 'NONE', *, *, #61871, .T. ) ;
#49426=EDGE_CURVE ( 'NONE', #45416, #1129, #58100, .T. ) ;
#49455=AXIS2_PLACEMENT_3D ( 'NONE', #6423, #73957, #33 ) ;
#49466=CIRCLE ( 'NONE', #26582, 5.000000000000000000 ) ;
#49469=AXIS2_PLACEMENT_3D ( 'NONE', #69277, #34594, #73815 ) ;
#49516=CARTESIAN_POINT ( 'NONE',  ( -5.000000000000000000, -29.68417822476656553, 4.268394125862918997 ) ) ;
#49565=CARTESIAN_POINT ( 'NONE',  ( -2.216418498312179075, -16.40908668940157611, 68.78644440154799611 ) ) ;
#49597=ORIENTED_EDGE ( 'NONE', *, *, #29605, .F. ) ;
#49599=ORIENTED_EDGE ( 'NONE', *, *, #52654, .T. ) ;
#49615=EDGE_CURVE ( 'NONE', #17647, #58637, #61618, .T. ) ;
#49656=VERTEX_POINT ( 'NONE', #32748 ) ;
#49662=CARTESIAN_POINT ( 'NONE',  ( 1.308779242313053537, -60.23127520338580609, -22.90411807697111257 ) ) ;
#49716=CARTESIAN_POINT ( 'NONE',  ( -3.228176881614092331, 60.48309044411788449, 23.05774181791989008 ) ) ;
#49723=ORIENTED_EDGE ( 'NONE', *, *, #50675, .T. ) ;
#49776=DIRECTION ( 'NONE',  ( 1.000000000000000000, -0.000000000000000000, -0.000000000000000000 ) ) ;
#49786=CARTESIAN_POINT ( 'NONE',  ( 1.506680654954607457, 10.12163528317106120, 70.16331425390788468 ) ) ;
#49808=ORIENTED_EDGE ( 'NONE', *, *, #22673, .T. ) ;
#49837=CARTESIAN_POINT ( 'NONE',  ( 5.000000000000000000, 10.26105934116143281, 64.40045319026697257 ) ) ;
#49970=ORIENTED_EDGE ( 'NONE', *, *, #35639, .T. ) ;
#50031=CARTESIAN_POINT ( 'NONE',  ( -0.4451317748866462920, -67.59323688304517930, -20.03471819849869817 ) ) ;
#50038=CARTESIAN_POINT ( 'NONE',  ( -5.000000000000000000, -16.24494643555759410, -69.83755725260751035 ) ) ;
#50052=CARTESIAN_POINT ( 'NONE',  ( 0.8997857290928857887, -51.17549659653120386, 48.53090770943006049 ) ) ;
#50079=CARTESIAN_POINT ( 'NONE',  ( 5.000000000000000000, -53.55895565990308427, 45.41404144516045704 ) ) ;
#50098=EDGE_CURVE ( 'NONE', #41307, #16897, #64165, .T. ) ;
#50141=CARTESIAN_POINT ( 'NONE',  ( 1.780377099649257167, -51.29164421682789765, -48.57534666485256025 ) ) ;
#50167=DIRECTION ( 'NONE',  ( 0.000000000000000000, 0.000000000000000000, -1.000000000000000000 ) ) ;
#50177=CARTESIAN_POINT ( 'NONE',  ( -2.219371606100929206, 51.37365828841677740, -48.60677221569366679 ) ) ;
#50185=ORIENTED_EDGE ( 'NONE', *, *, #70525, .T. ) ;
#50310=CARTESIAN_POINT ( 'NONE',  ( -5.000000000000000000, 63.46149047932892984, 24.14127879314137815 ) ) ;
#50319=CARTESIAN_POINT ( 'NONE',  ( -5.000000000000000000, 52.63864145287860197, 42.88977517748130452 ) ) ;
#50326=CARTESIAN_POINT ( 'NONE',  ( -0.6474643998436649950, -10.28110762191874805, -63.57179091896463063 ) ) ;
#50344=CARTESIAN_POINT ( 'NONE',  ( -5.000000000000000888, 11.44657803507906024, -68.01244171956641082 ) ) ;
#50370=ORIENTED_EDGE ( 'NONE', *, *, #34293, .T. ) ;
#50375=CARTESIAN_POINT ( 'NONE',  ( 5.000000000000000000, 0.000000000000000000, 0.000000000000000000 ) ) ;
#50389=CARTESIAN_POINT ( 'NONE',  ( 5.000000000000000000, 53.21762015693931147, -47.70201125340150838 ) ) ;
#50403=CARTESIAN_POINT ( 'NONE',  ( -2.436599634630704614, -67.82108862182700193, -20.21956363439016258 ) ) ;
#50444=CARTESIAN_POINT ( 'NONE',  ( 5.000000000000000888, -51.74377041917559694, 41.86884046506250456 ) ) ;
#50465=ADVANCED_FACE ( 'NONE', ( #53705 ), #42442, .T. ) ;
#50514=EDGE_LOOP ( 'NONE', ( #14179, #14882, #53186, #4944, #27367 ) ) ;
#50515=DIRECTION ( 'NONE',  ( 0.000000000000000000, 0.02418647091589873691, -0.9997074645238147594 ) ) ;
#50539=CYLINDRICAL_SURFACE ( 'NONE', #460, 5.000000000000000888 ) ;
#50545=CARTESIAN_POINT ( 'NONE',  ( 5.126106709302933773, 52.42424824936820471, -49.01286957842418701 ) ) ;
#50557=CIRCLE ( 'NONE', #38511, 70.50000000000000000 ) ;
#50566=ORIENTED_EDGE ( 'NONE', *, *, #18926, .T. ) ;
#50609=CARTESIAN_POINT ( 'NONE',  ( -4.193030820683908644, 10.26769724739506984, 64.12608639927678666 ) ) ;
#50626=CARTESIAN_POINT ( 'NONE',  ( 5.000000000000000000, 52.16438407847101644, 42.28020805311251706 ) ) ;
#50633=CARTESIAN_POINT ( 'NONE',  ( 5.000000000000000000, 10.38759426015435139, 65.74583990312709147 ) ) ;
#50675=EDGE_CURVE ( 'NONE', #17960, #2769, #67628, .T. ) ;
#50694=CARTESIAN_POINT ( 'NONE',  ( -0.8588954341814977189, 10.28066745654381720, -63.58998442112849858 ) ) ;
#50709=CARTESIAN_POINT ( 'NONE',  ( -0.4320110153365220862, -49.91454558245964535, -40.68976686129133213 ) ) ;
#50769=CARTESIAN_POINT ( 'NONE',  ( -0.7581620860329574274, 55.63814191977067480, 43.81219805000592515 ) ) ;
#50771=CARTESIAN_POINT ( 'NONE',  ( 5.086519500889780332, -60.91611154180146315, -23.32191296475813758 ) ) ;
#50776=CARTESIAN_POINT ( 'NONE',  ( 5.000000000000000000, -53.18690467503068220, -43.91652490638241346 ) ) ;
#50778=CARTESIAN_POINT ( 'NONE',  ( -4.999999999999999112, -15.48016642534408405, -69.96422921944751749 ) ) ;
#50797=FACE_OUTER_BOUND ( 'NONE', #24355, .T. ) ;
#50820=CARTESIAN_POINT ( 'NONE',  ( -5.000000000000000000, -16.24494643555759410, 69.83755725260752456 ) ) ;
#50871=EDGE_CURVE ( 'NONE', #38797, #70301, #5006, .T. ) ;
#50884=CARTESIAN_POINT ( 'NONE',  ( 0.6474643998346684137, -49.91423208894351404, -40.68959583910973521 ) ) ;
#50896=CARTESIAN_POINT ( 'NONE',  ( 3.223881452105103573, 10.27322224982961529, 63.89771963198208482 ) ) ;
#50907=FACE_OUTER_BOUND ( 'NONE', #20776, .T. ) ;
#50915=CARTESIAN_POINT ( 'NONE',  ( 5.000000000000000000, -68.60357193678713372, 20.85024232999320404 ) ) ;
#50922=CARTESIAN_POINT ( 'NONE',  ( -6.308070865140195771, 51.03903544636535372, -41.30321721933843548 ) ) ;
#50932=ORIENTED_EDGE ( 'NONE', *, *, #44247, .T. ) ;
#50993=EDGE_CURVE ( 'NONE', #21755, #60656, #48114, .T. ) ;
#50999=CARTESIAN_POINT ( 'NONE',  ( -4.999999999999998224, 52.84634075987170831, -43.22150062466479170 ) ) ;
#51001=CARTESIAN_POINT ( 'NONE',  ( 1.317228840344650820, -65.80815776305074394, 26.30638062134261190 ) ) ;
#51024=CARTESIAN_POINT ( 'NONE',  ( -5.000000000000000000, -60.90295814858238543, -23.31388853594834032 ) ) ;
#51054=CARTESIAN_POINT ( 'NONE',  ( -6.298842414732763295, -61.32333038069151598, 23.57034304878679976 ) ) ;
#51074=CARTESIAN_POINT ( 'NONE',  ( 4.471435261903841329, -10.26549131683148985, -64.21726486257124122 ) ) ;
#51082=CARTESIAN_POINT ( 'NONE',  ( 1.704527592502775635, -49.99193291617169876, 40.73198448289673479 ) ) ;
#51084=ORIENTED_EDGE ( 'NONE', *, *, #48693, .T. ) ;
#51168=CARTESIAN_POINT ( 'NONE',  ( -0.7509181236817221716, -55.63764137817485533, 43.81192498625236453 ) ) ;
#51228=CARTESIAN_POINT ( 'NONE',  ( 4.999999999999999112, -66.11467145570902915, 23.67355326543016858 ) ) ;
#51295=ORIENTED_EDGE ( 'NONE', *, *, #62415, .F. ) ;
#51323=ORIENTED_EDGE ( 'NONE', *, *, #48597, .T. ) ;
#51332=B_SPLINE_CURVE_WITH_KNOTS ( 'NONE', 3,
 ( #59927, #8241, #31631, #4089, #32765, #54651, #67080, #60671, #55399, #31252, #44071, #43310 ),
 .UNSPECIFIED., .F., .F.,
 ( 4, 2, 2, 2, 2, 4 ),
 ( 0.000000000000000000, 0.002547658444427994794, 0.005095316888855989587, 0.006369146111069987418, 0.007642975333283985248, 0.01019063377771197744 ),
 .UNSPECIFIED. ) ;
#51358=LINE ( 'NONE', #63417, #5749 ) ;
#51365=CARTESIAN_POINT ( 'NONE',  ( 2.170320029194602984, 67.76782500014425636, -20.17643218080212719 ) ) ;
#51374=CARTESIAN_POINT ( 'NONE',  ( 4.999999999999999112, 53.39837237779229184, 47.14918772354995724 ) ) ;
#51387=( BOUNDED_SURFACE ( )  B_SPLINE_SURFACE ( 3, 2, ( 
 ( #34476, #57853, #33728 ),
 ( #56730, #28044, #17461 ),
 ( #40482, #39734, #51054 ),
 ( #62734, #34102, #51424 ),
 ( #45765, #5788, #51800 ),
 ( #11809, #34848, #9902 ),
 ( #38946, #16278, #22313 ),
 ( #68356, #27994, #45709 ),
 ( #4616, #34053, #67983 ),
 ( #45339, #62318, #44978 ),
 ( #74012, #44235, #16651 ),
 ( #32932, #51001, #61946 ),
 ( #39683, #10275, #55938 ),
 ( #61583, #39320, #3875 ),
 ( #5360, #10644, #40059 ),
 ( #21578, #17033, #22691 ),
 ( #33673, #56677, #73642 ),
 ( #4249, #62683, #4994 ) ),
 .UNSPECIFIED., .F., .F., .F. ) 
 B_SPLINE_SURFACE_WITH_KNOTS ( ( 4, 2, 2, 2, 2, 2, 2, 2, 4 ),
 ( 3, 3 ),
 ( 0.04202945594032910653, 0.04396162471216781553, 0.04589379348400653147, 0.04782596225584524741, 0.04975813102768396334, 0.05169029979952267928, 0.05265638418544203725, 0.05362246857136138828, 0.05748680611503881321 ),
 ( 0.000000000000000000, 1.000000000000000000 ),
 .UNSPECIFIED. ) 
 GEOMETRIC_REPRESENTATION_ITEM ( )  RATIONAL_B_SPLINE_SURFACE ( (
 ( 1.000000000000000000, 0.6241276099608162875, 1.000000000000000000),
 ( 1.000000000000000000, 0.6218761496800390143, 1.000000000000000000),
 ( 1.000000000000000000, 0.6198047272364022309, 1.000000000000000000),
 ( 1.000000000000000000, 0.6161935119824402118, 1.000000000000000000),
 ( 1.000000000000000000, 0.6146642324079480968, 1.000000000000000000),
 ( 1.000000000000000000, 0.6121850116872522563, 1.000000000000000000),
 ( 1.000000000000000000, 0.6112350889399755793, 1.000000000000000000),
 ( 1.000000000000000000, 0.6099522725972823523, 1.000000000000000000),
 ( 1.000000000000000000, 0.6096208180307279845, 1.000000000000000000),
 ( 1.000000000000000000, 0.6096183796350086448, 1.000000000000000000),
 ( 1.000000000000000000, 0.6099422200101831670, 1.000000000000000000),
 ( 1.000000000000000000, 0.6109087447823332573, 1.000000000000000000),
 ( 1.000000000000000000, 0.6113123981688617370, 1.000000000000000000),
 ( 1.000000000000000000, 0.6122677719808993224, 1.000000000000000000),
 ( 1.000000000000000000, 0.6128199619020365807, 1.000000000000000000),
 ( 1.000000000000000000, 0.6159350830268174315, 1.000000000000000000),
 ( 1.000000000000000000, 0.6195556778513785501, 1.000000000000000000),
 ( 1.000000000000000000, 0.6241278272307889674, 1.000000000000000000) ) ) 
 REPRESENTATION_ITEM ( '' )  SURFACE ( )  );
#51401=CARTESIAN_POINT ( 'NONE',  ( -5.000000000000000000, -18.53862685874495853, -23.57305537018139674 ) ) ;
#51410=EDGE_CURVE ( 'NONE', #69045, #53254, #40265, .T. ) ;
#51424=CARTESIAN_POINT ( 'NONE',  ( -5.086519500887583867, -60.91611154180644405, 23.32191296476066356 ) ) ;
#51433=DIRECTION ( 'NONE',  ( 1.000000000000000000, 0.000000000000000000, 0.000000000000000000 ) ) ;
#51443=CARTESIAN_POINT ( 'NONE',  ( -2.124081043562908722, 10.27770035960974759, -63.71262442773669932 ) ) ;
#51454=CARTESIAN_POINT ( 'NONE',  ( 3.369429374625377172, -50.21921270641806956, -40.85597392306833342 ) ) ;
#51498=EDGE_CURVE ( 'NONE', #13141, #10343, #42587, .T. ) ;
#51515=CARTESIAN_POINT ( 'NONE',  ( 0.4451317748862709811, 51.14719335908506537, 48.52010116548684238 ) ) ;
#51529=CARTESIAN_POINT ( 'NONE',  ( -0.4320110153365229189, -60.19564456717424150, 22.88238106212085654 ) ) ;
#51531=APPLICATION_CONTEXT ( 'automotive_design' ) ;
#51537=CARTESIAN_POINT ( 'NONE',  ( -1.308779242310801116, 60.23127520339139807, -22.90411807697349289 ) ) ;
#51549=CARTESIAN_POINT ( 'NONE',  ( 5.000000000000000888, -14.70421557449305361, 69.92631206022691970 ) ) ;
#51567=EDGE_CURVE ( 'NONE', #17054, #34668, #28186, .T. ) ;
#51597=CARTESIAN_POINT ( 'NONE',  ( 0.4368895104448404787, 16.44602605510734605, -68.55492853905226980 ) ) ;
#51598=CARTESIAN_POINT ( 'NONE',  ( -13.99999999999999822, 0.000000000000000000, 0.000000000000000000 ) ) ;
#51600=CARTESIAN_POINT ( 'NONE',  ( 5.000000000000000000, 52.35862550122891435, 48.98731492261470777 ) ) ;
#51614=CARTESIAN_POINT ( 'NONE',  ( 5.000000000000000000, 60.90295814858223622, 23.31388853594876664 ) ) ;
#51620=CYLINDRICAL_SURFACE ( 'NONE', #3159, 17.50000000000000000 ) ;
#51647=CARTESIAN_POINT ( 'NONE',  ( -1.506524674528488372, 10.12152537343924941, 70.16785718945649819 ) ) ;
#51723=CARTESIAN_POINT ( 'NONE',  ( -0.4369882809986812555, 51.14729664189420077, 48.52014062455138088 ) ) ;
#51724=CARTESIAN_POINT ( 'NONE',  ( 13.99999999999999822, 0.000000000000000000, 0.000000000000000000 ) ) ;
#51743=CARTESIAN_POINT ( 'NONE',  ( -5.000000000000000000, 53.50771145605737189, -45.03482491321273073 ) ) ;
#51749=CARTESIAN_POINT ( 'NONE',  ( 5.000000000000000888, 53.20585484986760605, 47.69738026034786316 ) ) ;
#51757=CARTESIAN_POINT ( 'NONE',  ( 5.000000000000000000, 10.26105934116143281, 64.40045319026697257 ) ) ;
#51800=CARTESIAN_POINT ( 'NONE',  ( -4.471435261917410919, -60.74652839096143708, 23.21845616858397676 ) ) ;
#51831=CARTESIAN_POINT ( 'NONE',  ( -4.193030820682222881, -50.40097124335162704, 40.95512985424973351 ) ) ;
#51861=CIRCLE ( 'NONE', #19298, 71.70204102886728492 ) ;
#51886=CARTESIAN_POINT ( 'NONE',  ( 0.4320110153364595806, -10.28109898471437589, -63.57214792341208920 ) ) ;
#51912=CARTESIAN_POINT ( 'NONE',  ( 5.000000000000000000, -60.90295814858255596, 23.31388853594792110 ) ) ;
#51916=CARTESIAN_POINT ( 'NONE',  ( 5.000000000000000000, -68.60357193678697740, -20.85024232999374050 ) ) ;
#51921=CARTESIAN_POINT ( 'NONE',  ( 0.4451317748864607737, 67.59323688304490929, -20.03471819849965030 ) ) ;
#51934=CARTESIAN_POINT ( 'NONE',  ( 5.000000000000000000, -14.13320814749868326, 69.81894086168452418 ) ) ;
#51944=ORIENTED_EDGE ( 'NONE', *, *, #34293, .F. ) ;
#51964=CARTESIAN_POINT ( 'NONE',  ( -2.995737153982818146, -51.55860531535488178, -48.67776149471355041 ) ) ;
#51979=CIRCLE ( 'NONE', #53165, 92.50000000000000000 ) ;
#51982=CARTESIAN_POINT ( 'NONE',  ( -5.000000000000000000, -10.38759426015435139, 65.74583990312709147 ) ) ;
#52033=VECTOR ( 'NONE', #65294, 1000.000000000000000 ) ;
#52040=CARTESIAN_POINT ( 'NONE',  ( -1.317228840344501606, 65.80815776305036024, 26.30638062134577382 ) ) ;
#52056=CIRCLE ( 'NONE', #2665, 70.50000000000000000 ) ;
#52077=EDGE_CURVE ( 'NONE', #38888, #47939, #29963, .T. ) ;
#52128=CARTESIAN_POINT ( 'NONE',  ( -4.999999999999953815, -52.35862550122923409, -48.98731492261434539 ) ) ;
#52181=ORIENTED_EDGE ( 'NONE', *, *, #48999, .T. ) ;
#52183=CARTESIAN_POINT ( 'NONE',  ( 3.511653767259352410, -16.35475815726353233, 69.12977678000895310 ) ) ;
#52268=PLANE ( 'NONE',  #24120 ) ;
#52279=CARTESIAN_POINT ( 'NONE',  ( 4.999999999999999112, -53.50771145605675372, -45.03482491321348391 ) ) ;
#52282=CARTESIAN_POINT ( 'NONE',  ( 5.000000000000000000, -52.35862550122924830, -48.98731492261435250 ) ) ;
#52285=CARTESIAN_POINT ( 'NONE',  ( -14.00000000000000178, 2.249999999994893862, 10.23492587299426404 ) ) ;
#52295=CARTESIAN_POINT ( 'NONE',  ( -2.990854866097343745, 66.07503719301357137, -26.46919450145105301 ) ) ;
#52297=LINE ( 'NONE', #39486, #31061 ) ;
#52335=VERTEX_POINT ( 'NONE', #20106 ) ;
#52353=CARTESIAN_POINT ( 'NONE',  ( -5.000000000000000000, -11.82742353449332917, 68.45184936927694253 ) ) ;
#52354=CARTESIAN_POINT ( 'NONE',  ( 1.739508062058411131, 51.27839935804142613, 48.57027215863440262 ) ) ;
#52398=CARTESIAN_POINT ( 'NONE',  ( -2.219371606097579441, 16.40787039054625396, 68.79427927095593986 ) ) ;
#52419=CARTESIAN_POINT ( 'NONE',  ( 13.99999999999999822, -2.250000000005106138, 7.677076266390546522 ) ) ;
#52441=CARTESIAN_POINT ( 'NONE',  ( -3.496982156820191978, 16.35094707925454216, -69.15443034747076467 ) ) ;
#52474=CARTESIAN_POINT ( 'NONE',  ( -2.995737153994215252, 51.55860531535790869, 48.67776149471519886 ) ) ;
#52495=DIRECTION ( 'NONE',  ( 1.000000000000000000, 0.000000000000000000, 0.000000000000000000 ) ) ;
#52558=CARTESIAN_POINT ( 'NONE',  ( -14.00000000000000178, 2.249999999994893862, 10.23492587299426404 ) ) ;
#52576=CARTESIAN_POINT ( 'NONE',  ( 4.193070328474941100, -50.40098303874172103, 40.95513628906654446 ) ) ;
#52582=CARTESIAN_POINT ( 'NONE',  ( -5.000000000000000000, -32.28817737728140003, -1.075528555105620399E-13 ) ) ;
#52585=EDGE_CURVE ( 'NONE', #37723, #53254, #72267, .T. ) ;
#52591=ORIENTED_EDGE ( 'NONE', *, *, #3124, .T. ) ;
#52629=DIRECTION ( 'NONE',  ( 1.000000000000000000, -0.000000000000000000, 0.000000000000000000 ) ) ;
#52630=CARTESIAN_POINT ( 'NONE',  ( 4.193070328474939323, -10.26769692241485998, -64.12609983179218887 ) ) ;
#52634=CARTESIAN_POINT ( 'NONE',  ( 0.8419854211626194296, -10.28111362163632769, 63.57154293063803152 ) ) ;
#52640=CARTESIAN_POINT ( 'NONE',  ( 5.000000000000000000, 11.14555136602165142, 27.84144949604463193 ) ) ;
#52654=EDGE_CURVE ( 'NONE', #37917, #69045, #11409, .T. ) ;
#52659=CARTESIAN_POINT ( 'NONE',  ( 5.000000000000000000, -67.91996363552661364, -22.23680535815918446 ) ) ;
#52663=CARTESIAN_POINT ( 'NONE',  ( -2.266287154886550415, -50.05783744175262484, 40.76793781259078031 ) ) ;
#52673=ORIENTED_EDGE ( 'NONE', *, *, #58852, .F. ) ;
#52706=CARTESIAN_POINT ( 'NONE',  ( -0.8761883848702536337, -51.17400877215151667, -48.53033992007411968 ) ) ;
#52737=CARTESIAN_POINT ( 'NONE',  ( -0.8419854211626145446, 60.19512794652348475, 22.88206588978842504 ) ) ;
#52809=CARTESIAN_POINT ( 'NONE',  ( 0.7509181236784587821, 10.12341933770226277, -70.08957333326497974 ) ) ;
#52823=CIRCLE ( 'NONE', #60021, 10.99999999999999645 ) ;
#52846=ORIENTED_EDGE ( 'NONE', *, *, #33893, .T. ) ;
#52857=EDGE_CURVE ( 'NONE', #3120, #4298, #17342, .T. ) ;
#52864=ORIENTED_EDGE ( 'NONE', *, *, #15774, .F. ) ;
#52876=EDGE_CURVE ( 'NONE', #21239, #45651, #30845, .T. ) ;
#52880=UNCERTAINTY_MEASURE_WITH_UNIT (LENGTH_MEASURE( 1.000000000000000082E-05 ), #11761, 'distance_accuracy_value', 'NONE');
#52884=ORIENTED_EDGE ( 'NONE', *, *, #48891, .F. ) ;
#52915=EDGE_CURVE ( 'NONE', #7738, #1129, #46681, .T. ) ;
#52945=LINE ( 'NONE', #1275, #60433 ) ;
#53016=B_SPLINE_CURVE_WITH_KNOTS ( 'NONE', 3,
 ( #22394, #51831, #16734, #74464, #40513, #23525, #68431, #51082, #39760, #69183, #52576, #12202 ),
 .UNSPECIFIED., .F., .F.,
 ( 4, 2, 2, 2, 2, 4 ),
 ( 0.000000000000000000, 0.002547658444427995227, 0.005095316888855990455, 0.006369146111069988285, 0.007642975333283986983, 0.01019063377771197917 ),
 .UNSPECIFIED. ) ;
#53019=CARTESIAN_POINT ( 'NONE',  ( -0.4369882810000410012, -67.59332269700179552, 20.03478791450388030 ) ) ;
#53024=CARTESIAN_POINT ( 'NONE',  ( -4.231687259407056700, -51.96503165405702873, 48.83411696341828190 ) ) ;
#53031=CIRCLE ( 'NONE', #42126, 92.50000000000000000 ) ;
#53035=CARTESIAN_POINT ( 'NONE',  ( 1.780377099649100181, 67.71330631781181353, -20.13219356122023385 ) ) ;
#53086=CARTESIAN_POINT ( 'NONE',  ( -5.000000000000000888, 12.55543720214795478, 69.09376167622116327 ) ) ;
#53102=B_SPLINE_CURVE_WITH_KNOTS ( 'NONE', 3,
 ( #17029, #10640, #11016, #4990, #51365, #63799, #22687, #40055 ),
 .UNSPECIFIED., .F., .F.,
 ( 4, 2, 2, 4 ),
 ( 0.005256334970462575411, 0.006570121696640842182, 0.007883908422819108086, 0.01051148187517563469 ),
 .UNSPECIFIED. ) ;
#53152=CARTESIAN_POINT ( 'NONE',  ( 2.620431783929131786, 65.99617417813951192, 26.42108291244571561 ) ) ;
#53165=AXIS2_PLACEMENT_3D ( 'NONE', #19321, #46893, #69917 ) ;
#53182=CARTESIAN_POINT ( 'NONE',  ( 2.069125466538726865, 10.11940336925073503, -70.25556669587955128 ) ) ;
#53186=ORIENTED_EDGE ( 'NONE', *, *, #17273, .F. ) ;
#53249=CARTESIAN_POINT ( 'NONE',  ( 4.999999999999999112, 14.31098243164692008, 69.87317657433686691 ) ) ;
#53254=VERTEX_POINT ( 'NONE', #20596 ) ;
#53289=ORIENTED_EDGE ( 'NONE', *, *, #3124, .F. ) ;
#53295=CARTESIAN_POINT ( 'NONE',  ( -5.000000000000000000, -60.11723469343116477, 46.25570701698070764 ) ) ;
#53301=EDGE_CURVE ( 'NONE', #4298, #3, #35840, .T. ) ;
#53358=VERTEX_POINT ( 'NONE', #48249 ) ;
#53366=ORIENTED_EDGE ( 'NONE', *, *, #52585, .F. ) ;
#53408=CARTESIAN_POINT ( 'NONE',  ( 5.126144196591289059, 68.65853088339399335, -20.89430926782988962 ) ) ;
#53441=DIRECTION ( 'NONE',  ( 0.000000000000000000, 0.000000000000000000, -1.000000000000000000 ) ) ;
#53493=CARTESIAN_POINT ( 'NONE',  ( -4.999999999999944045, 68.60357193678724741, -20.85024232999276350 ) ) ;
#53499=CARTESIAN_POINT ( 'NONE',  ( -5.000000000000000000, -53.12474899268202222, 47.87640533067842341 ) ) ;
#53564=CARTESIAN_POINT ( 'NONE',  ( -5.000000000000000000, 70.11723469343132820, -28.93519894129142145 ) ) ;
#53605=EDGE_LOOP ( 'NONE', ( #73473, #62074, #68932, #16976, #45808, #25097, #59573, #46349, #11976, #53746, #11120, #57373, #17632, #19349, #69682, #59491 ) ) ;
#53617=B_SPLINE_CURVE_WITH_KNOTS ( 'NONE', 3,
 ( #13944, #36986, #31318, #42265, #72433, #23902, #65277, #54345, #19621 ),
 .UNSPECIFIED., .F., .F.,
 ( 4, 2, 1, 2, 4 ),
 ( 0.000000000000000000, 0.001314083742622694853, 0.002628167485245389706, 0.003942251227868084559, 0.005256334970490779412 ),
 .UNSPECIFIED. ) ;
#53687=AXIS2_PLACEMENT_3D ( 'NONE', #56429, #60963, #32686 ) ;
#53705=FACE_OUTER_BOUND ( 'NONE', #44835, .T. ) ;
#53720=EDGE_CURVE ( 'NONE', #2769, #44073, #42463, .T. ) ;
#53746=ORIENTED_EDGE ( 'NONE', *, *, #55931, .F. ) ;
#53748=CARTESIAN_POINT ( 'NONE',  ( 5.107860025164002948, 50.62490018645832635, 41.07729128472288949 ) ) ;
#53749=CARTESIAN_POINT ( 'NONE',  ( -5.000000000000000000, 60.90295814858271939, -23.31388853594749833 ) ) ;
#53756=FACE_OUTER_BOUND ( 'NONE', #25140, .T. ) ;
#53826=CARTESIAN_POINT ( 'NONE',  ( 5.000000000000000000, 16.24494643555759410, -69.83755725260752456 ) ) ;
#53843=ORIENTED_EDGE ( 'NONE', *, *, #36921, .F. ) ;
#53877=CARTESIAN_POINT ( 'NONE',  ( -4.231687259407056700, 16.30907003467247307, 69.42009600258496960 ) ) ;
#53889=CARTESIAN_POINT ( 'NONE',  ( -7.456209740496419158, 61.82228229130262775, 23.87473629694281030 ) ) ;
#53891=CARTESIAN_POINT ( 'NONE',  ( 5.000000000000000000, 60.90295814858223622, 23.31388853594876664 ) ) ;
#53910=VERTEX_POINT ( 'NONE', #25151 ) ;
#53911=CARTESIAN_POINT ( 'NONE',  ( 5.000000000000000000, 70.11723469343132820, -28.93519894129142145 ) ) ;
#53934=CARTESIAN_POINT ( 'NONE',  ( 5.000000000000000000, -10.26105934116143459, 64.40045319026695836 ) ) ;
#53948=CARTESIAN_POINT ( 'NONE',  ( 0.4369882809721246097, 16.44602605510714355, 68.55492853905350614 ) ) ;
#53959=DIRECTION ( 'NONE',  ( 1.000000000000000000, -0.000000000000000000, 0.000000000000000000 ) ) ;
#53973=CARTESIAN_POINT ( 'NONE',  ( -3.018451720292563716E-14, -16.44602605510714355, -68.55492853905353456 ) ) ;
#53984=CARTESIAN_POINT ( 'NONE',  ( -5.000000000000000000, -10.26105934116142215, -64.40045319026754100 ) ) ;
#54040=LINE ( 'NONE', #42700, #66987 ) ;
#54043=ORIENTED_EDGE ( 'NONE', *, *, #26302, .T. ) ;
#54072=CARTESIAN_POINT ( 'NONE',  ( 6.891449706525156316, 51.31760009878723139, -41.45518442798378800 ) ) ;
#54136=EDGE_CURVE ( 'NONE', #67442, #18291, #12787, .T. ) ;
#54198=CARTESIAN_POINT ( 'NONE',  ( 5.000000000000000888, 12.55543720214775583, -69.09376167622102116 ) ) ;
#54232=EDGE_CURVE ( 'NONE', #74324, #41307, #68506, .T. ) ;
#54269=CARTESIAN_POINT ( 'NONE',  ( -5.000000000000000000, 50.64189880742059557, 41.08656465431948845 ) ) ;
#54291=CARTESIAN_POINT ( 'NONE',  ( 4.999999999999999112, -14.31098243164691652, -69.87317657433686691 ) ) ;
#54298=CARTESIAN_POINT ( 'NONE',  ( 1.704527592502767863, 49.99193291617198298, -40.73198448289638662 ) ) ;
#54300=ORIENTED_EDGE ( 'NONE', *, *, #46837, .F. ) ;
#54301=EDGE_CURVE ( 'NONE', #28093, #32715, #58325, .T. ) ;
#54322=DIRECTION ( 'NONE',  ( 0.000000000000000000, -0.000000000000000000, -1.000000000000000000 ) ) ;
#54345=CARTESIAN_POINT ( 'NONE',  ( 0.4369882809721256645, -67.59332269700064444, -20.03478791450352503 ) ) ;
#54364=ADVANCED_BREP_SHAPE_REPRESENTATION ( '', ( #17160, #57354 ), #64563 ) ;
#54388=CARTESIAN_POINT ( 'NONE',  ( 5.000000000000000000, -16.14408868864072844, 27.96238185062368586 ) ) ;
#54428=CARTESIAN_POINT ( 'NONE',  ( 5.000000000000000000, 60.90295814858223622, 23.31388853594876664 ) ) ;
#54436=CARTESIAN_POINT ( 'NONE',  ( 5.000000000000000000, -68.60357193678697740, -20.85024232999374050 ) ) ;
#54449=CARTESIAN_POINT ( 'NONE',  ( -3.728321214210839063, 56.13798660966043741, -44.08488161416902784 ) ) ;
#54485=ORIENTED_EDGE ( 'NONE', *, *, #48477, .T. ) ;
#54497=AXIS2_PLACEMENT_3D ( 'NONE', #19599, #49776, #61090 ) ;
#54521=CARTESIAN_POINT ( 'NONE',  ( 3.544144923083450749, 60.54353712382587105, -23.09461823984437956 ) ) ;
#54550=CARTESIAN_POINT ( 'NONE',  ( -4.217983994794429314, 68.29231466825656582, -20.60018752343895088 ) ) ;
#54583=CARTESIAN_POINT ( 'NONE',  ( 5.000000000000000000, 60.11723469343052528, 46.25570701698154608 ) ) ;
#54590=CARTESIAN_POINT ( 'NONE',  ( -5.000000000000000000, 10.26105934116142215, 64.40045319026754100 ) ) ;
#54592=VERTEX_POINT ( 'NONE', #13004 ) ;
#54613=CARTESIAN_POINT ( 'NONE',  ( -5.000000000000000000, 29.68417822476651580, 4.268394125863326671 ) ) ;
#54640=CARTESIAN_POINT ( 'NONE',  ( 5.000000000000000000, 67.66743717231469191, 22.54291394825019168 ) ) ;
#54651=CARTESIAN_POINT ( 'NONE',  ( -0.4320110153365262495, 60.19564456717440493, -22.88238106212044087 ) ) ;
#54703=ADVANCED_FACE ( 'NONE', ( #32998 ), #15236, .T. ) ;
#54710=DIRECTION ( 'NONE',  ( 0.000000000000000000, 0.8536788251726021848, 0.5207998305029730712 ) ) ;
#54788=DIRECTION ( 'NONE',  ( 1.000000000000000000, -0.000000000000000000, -0.000000000000000000 ) ) ;
#54900=CARTESIAN_POINT ( 'NONE',  ( -4.999999999999998224, -64.42874436516127901, 24.11656705754152341 ) ) ;
#54912=EDGE_CURVE ( 'NONE', #63044, #17271, #65021, .T. ) ;
#55016=CARTESIAN_POINT ( 'NONE',  ( 3.373128826976384165, -60.49298623944814324, -23.06377889928852554 ) ) ;
#55038=CARTESIAN_POINT ( 'NONE',  ( 5.000000000000000000, -10.25159769123455256, -64.79153472057839735 ) ) ;
#55042=CARTESIAN_POINT ( 'NONE',  ( 0.8761883848702568534, -51.17400877215189325, 48.53033992007376440 ) ) ;
#55067=CARTESIAN_POINT ( 'NONE',  ( 4.336811714529654083, -52.00708776950327916, -48.85034107298358208 ) ) ;
#55105=EDGE_CURVE ( 'NONE', #53358, #24578, #53102, .T. ) ;
#55118=ORIENTED_EDGE ( 'NONE', *, *, #20866, .F. ) ;
#55139=VERTEX_POINT ( 'NONE', #40426 ) ;
#55244=CARTESIAN_POINT ( 'NONE',  ( -2.990854866088966002, -10.11452374054218240, 70.45725801587769865 ) ) ;
#55255=CARTESIAN_POINT ( 'NONE',  ( -5.000000000000000000, 53.17721328501306033, 43.91924822456324762 ) ) ;
#55283=CARTESIAN_POINT ( 'NONE',  ( -4.999999999999999112, 13.22058908515350062, -69.49198671174478648 ) ) ;
#55305=ORIENTED_EDGE ( 'NONE', *, *, #743, .F. ) ;
#55336=CARTESIAN_POINT ( 'NONE',  ( 6.298842414730434491, -61.32333038069613451, -23.57034304879013575 ) ) ;
#55348=ORIENTED_EDGE ( 'NONE', *, *, #9152, .T. ) ;
#55358=CARTESIAN_POINT ( 'NONE',  ( 3.223881452091941213, -50.20043732027839667, 40.84573126306743518 ) ) ;
#55389=CARTESIAN_POINT ( 'NONE',  ( -1.688721909672324495, -60.25432409644719201, -22.91817940688312660 ) ) ;
#55390=CARTESIAN_POINT ( 'NONE',  ( 5.000000000000000888, 66.79212039439808279, 23.29662735513495164 ) ) ;
#55399=CARTESIAN_POINT ( 'NONE',  ( -2.124081043562903837, 60.31560147600205113, -22.95556260996129794 ) ) ;
#55411=ORIENTED_EDGE ( 'NONE', *, *, #3142, .T. ) ;
#55441=CARTESIAN_POINT ( 'NONE',  ( -1.781595147096349363, -51.28498669165043111, -48.57279346520105179 ) ) ;
#55560=CYLINDRICAL_SURFACE ( 'NONE', #73906, 5.000000000000000888 ) ;
#55614=ORIENTED_EDGE ( 'NONE', *, *, #49615, .F. ) ;
#55616=CARTESIAN_POINT ( 'NONE',  ( -4.737866951552680561, -16.26762833211037318, 69.68949229522927169 ) ) ;
#55627=DIRECTION ( 'NONE',  ( 0.000000000000000000, 0.000000000000000000, -1.000000000000000000 ) ) ;
#55628=CARTESIAN_POINT ( 'NONE',  ( -4.999999999999999112, 51.30314553820166168, 41.49361401976570107 ) ) ;
#55637=CARTESIAN_POINT ( 'NONE',  ( 4.737866951551791495, -16.26762833211076043, -69.68949229522870326 ) ) ;
#55650=CARTESIAN_POINT ( 'NONE',  ( -5.000000000000000000, -68.48952624890536356, 21.22548696402875734 ) ) ;
#55657=CARTESIAN_POINT ( 'NONE',  ( -5.000000000000000000, 11.32881245867859121, -67.85521288293392672 ) ) ;
#55708=VECTOR ( 'NONE', #73100, 1000.000000000000000 ) ;
#55712=CARTESIAN_POINT ( 'NONE',  ( 2.591411123064221389, -60.37037679142930102, -22.98897912932425314 ) ) ;
#55732=CARTESIAN_POINT ( 'NONE',  ( 1.781595147087996267, -51.28498669164731183, 48.57279346520238761 ) ) ;
#55756=CARTESIAN_POINT ( 'NONE',  ( 5.000000000000000000, -53.57153130924498896, 46.19535935661046011 ) ) ;
#55818=CARTESIAN_POINT ( 'NONE',  ( 0.8912353796322691757, -51.17464048783892139, -48.53058040617464286 ) ) ;
#55850=FACE_OUTER_BOUND ( 'NONE', #73962, .T. ) ;
#55856=CARTESIAN_POINT ( 'NONE',  ( 2.620431783921520541, 55.87941608673474292, -43.94382193462354991 ) ) ;
#55931=EDGE_CURVE ( 'NONE', #15493, #16375, #48160, .T. ) ;
#55938=CARTESIAN_POINT ( 'NONE',  ( 2.589639417652957132, -60.37884160280833612, 22.99414321703618924 ) ) ;
#55940=CARTESIAN_POINT ( 'NONE',  ( 4.999999999999998224, 53.32026166094831154, 44.27875806162001027 ) ) ;
#55942=CIRCLE ( 'NONE', #13714, 17.50000000000000000 ) ;
#55999=CARTESIAN_POINT ( 'NONE',  ( -5.000000000000000888, 53.09993190648213357, 43.73864582539290780 ) ) ;
#56005=AXIS2_PLACEMENT_3D ( 'NONE', #31769, #54788, #24609 ) ;
#56008=CARTESIAN_POINT ( 'NONE',  ( -6.308070865131614191, -10.25011764679139503, -64.85270989089528371 ) ) ;
#56022=CARTESIAN_POINT ( 'NONE',  ( -5.000000000000000000, -67.10422270468713180, 23.07049055144742766 ) ) ;
#56068=CARTESIAN_POINT ( 'NONE',  ( 5.000000000000000000, 53.35645474066845395, -47.33026262608697010 ) ) ;
#56081=CARTESIAN_POINT ( 'NONE',  ( 4.465349678524231258, -66.51625814178485996, -26.73836809291886496 ) ) ;
#56128=CARTESIAN_POINT ( 'NONE',  ( 5.000000000000000888, -53.36732872257306326, 44.46877392682749530 ) ) ;
#56150=ORIENTED_EDGE ( 'NONE', *, *, #47948, .F. ) ;
#56162=SHAPE_DEFINITION_REPRESENTATION ( #16795, #5031 ) ;
#56189=CARTESIAN_POINT ( 'NONE',  ( -0.3794862803193519429, -55.62190996747714422, -43.80334292620955949 ) ) ;
#56207=CARTESIAN_POINT ( 'NONE',  ( 0.000000000000000000, 9.980871413050930352E-15, 81.50000000000000000 ) ) ;
#56224=CARTESIAN_POINT ( 'NONE',  ( -1.780377099653301709, 51.29164421682977348, -48.57534666485153707 ) ) ;
#56230=CARTESIAN_POINT ( 'NONE',  ( -5.000000000000000000, 60.11723469343148452, -46.25570701698029552 ) ) ;
#56285=CARTESIAN_POINT ( 'NONE',  ( -0.8419854211627070262, 10.28111362163633125, 63.57154293063805994 ) ) ;
#56302=CARTESIAN_POINT ( 'NONE',  ( 4.999999999999999112, 53.18690467503036956, 43.91652490638277584 ) ) ;
#56304=CARTESIAN_POINT ( 'NONE',  ( 3.407298021510790864, 68.04056125360874319, 20.39715949456173050 ) ) ;
#56344=CARTESIAN_POINT ( 'NONE',  ( -2.886287813027996254E-11, 51.14729664189304970, 48.52014062455092613 ) ) ;
#56354=CARTESIAN_POINT ( 'NONE',  ( 2.219371606101167238, -16.40787039054615093, 68.79427927095674988 ) ) ;
#56371=VECTOR ( 'NONE', #31309, 1000.000000000000000 ) ;
#56373=CARTESIAN_POINT ( 'NONE',  ( -5.107860025166345075, -10.26152767799330690, -64.38109526788291248 ) ) ;
#56389=ORIENTED_EDGE ( 'NONE', *, *, #4731, .F. ) ;
#56429=CARTESIAN_POINT ( 'NONE',  ( 5.000000000000000000, -10.00000000000000000, 75.19090595827292134 ) ) ;
#56446=CARTESIAN_POINT ( 'NONE',  ( -1.506680654954638987, 55.70239491600216297, 43.84725041001183143 ) ) ;
#56462=EDGE_CURVE ( 'NONE', #19443, #4330, #70975, .T. ) ;
#56466=DIRECTION ( 'NONE',  ( 0.000000000000000000, 0.000000000000000000, -1.000000000000000000 ) ) ;
#56472=CARTESIAN_POINT ( 'NONE',  ( 4.737866951550043559, -52.21905653846192052, 48.93292554253444138 ) ) ;
#56510=CARTESIAN_POINT ( 'NONE',  ( -3.428378827827392783, -16.35907404636618523, -69.10239319626211341 ) ) ;
#56528=CARTESIAN_POINT ( 'NONE',  ( 0.8721677472502531447, 16.44158143986616949, -68.58266913489720196 ) ) ;
#56563=CARTESIAN_POINT ( 'NONE',  ( 5.126144196591278401, -52.42426806216655422, -49.01287729762245959 ) ) ;
#56570=ORIENTED_EDGE ( 'NONE', *, *, #62415, .T. ) ;
#56576=CARTESIAN_POINT ( 'NONE',  ( 5.126106709314341536, 16.23426604260439632, 69.90716554747308464 ) ) ;
#56602=CARTESIAN_POINT ( 'NONE',  ( -2.997005883569377804, 55.94527535363560844, -43.97975057404802612 ) ) ;
#56629=EDGE_LOOP ( 'NONE', ( #68638, #43510, #32551, #28278, #35756 ) ) ;
#56675=CARTESIAN_POINT ( 'NONE',  ( -5.000000000000000000, 53.39837237779330081, -47.14918772354884879 ) ) ;
#56676=VERTEX_POINT ( 'NONE', #40852 ) ;
#56677=CARTESIAN_POINT ( 'NONE',  ( 3.728321214240235548, -66.24762070548278814, 26.57448171413092197 ) ) ;
#56681=CARTESIAN_POINT ( 'NONE',  ( 5.000000000000000888, 53.12474899268135431, 47.87640533067916948 ) ) ;
#56689=CARTESIAN_POINT ( 'NONE',  ( 5.000000000000000000, 10.00000000000000000, -75.19090595827292134 ) ) ;
#56698=ORIENTED_EDGE ( 'NONE', *, *, #61345, .F. ) ;
#56730=CARTESIAN_POINT ( 'NONE',  ( -4.737866951563228568, -68.48668487056878007, 20.75656675268391638 ) ) ;
#56732=CARTESIAN_POINT ( 'NONE',  ( -5.000000000000000000, 65.00666015986153923, 24.03732210400620062 ) ) ;
#56764=EDGE_LOOP ( 'NONE', ( #64859, #70302, #33726, #32594, #44720 ) ) ;
#56789=EDGE_CURVE ( 'NONE', #35502, #9105, #53031, .T. ) ;
#56806=DIRECTION ( 'NONE',  ( 0.000000000000000000, -0.8778652960885079404, 0.4789076340208374138 ) ) ;
#56810=AXIS2_PLACEMENT_3D ( 'NONE', #24267, #6564, #2006 ) ;
#56818=CARTESIAN_POINT ( 'NONE',  ( 2.589639417653039288, 50.10293296561670218, 40.79253907059217710 ) ) ;
#56819=CARTESIAN_POINT ( 'NONE',  ( 5.000000000000000000, -60.90295814858238543, -23.31388853594834032 ) ) ;
#56825=CARTESIAN_POINT ( 'NONE',  ( 4.999999999999999112, -50.98458432551128539, -41.27351214092455933 ) ) ;
#56838=CARTESIAN_POINT ( 'NONE',  ( 5.000000000000000000, -67.10422270468698969, -23.07049055144788952 ) ) ;
#56842=CARTESIAN_POINT ( 'NONE',  ( 2.620431783923081959, -55.87941608673214233, 43.94382193462615049 ) ) ;
#56855=DIRECTION ( 'NONE',  ( 1.000000000000000000, -0.000000000000000000, 0.000000000000000000 ) ) ;
#56910=CIRCLE ( 'NONE', #29230, 5.000000000000000000 ) ;
#56946=CARTESIAN_POINT ( 'NONE',  ( 4.737866951562321738, 16.26762833210778680, 69.68949229523451550 ) ) ;
#56998=VERTEX_POINT ( 'NONE', #61170 ) ;
#57029=LINE ( 'NONE', #44586, #41895 ) ;
#57047=CARTESIAN_POINT ( 'NONE',  ( -5.000000000000000000, 53.55923425356163392, -45.42020841079019533 ) ) ;
#57066=ORIENTED_EDGE ( 'NONE', *, *, #58421, .T. ) ;
#57077=ORIENTED_EDGE ( 'NONE', *, *, #6917, .F. ) ;
#57095=ORIENTED_EDGE ( 'NONE', *, *, #62531, .T. ) ;
#57097=CARTESIAN_POINT ( 'NONE',  ( 1.506524674532313535, -10.12152537343867031, 70.16785718946155725 ) ) ;
#57120=CARTESIAN_POINT ( 'NONE',  ( 1.506680654948938658, -10.12163528317107719, -70.16331425389822130 ) ) ;
#57134=DIRECTION ( 'NONE',  ( 1.000000000000000000, 0.000000000000000000, 0.000000000000000000 ) ) ;
#57179=CARTESIAN_POINT ( 'NONE',  ( 4.999999999999998224, 52.63864145287949725, -42.88977517748021029 ) ) ;
#57191=CARTESIAN_POINT ( 'NONE',  ( -0.4501631047668632757, 51.14740050675958116, 48.52018030598983955 ) ) ;
#57214=CARTESIAN_POINT ( 'NONE',  ( -3.728321214209889156, -56.13798660964528864, 44.08488161418000573 ) ) ;
#57257=CARTESIAN_POINT ( 'NONE',  ( 4.217983994794715308, 51.98644305215067618, -48.84278562423046566 ) ) ;
#57276=CARTESIAN_POINT ( 'NONE',  ( -5.000000000000001776, -10.82431413986196134, 67.03128830763429846 ) ) ;
#57287=ORIENTED_EDGE ( 'NONE', *, *, #36921, .T. ) ;
#57322=CARTESIAN_POINT ( 'NONE',  ( 2.216418498319753017, 16.40908668940204151, 68.78644440154937456 ) ) ;
#57354=AXIS2_PLACEMENT_3D ( 'NONE', #63097, #11422, #34459 ) ;
#57373=ORIENTED_EDGE ( 'NONE', *, *, #59765, .F. ) ;
#57390=DIRECTION ( 'NONE',  ( 1.000000000000000000, -0.000000000000000000, 0.000000000000000000 ) ) ;
#57428=CARTESIAN_POINT ( 'NONE',  ( 4.999999999999999112, 50.98458432551099406, 41.27351214092492881 ) ) ;
#57436=CARTESIAN_POINT ( 'NONE',  ( 5.000000000000001776, 62.32183698944635353, -23.94439461060335361 ) ) ;
#57455=VERTEX_POINT ( 'NONE', #53934 ) ;
#57466=VERTEX_POINT ( 'NONE', #65615 ) ;
#57483=CARTESIAN_POINT ( 'NONE',  ( 1.882291019712136082, -10.12018455450522580, 70.22327770540285030 ) ) ;
#57498=B_SPLINE_CURVE_WITH_KNOTS ( 'NONE', 3,
 ( #22903, #21777, #73468, #4080, #68556, #44804, #67445, #22519, #16859, #44430 ),
 .UNSPECIFIED., .F., .F.,
 ( 4, 2, 2, 2, 4 ),
 ( 0.000000000000000000, 0.001314083742622693986, 0.002628167485245387971, 0.003942251227868081957, 0.005256334970490775943 ),
 .UNSPECIFIED. ) ;
#57565=CARTESIAN_POINT ( 'NONE',  ( 3.369429374625374951, -10.27270496052241278, 63.91910092334654792 ) ) ;
#57571=CARTESIAN_POINT ( 'NONE',  ( 1.296342370383217313, 49.95006747299250804, 40.70914535207719354 ) ) ;
#57593=CARTESIAN_POINT ( 'NONE',  ( -0.7581620860321414135, 65.76154746682149721, -26.27794529688514658 ) ) ;
#57595=FACE_BOUND ( 'NONE', #71227, .T. ) ;
#57605=CARTESIAN_POINT ( 'NONE',  ( 4.999999999999999112, -10.82378452496227261, 67.02990231369372509 ) ) ;
#57629=CARTESIAN_POINT ( 'NONE',  ( -0.4368895104720005862, -16.44602605510715421, -68.55492853905352035 ) ) ;
#57641=B_SPLINE_CURVE_WITH_KNOTS ( 'NONE', 3,
 ( #45843, #6610, #63192, #58667, #11893, #51886, #12983, #29617, #28496, #226, #52630, #594 ),
 .UNSPECIFIED., .F., .F.,
 ( 4, 2, 2, 2, 2, 4 ),
 ( 1.618164387277533384E-15, 0.002547658444429638010, 0.005095316888857658391, 0.006369146111071668365, 0.007642975333285679206, 0.01019063377771369655 ),
 .UNSPECIFIED. ) ;
#57654=CARTESIAN_POINT ( 'NONE',  ( 5.000000000000000000, -61.58678017309387798, 23.68362420833305038 ) ) ;
#57689=DIRECTION ( 'NONE',  ( 0.000000000000000000, 0.000000000000000000, -1.000000000000000000 ) ) ;
#57698=CARTESIAN_POINT ( 'NONE',  ( -5.107860025160073647, 10.26152767799289123, 64.38109526790010761 ) ) ;
#57706=DIRECTION ( 'NONE',  ( 0.000000000000000000, 0.000000000000000000, 1.000000000000000000 ) ) ;
#57711=CARTESIAN_POINT ( 'NONE',  ( 4.104248244562368697, 66.38464254922966745, 26.65807398667948291 ) ) ;
#57778=CARTESIAN_POINT ( 'NONE',  ( -1.736494649864163131, 51.27805538754891757, 48.57014059985818477 ) ) ;
#57796=CARTESIAN_POINT ( 'NONE',  ( -5.000000000000000000, -53.21762015693864356, -47.70201125340226156 ) ) ;
#57813=CARTESIAN_POINT ( 'NONE',  ( 4.999999999999999112, 65.75515815785567497, -23.82162496270573016 ) ) ;
#57853=CARTESIAN_POINT ( 'NONE',  ( -4.465349678524266785, -66.51625814178508733, 26.73836809291843153 ) ) ;
#57922=EDGE_CURVE ( 'NONE', #47939, #63554, #60287, .T. ) ;
#57943=CARTESIAN_POINT ( 'NONE',  ( -3.373128826976394379, -10.27267468567300135, 63.92035228378879452 ) ) ;
#57956=CARTESIAN_POINT ( 'NONE',  ( 5.000000000000000888, -53.20585484986793290, -47.69738026034749367 ) ) ;
#57969=CARTESIAN_POINT ( 'NONE',  ( 5.000000000000000000, -68.48952624890522145, -21.22548696402925117 ) ) ;
#57973=CARTESIAN_POINT ( 'NONE',  ( -1.780377099653247974, -51.29164421682995822, 48.57534666485132391 ) ) ;
#57980=DIRECTION ( 'NONE',  ( -0.000000000000000000, -1.000000000000000000, -0.000000000000000000 ) ) ;
#57987=CARTESIAN_POINT ( 'NONE',  ( 5.000000000000000000, -11.00774715070946108, 67.37702390743022818 ) ) ;
#58003=LINE ( 'NONE', #47387, #36292 ) ;
#58014=CARTESIAN_POINT ( 'NONE',  ( -5.000000000000000000, 0.000000000000000000, 0.000000000000000000 ) ) ;
#58043=CARTESIAN_POINT ( 'NONE',  ( 4.193070328474943764, 60.66867996115621509, 23.17096354272623415 ) ) ;
#58059=CARTESIAN_POINT ( 'NONE',  ( -5.000000000000000888, 65.00653492603765926, -24.02639942437745191 ) ) ;
#58089=CARTESIAN_POINT ( 'NONE',  ( 2.170320029193293809, -67.76782500014387267, 20.17643218080241496 ) ) ;
#58100=CIRCLE ( 'NONE', #8695, 5.000000000000000888 ) ;
#58118=CARTESIAN_POINT ( 'NONE',  ( 2.997005883564160644, 10.11494357242049524, -70.43990496500994425 ) ) ;
#58122=B_SPLINE_CURVE_WITH_KNOTS ( 'NONE', 3,
 ( #62908, #12346, #6697, #18382, #35737, #7065, #30071, #16878, #39901, #53086, #42115, #65127, #24405, #13436, #14177, #13800, #36473, #20210, #19110, #59489 ),
 .UNSPECIFIED., .F., .F.,
 ( 4, 2, 2, 2, 2, 2, 2, 2, 2, 4 ),
 ( 0.000000000000000000, 0.001156441540183927559, 0.001734662310275893616, 0.002312883080367859456, 0.003469324620551791135, 0.004625766160735723248, 0.005782207700919654060, 0.006938649241103586607, 0.008095090781287518286, 0.009251532321471449966 ),
 .UNSPECIFIED. ) ;
#58153=CARTESIAN_POINT ( 'NONE',  ( 2.170320029210516921, -16.41060967376241564, 68.77687409974784316 ) ) ;
#58243=DIRECTION ( 'NONE',  ( 1.000000000000000000, -0.000000000000000000, -0.000000000000000000 ) ) ;
#58262=DIRECTION ( 'NONE',  ( 0.000000000000000000, -0.5207998305029790664, 0.8536788251725986321 ) ) ;
#58301=ORIENTED_EDGE ( 'NONE', *, *, #51567, .T. ) ;
#58325=LINE ( 'NONE', #62838, #66148 ) ;
#58336=CARTESIAN_POINT ( 'NONE',  ( 5.000000000000000000, -66.10919140997980037, -23.67639547906034991 ) ) ;
#58337=EDGE_CURVE ( 'NONE', #24245, #35502, #28954, .T. ) ;
#58341=CARTESIAN_POINT ( 'NONE',  ( -1.317228840348880325, -55.68607278122971849, 43.83834608838142088 ) ) ;
#58391=CARTESIAN_POINT ( 'NONE',  ( -5.000000000000000000, 11.14555136602165142, 27.84144949604463193 ) ) ;
#58421=EDGE_CURVE ( 'NONE', #57455, #30587, #11801, .T. ) ;
#58437=CARTESIAN_POINT ( 'NONE',  ( -0.7509181236784702174, 10.12341933770169256, 70.08957333326500816 ) ) ;
#58451=CARTESIAN_POINT ( 'NONE',  ( 1.506680654955621534, 65.82403019916786491, 26.31606384388625131 ) ) ;
#58481=CARTESIAN_POINT ( 'NONE',  ( -4.471435261917971360, 10.26549131683129623, -64.21726486257941247 ) ) ;
#58537=CARTESIAN_POINT ( 'NONE',  ( 5.000000000000000000, 52.35862550122993042, -48.98731492261362064 ) ) ;
#58637=VERTEX_POINT ( 'NONE', #30268 ) ;
#58667=CARTESIAN_POINT ( 'NONE',  ( -1.688721909672437294, -10.27943647337372290, -63.64086505882561795 ) ) ;
#58745=EDGE_CURVE ( 'NONE', #3455, #31632, #18575, .T. ) ;
#58752=EDGE_CURVE ( 'NONE', #55139, #49656, #9741, .T. ) ;
#58765=DIRECTION ( 'NONE',  ( 0.000000000000000000, -0.8778652960884978373, -0.4789076340208558435 ) ) ;
#58818=CARTESIAN_POINT ( 'NONE',  ( 7.456155213548061766, 61.82225697226374450, 23.87472085067569694 ) ) ;
#58847=CARTESIAN_POINT ( 'NONE',  ( 0.6474643998349955964, 10.28110762191874805, -63.57179091896464485 ) ) ;
#58852=EDGE_CURVE ( 'NONE', #71456, #22076, #44561, .T. ) ;
#58883=CARTESIAN_POINT ( 'NONE',  ( -3.407298021519794773, 51.68473891413969312, 48.72627478609783225 ) ) ;
#58917=CARTESIAN_POINT ( 'NONE',  ( 4.999999999999999112, 14.70234347858786528, 69.93881661156081009 ) ) ;
#58918=CARTESIAN_POINT ( 'NONE',  ( 5.000000000000000000, 64.62627855237467145, -24.10294814404638686 ) ) ;
#58919=B_SPLINE_CURVE_WITH_KNOTS ( 'NONE', 3,
 ( #37190, #8512, #54550, #2857, #25845, #48865, #65105, #60940, #14902 ),
 .UNSPECIFIED., .F., .F.,
 ( 4, 2, 1, 2, 4 ),
 ( 0.000000000000000000, 0.001314083742615642985, 0.002628167485231287272, 0.003942251227846931341, 0.005256334970462575411 ),
 .UNSPECIFIED. ) ;
#59012=CARTESIAN_POINT ( 'NONE',  ( 5.000000000000000000, 29.68417822476661527, -4.268394125862720934 ) ) ;
#59045=ORIENTED_EDGE ( 'NONE', *, *, #24375, .T. ) ;
#59073=CARTESIAN_POINT ( 'NONE',  ( 4.336811714529170025, 68.30918023748891699, -20.61428864874696032 ) ) ;
#59078=CARTESIAN_POINT ( 'NONE',  ( -14.00000000000000178, 0.000000000000000000, -17.50000000000000000 ) ) ;
#59099=CARTESIAN_POINT ( 'NONE',  ( -5.000000000000000000, 18.53862685874493010, -23.57305537018094554 ) ) ;
#59112=CARTESIAN_POINT ( 'NONE',  ( 2.160335347094620939, 51.35526406371981523, -48.59969451235843962 ) ) ;
#59124=CARTESIAN_POINT ( 'NONE',  ( 5.000000000000000888, 13.57926339724853371, -69.65188861886713312 ) ) ;
#59133=CIRCLE ( 'NONE', #49469, 70.50000000000000000 ) ;
#59187=ORIENTED_EDGE ( 'NONE', *, *, #19650, .F. ) ;
#59188=CARTESIAN_POINT ( 'NONE',  ( -0.6474643998350495533, 60.19533971085391499, 22.88219507985867196 ) ) ;
#59222=ORIENTED_EDGE ( 'NONE', *, *, #26143, .F. ) ;
#59283=CARTESIAN_POINT ( 'NONE',  ( 4.999999999999999112, 15.47455834364811622, 69.96446835377025764 ) ) ;
#59295=AXIS2_PLACEMENT_3D ( 'NONE', #47080, #40691, #57689 ) ;
#59418=CARTESIAN_POINT ( 'NONE',  ( -3.407298021520221543, -68.04056125361168483, 20.39715949456294908 ) ) ;
#59476=DIRECTION ( 'NONE',  ( 1.000000000000000000, -0.000000000000000000, -0.000000000000000000 ) ) ;
#59484=AXIS2_PLACEMENT_3D ( 'NONE', #37334, #25621, #54322 ) ;
#59489=CARTESIAN_POINT ( 'NONE',  ( -5.000000000000000000, 10.26105934116142215, 64.40045319026754100 ) ) ;
#59491=ORIENTED_EDGE ( 'NONE', *, *, #27807, .F. ) ;
#59498=CARTESIAN_POINT ( 'NONE',  ( 0.000000000000000000, 0.000000000000000000, 0.000000000000000000 ) ) ;
#59505=ORIENTED_EDGE ( 'NONE', *, *, #49615, .T. ) ;
#59538=CARTESIAN_POINT ( 'NONE',  ( -1.739508062077478989, 67.70228923712431879, 20.12326043015404764 ) ) ;
#59550=CARTESIAN_POINT ( 'NONE',  ( -5.107860025165151363, 60.88642786445262090, 23.30380398316496482 ) ) ;
#59573=ORIENTED_EDGE ( 'NONE', *, *, #39918, .T. ) ;
#59581=CARTESIAN_POINT ( 'NONE',  ( 3.373128826976389938, 50.22031155377564460, -40.85657338450008069 ) ) ;
#59641=ORIENTED_EDGE ( 'NONE', *, *, #40490, .F. ) ;
#59668=( NAMED_UNIT ( * ) SI_UNIT ( $, .STERADIAN. ) SOLID_ANGLE_UNIT ( ) );
#59765=EDGE_CURVE ( 'NONE', #58637, #3120, #61217, .T. ) ;
#59794=CARTESIAN_POINT ( 'NONE',  ( 4.330454160157055199, -16.29811171461376063, -69.49285720718685866 ) ) ;
#59834=DIRECTION ( 'NONE',  ( 0.000000000000000000, 0.000000000000000000, 1.000000000000000000 ) ) ;
#59902=CARTESIAN_POINT ( 'NONE',  ( -1.739508062077478767, 16.42388987907938258, 68.69353258878824420 ) ) ;
#59915=CARTESIAN_POINT ( 'NONE',  ( -6.308070865121395698, 61.28915309318116300, 23.54949267155276971 ) ) ;
#59917=CARTESIAN_POINT ( 'NONE',  ( 5.000000000000001776, 68.60357193678683529, 20.85024232999420946 ) ) ;
#59927=CARTESIAN_POINT ( 'NONE',  ( 5.000000000000000000, 60.90295814858271939, -23.31388853594749833 ) ) ;
#59999=DIRECTION ( 'NONE',  ( -0.000000000000000000, -1.000000000000000000, -0.000000000000000000 ) ) ;
#60021=AXIS2_PLACEMENT_3D ( 'NONE', #70181, #64516, #12814 ) ;
#60091=CARTESIAN_POINT ( 'NONE',  ( -0.4451317748924059625, 51.14719335908522169, -48.52010116548709817 ) ) ;
#60252=ORIENTED_EDGE ( 'NONE', *, *, #24852, .F. ) ;
#60287=CIRCLE ( 'NONE', #49455, 4.999999999999997335 ) ;
#60338=CARTESIAN_POINT ( 'NONE',  ( 4.217983994790206914, 16.30587161610658242, 69.44297314766849638 ) ) ;
#60348=DIRECTION ( 'NONE',  ( 0.000000000000000000, 0.5207998305029731823, -0.8536788251726022958 ) ) ;
#60400=CARTESIAN_POINT ( 'NONE',  ( -5.000000000000000000, -29.68417822476651580, -4.268394125863113509 ) ) ;
#60412=B_SPLINE_CURVE_WITH_KNOTS ( 'NONE', 3,
 ( #6112, #40065, #17041, #56304, #46087, #22697, #4620, #63070, #11763 ),
 .UNSPECIFIED., .F., .F.,
 ( 4, 2, 1, 2, 4 ),
 ( 0.000000000000000000, 0.001314083742622694203, 0.002628167485245388405, 0.003942251227868082825, 0.005256334970490776810 ),
 .UNSPECIFIED. ) ;
#60433=VECTOR ( 'NONE', #38194, 1000.000000000000000 ) ;
#60447=CARTESIAN_POINT ( 'NONE',  ( -4.999999999999999112, 52.62579568235267402, -48.70175807017950120 ) ) ;
#60459=VERTEX_POINT ( 'NONE', #25067 ) ;
#60460=EDGE_CURVE ( 'NONE', #1129, #42334, #48085, .T. ) ;
#60529=CARTESIAN_POINT ( 'NONE',  ( 3.074111742560546201, -16.37317034319798026, -69.01341173090936820 ) ) ;
#60586=ORIENTED_EDGE ( 'NONE', *, *, #33856, .T. ) ;
#60632=CARTESIAN_POINT ( 'NONE',  ( -4.999999999999999112, -51.89737250574534499, 42.00009673807092980 ) ) ;
#60644=CARTESIAN_POINT ( 'NONE',  ( -2.926785083138225622E-14, 16.44602605510714355, 68.55492853905353456 ) ) ;
#60656=VERTEX_POINT ( 'NONE', #61279 ) ;
#60671=CARTESIAN_POINT ( 'NONE',  ( -1.704527592502764533, 60.27089976682823647, -22.92829164824309984 ) ) ;
#60684=CARTESIAN_POINT ( 'NONE',  ( 5.000000000000000000, -10.28295106684163684, -65.17663434001590872 ) ) ;
#60691=CARTESIAN_POINT ( 'NONE',  ( -5.000000000000000000, 50.64189880742145533, -41.08656465431843685 ) ) ;
#60694=ORIENTED_EDGE ( 'NONE', *, *, #27403, .F. ) ;
#60815=CARTESIAN_POINT ( 'NONE',  ( -14.00000000000000178, 2.249999999994893862, 7.677076266393539683 ) ) ;
#60851=ORIENTED_EDGE ( 'NONE', *, *, #56462, .F. ) ;
#60884=CARTESIAN_POINT ( 'NONE',  ( -4.330454160155839283, -16.29811171461466301, 69.49285720718616233 ) ) ;
#60895=CARTESIAN_POINT ( 'NONE',  ( -5.000000000000000000, 53.36732872257244509, 44.46877392682823427 ) ) ;
#60900=ORIENTED_EDGE ( 'NONE', *, *, #24375, .F. ) ;
#60937=B_SPLINE_CURVE_WITH_KNOTS ( 'NONE', 3,
 ( #65999, #37340, #60338, #65255, #20339, #25991, #49391, #37720, #53948, #49015 ),
 .UNSPECIFIED., .F., .F.,
 ( 4, 2, 2, 2, 4 ),
 ( 0.000000000000000000, 0.001314083742622693335, 0.002628167485245387971, 0.003942251227868082825, 0.005256334970490775943 ),
 .UNSPECIFIED. ) ;
#60940=CARTESIAN_POINT ( 'NONE',  ( -0.4369882809979233063, 67.59332269700190921, -20.03478791450335095 ) ) ;
#60954=VECTOR ( 'NONE', #1880, 1000.000000000000227 ) ;
#60963=DIRECTION ( 'NONE',  ( 0.000000000000000000, 0.9997074645238147594, -0.02418647091589873691 ) ) ;
#60979=CARTESIAN_POINT ( 'NONE',  ( 4.471435261917476645, -60.74652839096075496, -23.21845616858407979 ) ) ;
#61026=B_SPLINE_CURVE_WITH_KNOTS ( 'NONE', 3,
 ( #5433, #28436, #11094, #44677, #67692, #27686, #50694, #22024, #51443, #74456, #44304, #16350 ),
 .UNSPECIFIED., .F., .F.,
 ( 4, 2, 2, 2, 2, 4 ),
 ( 0.000000000000000000, 0.002547658444427996095, 0.005095316888855990455, 0.006369146111069987418, 0.007642975333283984381, 0.01019063377771197917 ),
 .UNSPECIFIED. ) ;
#61031=CARTESIAN_POINT ( 'NONE',  ( 4.999999999999999112, 61.58609660504352945, 23.68302032025150439 ) ) ;
#61037=EDGE_CURVE ( 'NONE', #16375, #37723, #29308, .T. ) ;
#61053=CARTESIAN_POINT ( 'NONE',  ( -4.999999999999996447, 11.14555136602165142, 27.84144949604463193 ) ) ;
#61055=CARTESIAN_POINT ( 'NONE',  ( 5.000000000000000000, -13.22058908515350417, -69.49198671174480069 ) ) ;
#61084=CARTESIAN_POINT ( 'NONE',  ( -1.877992804782812053, -55.75022808459689827, -43.87334515336773677 ) ) ;
#61090=DIRECTION ( 'NONE',  ( 0.000000000000000000, 0.000000000000000000, -1.000000000000000000 ) ) ;
#61116=CARTESIAN_POINT ( 'NONE',  ( 5.000000000000000000, -16.14408868864072844, 27.96238185062368586 ) ) ;
#61170=CARTESIAN_POINT ( 'NONE',  ( -5.000000000000000000, 52.35862550122993042, -48.98731492261362064 ) ) ;
#61181=ADVANCED_FACE ( 'NONE', ( #61850 ), #27013, .F. ) ;
#61216=ORIENTED_EDGE ( 'NONE', *, *, #52654, .F. ) ;
#61217=CIRCLE ( 'NONE', #21618, 71.70204102886728492 ) ;
#61257=ORIENTED_EDGE ( 'NONE', *, *, #22673, .F. ) ;
#61272=CARTESIAN_POINT ( 'NONE',  ( -5.000000000000000000, 52.62657404299657316, 48.70092614269928788 ) ) ;
#61279=CARTESIAN_POINT ( 'NONE',  ( 4.999999999999997335, 16.24494643555759410, 69.83755725260752456 ) ) ;
#61293=ORIENTED_EDGE ( 'NONE', *, *, #33856, .F. ) ;
#61310=ORIENTED_EDGE ( 'NONE', *, *, #7790, .T. ) ;
#61321=CARTESIAN_POINT ( 'NONE',  ( -2.967813307894019431E-11, 16.44602605510714355, -68.55492853905352035 ) ) ;
#61345=EDGE_CURVE ( 'NONE', #70301, #27257, #64862, .T. ) ;
#61356=CARTESIAN_POINT ( 'NONE',  ( -3.544144923084051602, -60.54353712382344099, -23.09461823984392481 ) ) ;
#61400=CARTESIAN_POINT ( 'NONE',  ( 5.000000000000000000, -53.35645474066812710, 47.33026262608733958 ) ) ;
#61408=CARTESIAN_POINT ( 'NONE',  ( 5.000000000000000000, 67.10422270468680495, 23.07049055144833716 ) ) ;
#61430=CARTESIAN_POINT ( 'NONE',  ( 4.231687259402700185, 16.30907003467283189, -69.42009600258256796 ) ) ;
#61463=CARTESIAN_POINT ( 'NONE',  ( -1.308779242311861601, -49.95118570763067822, -40.70975538998027332 ) ) ;
#61489=CARTESIAN_POINT ( 'NONE',  ( 0.000000000000000000, 0.000000000000000000, 0.000000000000000000 ) ) ;
#61491=LINE ( 'NONE', #43762, #65671 ) ;
#61500=CARTESIAN_POINT ( 'NONE',  ( 2.990854866088366482, 55.96051345247598618, -43.98806351443035112 ) ) ;
#61527=EDGE_CURVE ( 'NONE', #18569, #3989, #22062, .T. ) ;
#61583=CARTESIAN_POINT ( 'NONE',  ( 2.219371606097704230, -67.78152867896255884, 20.18750705526123923 ) ) ;
#61589=ORIENTED_EDGE ( 'NONE', *, *, #24106, .T. ) ;
#61613=VECTOR ( 'NONE', #44672, 1000.000000000000000 ) ;
#61618=B_SPLINE_CURVE_WITH_KNOTS ( 'NONE', 3,
 ( #48205, #71213, #27810, #50444, #73461, #21399, #20654, #33131, #39512, #15361, #44796, #72341, #56128, #3315, #50079, #55756, #72724, #61400, #27429, #49326, #21769, #32367 ),
 .UNSPECIFIED., .F., .F.,
 ( 4, 2, 2, 2, 2, 2, 2, 2, 2, 2, 4 ),
 ( 0.000000000000000000, 0.001156727053362487578, 0.001735090580043716513, 0.002313454106724945666, 0.003470181160087403537, 0.004048544686768637026, 0.004626908213449870515, 0.005783635266812338360, 0.006940362320174804471, 0.008097089373537270582, 0.009253816426899737560 ),
 .UNSPECIFIED. ) ;
#61638=CARTESIAN_POINT ( 'NONE',  ( -1.506680654948961307, -10.12163528317163674, 70.16331425389374488 ) ) ;
#61658=CARTESIAN_POINT ( 'NONE',  ( 1.877992804775685087, -10.12031740952197190, -70.21778636472329538 ) ) ;
#61669=CARTESIAN_POINT ( 'NONE',  ( -5.000000000000000000, -62.88740100213664874, 24.06179116403727036 ) ) ;
#61711=AXIS2_PLACEMENT_3D ( 'NONE', #19383, #52629, #29981 ) ;
#61716=CARTESIAN_POINT ( 'NONE',  ( 5.000000000000000000, 51.74377041917585984, -41.86884046506214929 ) ) ;
#61729=CARTESIAN_POINT ( 'NONE',  ( -2.589639417652795483, -60.37884160280842138, -22.99414321703674347 ) ) ;
#61752=CARTESIAN_POINT ( 'NONE',  ( 1.877992804773993329, -55.75022808459807067, 43.87334515336884522 ) ) ;
#61773=DIRECTION ( 'NONE',  ( 0.000000000000000000, 0.000000000000000000, -1.000000000000000000 ) ) ;
#61836=CARTESIAN_POINT ( 'NONE',  ( 0.7509181236784723268, -55.63764137817189237, -43.81192498624803733 ) ) ;
#61850=FACE_OUTER_BOUND ( 'NONE', #10534, .T. ) ;
#61866=DIRECTION ( 'NONE',  ( 0.000000000000000000, 0.000000000000000000, -1.000000000000000000 ) ) ;
#61871=EDGE_CURVE ( 'NONE', #60459, #44073, #74571, .T. ) ;
#61874=CARTESIAN_POINT ( 'NONE',  ( 4.737866951553296957, 52.21905653844932260, -48.93292554255041438 ) ) ;
#61906=DIRECTION ( 'NONE',  ( 1.000000000000000000, -0.000000000000000000, -0.000000000000000000 ) ) ;
#61922=LINE ( 'NONE', #32905, #39688 ) ;
#61944=CARTESIAN_POINT ( 'NONE',  ( 5.000000000000000000, 16.14408868864073554, -27.96238185062347981 ) ) ;
#61946=CARTESIAN_POINT ( 'NONE',  ( 2.266287154879827348, -60.33498852648436639, 22.96738997677403660 ) ) ;
#61975=PRODUCT ( 'hand wheel', 'hand wheel', '', ( #34279 ) ) ;
#62003=CARTESIAN_POINT ( 'NONE',  ( 2.266287154886623689, -10.27715108473166694, 63.73532778936404242 ) ) ;
#62016=CARTESIAN_POINT ( 'NONE',  ( -4.999999999999996447, -18.53862685874494431, 23.57305537018116581 ) ) ;
#62023=CARTESIAN_POINT ( 'NONE',  ( 2.591411123055314292, -10.27614846265026038, -63.77676950206216588 ) ) ;
#62040=CARTESIAN_POINT ( 'NONE',  ( -4.999999999999999112, 14.31098243164692008, -69.87317657433686691 ) ) ;
#62056=ORIENTED_EDGE ( 'NONE', *, *, #54301, .T. ) ;
#62074=ORIENTED_EDGE ( 'NONE', *, *, #7035, .T. ) ;
#62094=CARTESIAN_POINT ( 'NONE',  ( -5.086519500888709189, 50.65542486323467131, 41.09394361259066386 ) ) ;
#62096=CARTESIAN_POINT ( 'NONE',  ( -3.728321214214307844, -66.24762070552739601, -26.57448171415594729 ) ) ;
#62135=CIRCLE ( 'NONE', #7890, 10.99999999999999645 ) ;
#62174=CARTESIAN_POINT ( 'NONE',  ( 0.4369882809721238326, -51.14729664189373182, 48.52014062455020849 ) ) ;
#62202=CARTESIAN_POINT ( 'NONE',  ( -1.506680654955159460, -55.70239491600695203, -43.84725041001593837 ) ) ;
#62238=CARTESIAN_POINT ( 'NONE',  ( -0.6474643998434820302, 49.91423208894237007, -40.68959583910810096 ) ) ;
#62245=ORIENTED_EDGE ( 'NONE', *, *, #67650, .F. ) ;
#62269=CARTESIAN_POINT ( 'NONE',  ( 5.000000000000000000, -10.26105934116143281, -64.40045319026697257 ) ) ;
#62316=CARTESIAN_POINT ( 'NONE',  ( -5.000000000000000000, 53.18690467503129327, -43.91652490638166739 ) ) ;
#62318=CARTESIAN_POINT ( 'NONE',  ( 0.3752463838826636811, -65.74564559951694775, 26.26824411940134851 ) ) ;
#62320=CARTESIAN_POINT ( 'NONE',  ( 5.000000000000000000, 52.63770595436645294, 42.88862352055369342 ) ) ;
#62365=CARTESIAN_POINT ( 'NONE',  ( 3.228176881619535088, -10.27295505383823304, 63.90876373295927237 ) ) ;
#62367=CARTESIAN_POINT ( 'NONE',  ( -5.000000000000000000, 66.11467145570868809, 23.67355326543111005 ) ) ;
#62377=CARTESIAN_POINT ( 'NONE',  ( 5.000000000000000000, 29.68417822476661172, -4.268394125862716493 ) ) ;
#62387=CARTESIAN_POINT ( 'NONE',  ( -2.997005883568874207, -10.11494357241825526, -70.43990496499247911 ) ) ;
#62404=CARTESIAN_POINT ( 'NONE',  ( -5.000000000000000000, 12.55023575007693104, -69.09043692422063998 ) ) ;
#62415=EDGE_CURVE ( 'NONE', #42285, #38888, #11758, .T. ) ;
#62445=CARTESIAN_POINT ( 'NONE',  ( 4.999999999999999112, 52.62657404299758923, -48.70092614269818654 ) ) ;
#62457=CARTESIAN_POINT ( 'NONE',  ( 2.266287154880008980, 50.05783744175044347, 40.76793781259059557 ) ) ;
#62480=CARTESIAN_POINT ( 'NONE',  ( 4.104248244547289204, -56.27889056305692606, 44.16174987544510344 ) ) ;
#62489=FACE_OUTER_BOUND ( 'NONE', #38786, .T. ) ;
#62531=EDGE_CURVE ( 'NONE', #4661, #10747, #7629, .T. ) ;
#62541=CARTESIAN_POINT ( 'NONE',  ( 3.428378827818546970, 51.66489094707695529, 48.71857030467419492 ) ) ;
#62563=ORIENTED_EDGE ( 'NONE', *, *, #47539, .T. ) ;
#62565=EDGE_CURVE ( 'NONE', #60656, #40460, #46204, .T. ) ;
#62582=CARTESIAN_POINT ( 'NONE',  ( -0.6474643998350001484, 10.28110762191874628, 63.57179091896463063 ) ) ;
#62672=CARTESIAN_POINT ( 'NONE',  ( -5.000000000000000000, 0.000000000000000000, -71.70204102886728492 ) ) ;
#62681=CARTESIAN_POINT ( 'NONE',  ( -5.000000000000000888, 53.20585484986858660, -47.69738026034675471 ) ) ;
#62683=CARTESIAN_POINT ( 'NONE',  ( 4.465384415997323053, -66.51627080308875861, 26.73837581714047573 ) ) ;
#62690=ORIENTED_EDGE ( 'NONE', *, *, #38104, .T. ) ;
#62701=ORIENTED_EDGE ( 'NONE', *, *, #48223, .F. ) ;
#62704=CARTESIAN_POINT ( 'NONE',  ( -4.999999999999999112, -67.91007042436109487, -22.22893179987999090 ) ) ;
#62724=ORIENTED_EDGE ( 'NONE', *, *, #40069, .F. ) ;
#62734=CARTESIAN_POINT ( 'NONE',  ( -3.496982156820189314, -68.06496700477784145, 20.41687962716806481 ) ) ;
#62739=DIRECTION ( 'NONE',  ( 0.000000000000000000, -0.8536788251726021848, -0.5207998305029730712 ) ) ;
#62756=ADVANCED_FACE ( 'NONE', ( #72439 ), #3034, .F. ) ;
#62778=ORIENTED_EDGE ( 'NONE', *, *, #45656, .F. ) ;
#62803=B_SPLINE_CURVE_WITH_KNOTS ( 'NONE', 3,
 ( #27845, #34647, #321, #51982, #5959, #11611, #22929, #57276, #39910, #16504, #39544, #68207, #52353, #35020, #5590, #23299, #28588, #10495, #74237, #10869, #39168, #63660 ),
 .UNSPECIFIED., .F., .F.,
 ( 4, 2, 2, 2, 2, 2, 2, 2, 2, 2, 4 ),
 ( 0.000000000000000000, 0.001156727053362482157, 0.001735090580043723235, 0.002313454106724964314, 0.003470181160087444303, 0.004048544686768682996, 0.004626908213449921689, 0.005783635266812366983, 0.006940362320174811410, 0.008097089373537256704, 0.009253816426899701131 ),
 .UNSPECIFIED. ) ;
#62818=CARTESIAN_POINT ( 'NONE',  ( 4.999999999999999112, 53.50647209750621158, -45.02947987234000493 ) ) ;
#62828=AXIS2_PLACEMENT_3D ( 'NONE', #64704, #41325, #64335 ) ;
#62829=CARTESIAN_POINT ( 'NONE',  ( -2.620431783932123615, 55.87941608673077099, 43.94382193463441411 ) ) ;
#62838=CARTESIAN_POINT ( 'NONE',  ( -5.000000000000000000, 10.00000000000000000, -75.19090595827292134 ) ) ;
#62839=CARTESIAN_POINT ( 'NONE',  ( 4.217983994790200697, -16.30587161610658598, -69.44297314766851059 ) ) ;
#62844=ORIENTED_EDGE ( 'NONE', *, *, #61871, .F. ) ;
#62851=CARTESIAN_POINT ( 'NONE',  ( -1.506680654955644849, 65.82403019917288134, -26.31606384388262754 ) ) ;
#62859=DIRECTION ( 'NONE',  ( 0.000000000000000000, 0.8778652960885044987, -0.4789076340208435756 ) ) ;
#62877=DIRECTION ( 'NONE',  ( 0.000000000000000000, 0.000000000000000000, 1.000000000000000000 ) ) ;
#62908=CARTESIAN_POINT ( 'NONE',  ( -5.000000000000000000, 16.24494643555759410, 69.83755725260752456 ) ) ;
#62915=VECTOR ( 'NONE', #57980, 1000.000000000000000 ) ;
#62918=CARTESIAN_POINT ( 'NONE',  ( 4.999999999999999112, -67.53158052529160216, 22.66975313813502879 ) ) ;
#62953=B_SPLINE_CURVE_WITH_KNOTS ( 'NONE', 3,
 ( #22316, #44607, #38948, #56681, #51749, #67621, #51374, #10277, #33304, #67985, #32934, #55940, #56302, #27239, #62320, #50626, #4618, #11390, #57428, #45342 ),
 .UNSPECIFIED., .F., .F.,
 ( 4, 2, 2, 2, 2, 2, 2, 2, 2, 4 ),
 ( 0.000000000000000000, 0.001156441540183989576, 0.001734662310275984038, 0.002312883080367979152, 0.003469324620551983689, 0.004625766160735988661, 0.005782207700919994066, 0.006938649241103998604, 0.008095090781288004009, 0.009251532321472008547 ),
 .UNSPECIFIED. ) ;
#62983=CARTESIAN_POINT ( 'NONE',  ( 5.000000000000000000, 60.11723469343148452, -46.25570701698029552 ) ) ;
#63000=ADVANCED_FACE ( 'NONE', ( #55850 ), #50539, .F. ) ;
#63044=VERTEX_POINT ( 'NONE', #10189 ) ;
#63060=CARTESIAN_POINT ( 'NONE',  ( -5.000000000000000000, -53.09993190648242489, -43.73864582539253831 ) ) ;
#63070=CARTESIAN_POINT ( 'NONE',  ( 0.4369882809721245542, 67.59332269700051654, 20.03478791450397978 ) ) ;
#63085=CARTESIAN_POINT ( 'NONE',  ( -5.000000000000000000, -61.23620218020153771, -23.51718915682094391 ) ) ;
#63097=CARTESIAN_POINT ( 'NONE',  ( 0.000000000000000000, 0.000000000000000000, 0.000000000000000000 ) ) ;
#63136=CARTESIAN_POINT ( 'NONE',  ( -1.780377099652985740, -16.42166210098330126, -68.70754022607323463 ) ) ;
#63148=ORIENTED_EDGE ( 'NONE', *, *, #2307, .T. ) ;
#63192=CARTESIAN_POINT ( 'NONE',  ( -3.369429374625494411, -10.27270496052241100, -63.91910092334655502 ) ) ;
#63213=CARTESIAN_POINT ( 'NONE',  ( 13.99999999999999822, 2.143131898507868248E-15, 17.50000000000000000 ) ) ;
#63219=CARTESIAN_POINT ( 'NONE',  ( -4.193070328474952646, -60.66867996115655615, 23.17096354272540282 ) ) ;
#63226=CARTESIAN_POINT ( 'NONE',  ( -4.471435261918117909, 60.74652839096160761, -23.21845616858355399 ) ) ;
#63238=CARTESIAN_POINT ( 'NONE',  ( 5.000000000000000000, -10.25161785469019193, 64.79070129774501652 ) ) ;
#63312=CIRCLE ( 'NONE', #42841, 5.000000000000000888 ) ;
#63330=CARTESIAN_POINT ( 'NONE',  ( -1.780377099648780215, 16.42166210098345402, 68.70754022607248146 ) ) ;
#63338=CARTESIAN_POINT ( 'NONE',  ( -5.000000000000000000, -16.14408868864072844, -27.96238185062390613 ) ) ;
#63343=CARTESIAN_POINT ( 'NONE',  ( 5.086519500887227707, 60.91611154180610299, 23.32191296476149489 ) ) ;
#63379=ORIENTED_EDGE ( 'NONE', *, *, #7146, .T. ) ;
#63380=ADVANCED_FACE ( 'NONE', ( #68496 ), #13980, .F. ) ;
#63409=CARTESIAN_POINT ( 'NONE',  ( -2.160335347094220371, 51.35526406371868546, 48.59969451235947702 ) ) ;
#63415=CARTESIAN_POINT ( 'NONE',  ( 0.4320110153364553618, 10.28109898471437589, 63.57214792341211762 ) ) ;
#63417=CARTESIAN_POINT ( 'NONE',  ( -5.000000000000000000, -11.14555136602165675, -27.84144949604441166 ) ) ;
#63427=CARTESIAN_POINT ( 'NONE',  ( -5.000000000000000000, -50.64189880742087269, -41.08656465431914029 ) ) ;
#63442=CARTESIAN_POINT ( 'NONE',  ( 4.999999999999998224, 67.66364885638974158, -22.52891795222217297 ) ) ;
#63452=CARTESIAN_POINT ( 'NONE',  ( -5.000000000000000000, -61.58678017309371455, -23.68362420833346960 ) ) ;
#63487=CARTESIAN_POINT ( 'NONE',  ( 2.436599634633794587, -16.39988855009488589, 68.84456747601390703 ) ) ;
#63554=VERTEX_POINT ( 'NONE', #52640 ) ;
#63573=CARTESIAN_POINT ( 'NONE',  ( 5.000000000000000000, -70.11723469343111503, 28.93519894129190817 ) ) ;
#63577=CARTESIAN_POINT ( 'NONE',  ( -4.465349678524261456, 56.41423509509874634, 44.23558526901069143 ) ) ;
#63599=CARTESIAN_POINT ( 'NONE',  ( -1.781595147096461274, 67.70776641946500263, -20.12770457511257050 ) ) ;
#63654=DIRECTION ( 'NONE',  ( 1.000000000000000000, 0.000000000000000000, 0.000000000000000000 ) ) ;
#63660=CARTESIAN_POINT ( 'NONE',  ( -5.000000000000000000, -16.24494643555759410, 69.83755725260752456 ) ) ;
#63662=CARTESIAN_POINT ( 'NONE',  ( 2.170320029194141132, 51.35721532638042675, 48.60044191894211707 ) ) ;
#63717=CARTESIAN_POINT ( 'NONE',  ( 6.891449706546032061, 61.56004288259459400, 23.71475313280759423 ) ) ;
#63729=ADVANCED_FACE ( 'NONE', ( #44724, #9274 ), #9658, .F. ) ;
#63735=EDGE_CURVE ( 'NONE', #17054, #24578, #31822, .T. ) ;
#63750=DIRECTION ( 'NONE',  ( 0.000000000000000000, 0.000000000000000000, -1.000000000000000000 ) ) ;
#63753=CARTESIAN_POINT ( 'NONE',  ( -2.216418498320018582, 16.40908668940205573, -68.78644440154944562 ) ) ;
#63799=CARTESIAN_POINT ( 'NONE',  ( 3.428378827818789443, 68.02396499344450831, -20.38382289158443328 ) ) ;
#63801=CARTESIAN_POINT ( 'NONE',  ( -5.000000000000000000, -53.50647209750557209, -45.02947987234075100 ) ) ;
#63934=UNCERTAINTY_MEASURE_WITH_UNIT (LENGTH_MEASURE( 1.000000000000000082E-05 ), #36657, 'distance_accuracy_value', 'NONE');
#63955=ORIENTED_EDGE ( 'NONE', *, *, #8623, .T. ) ;
#63960=CARTESIAN_POINT ( 'NONE',  ( -14.00000000000000178, 2.249999999994893862, 10.23492587299426404 ) ) ;
#63981=CARTESIAN_POINT ( 'NONE',  ( -1.882291019712000413, -55.75505015263659203, 43.87597576788989073 ) ) ;
#64039=AXIS2_PLACEMENT_3D ( 'NONE', #51724, #69455, #10999 ) ;
#64043=CARTESIAN_POINT ( 'NONE',  ( 4.999999999999999112, -67.66364885638958526, 22.52891795222265259 ) ) ;
#64085=CARTESIAN_POINT ( 'NONE',  ( -2.589639417653167630, 10.27590863719303904, 63.78668228762733605 ) ) ;
#64102=PLANE ( 'NONE',  #42949 ) ;
#64127=CARTESIAN_POINT ( 'NONE',  ( -3.223881452105385570, 10.27322224982961707, -63.89771963198208482 ) ) ;
#64129=TOROIDAL_SURFACE ( 'NONE', #59295, 81.50000000000000000, 10.99999999999999822 ) ;
#64151=DIRECTION ( 'NONE',  ( 0.000000000000000000, 0.8778652960884979484, 0.4789076340208558435 ) ) ;
#64165=CIRCLE ( 'NONE', #36478, 17.50000000000000000 ) ;
#64186=CARTESIAN_POINT ( 'NONE',  ( -0.4369882809994319883, 16.44602605510693749, -68.55492853905478512 ) ) ;
#64203=ORIENTED_EDGE ( 'NONE', *, *, #743, .T. ) ;
#64335=DIRECTION ( 'NONE',  ( 0.000000000000000000, 0.000000000000000000, -1.000000000000000000 ) ) ;
#64364=CARTESIAN_POINT ( 'NONE',  ( 5.000000000000000888, -13.57926339724853904, 69.65188861886710470 ) ) ;
#64368=CARTESIAN_POINT ( 'NONE',  ( 5.000000000000000000, 70.11723469343073134, 28.93519894129288517 ) ) ;
#64417=EDGE_CURVE ( 'NONE', #46951, #30587, #49160, .T. ) ;
#64428=CARTESIAN_POINT ( 'NONE',  ( 0.8588954341814998283, 60.21087566322560747, 22.89167302533804005 ) ) ;
#64443=CARTESIAN_POINT ( 'NONE',  ( -5.000000000000000000, 65.19475225706649724, -23.98307544244871181 ) ) ;
#64461=AXIS2_PLACEMENT_3D ( 'NONE', #33857, #56855, #22494 ) ;
#64473=CARTESIAN_POINT ( 'NONE',  ( 3.496982156819858467, 68.06496700477683248, 20.41687962717103844 ) ) ;
#64501=CARTESIAN_POINT ( 'NONE',  ( -5.086519500888152301, 10.26068667857073358, -64.41585657734927395 ) ) ;
#64513=DIRECTION ( 'NONE',  ( 0.000000000000000000, -0.000000000000000000, 1.000000000000000000 ) ) ;
#64516=DIRECTION ( 'NONE',  ( 0.000000000000000000, 1.000000000000000000, -1.224646799147353207E-16 ) ) ;
#64554=CARTESIAN_POINT ( 'NONE',  ( -4.217983994794729519, 16.30587161610626623, -69.44297314767059959 ) ) ;
#64563=( GEOMETRIC_REPRESENTATION_CONTEXT ( 3 ) GLOBAL_UNCERTAINTY_ASSIGNED_CONTEXT ( ( #63934 ) ) GLOBAL_UNIT_ASSIGNED_CONTEXT ( ( #36657, #37024, #59668 ) ) REPRESENTATION_CONTEXT ( 'NONE', 'WORKASPACE' ) );
#64568=CARTESIAN_POINT ( 'NONE',  ( 4.999999999999688249, 68.48985753891581396, -21.22439692019570856 ) ) ;
#64572=ORIENTED_EDGE ( 'NONE', *, *, #59765, .T. ) ;
#64611=LINE ( 'NONE', #53295, #65943 ) ;
#64704=CARTESIAN_POINT ( 'NONE',  ( 0.000000000000000000, 0.000000000000000000, 0.000000000000000000 ) ) ;
#64722=CARTESIAN_POINT ( 'NONE',  ( 1.296342370383412934, 60.23018777774911570, -22.90345467632036502 ) ) ;
#64800=ADVANCED_FACE ( 'NONE', ( #34742 ), #18437, .F. ) ;
#64803=CARTESIAN_POINT ( 'NONE',  ( -5.000000000000000000, 67.66743717231514665, -22.54291394824878481 ) ) ;
#64830=CARTESIAN_POINT ( 'NONE',  ( 0.6547826978431622313, 60.19560277018798189, 22.88235556323082065 ) ) ;
#64844=EDGE_CURVE ( 'NONE', #72436, #67442, #14693, .T. ) ;
#64859=ORIENTED_EDGE ( 'NONE', *, *, #71893, .F. ) ;
#64860=CARTESIAN_POINT ( 'NONE',  ( 4.465384415997312395, 10.10202268796506608, -70.97396818905025384 ) ) ;
#64862=CIRCLE ( 'NONE', #10695, 5.000000000000000888 ) ;
#64872=DIRECTION ( 'NONE',  ( 0.000000000000000000, 1.000000000000000000, 0.000000000000000000 ) ) ;
#64912=CARTESIAN_POINT ( 'NONE',  ( -2.160335347094679115, 16.41093803200631740, -68.77481055341850436 ) ) ;
#64924=CARTESIAN_POINT ( 'NONE',  ( 4.999999999999997335, 16.24494643555759410, 69.83755725260752456 ) ) ;
#64927=ADVANCED_FACE ( 'NONE', ( #22522, #17241 ), #34997, .T. ) ;
#64995=ORIENTED_EDGE ( 'NONE', *, *, #27403, .T. ) ;
#64997=FACE_OUTER_BOUND ( 'NONE', #30540, .T. ) ;
#65021=CIRCLE ( 'NONE', #8362, 5.000000000000000888 ) ;
#65072=CARTESIAN_POINT ( 'NONE',  ( 2.997005883566935758, 66.06021892606798929, -26.46015439094089672 ) ) ;
#65105=CARTESIAN_POINT ( 'NONE',  ( -0.8761883848934740593, 67.61551161115575326, -20.05282165013490925 ) ) ;
#65127=CARTESIAN_POINT ( 'NONE',  ( -5.000000000000000000, 11.68639849891318327, 68.31608016562505270 ) ) ;
#65138=ORIENTED_EDGE ( 'NONE', *, *, #52915, .F. ) ;
#65161=CARTESIAN_POINT ( 'NONE',  ( -5.000000000000000000, 67.10422270468733075, -23.07049055144695160 ) ) ;
#65255=CARTESIAN_POINT ( 'NONE',  ( 3.407298021510797525, 16.35582233947175013, 69.12343428065700834 ) ) ;
#65277=CARTESIAN_POINT ( 'NONE',  ( 0.8761883848702545219, -67.61551161115382058, -20.05282165013451845 ) ) ;
#65287=CIRCLE ( 'NONE', #21930, 17.50000000000000000 ) ;
#65294=DIRECTION ( 'NONE',  ( 1.000000000000000000, -0.000000000000000000, -0.000000000000000000 ) ) ;
#65299=ORIENTED_EDGE ( 'NONE', *, *, #52077, .F. ) ;
#65307=B_SPLINE_CURVE_WITH_KNOTS ( 'NONE', 3,
 ( #66957, #44694, #20548, #28079, #73365, #4337, #39405, #45066, #16008, #55657, #50344, #39038, #20925, #67710, #62404, #55283, #3587, #62040, #33026, #72621, #4711, #21300 ),
 .UNSPECIFIED., .F., .F.,
 ( 4, 2, 2, 2, 2, 2, 2, 2, 2, 2, 4 ),
 ( 0.000000000000000000, 0.001156727053362482157, 0.001735090580043723235, 0.002313454106724964314, 0.003470181160087444303, 0.004048544686768682996, 0.004626908213449921689, 0.005783635266812366983, 0.006940362320174811410, 0.008097089373537256704, 0.009253816426899701131 ),
 .UNSPECIFIED. ) ;
#65321=ORIENTED_EDGE ( 'NONE', *, *, #70951, .F. ) ;
#65351=DIRECTION ( 'NONE',  ( 0.000000000000000000, 0.000000000000000000, -1.000000000000000000 ) ) ;
#65474=DIRECTION ( 'NONE',  ( 1.000000000000000000, -0.000000000000000000, -0.000000000000000000 ) ) ;
#65504=CARTESIAN_POINT ( 'NONE',  ( 5.000000000000000000, 13.21930962315071767, -69.49101004078873700 ) ) ;
#65602=ORIENTED_EDGE ( 'NONE', *, *, #65768, .F. ) ;
#65615=CARTESIAN_POINT ( 'NONE',  ( -5.000000000000000000, -52.35862550122958936, 48.98731492261398301 ) ) ;
#65671=VECTOR ( 'NONE', #66776, 1000.000000000000000 ) ;
#65748=CARTESIAN_POINT ( 'NONE',  ( -5.126144196591230440, 52.42426806216718660, -49.01287729762170642 ) ) ;
#65766=EDGE_CURVE ( 'NONE', #6205, #74331, #48608, .T. ) ;
#65768=EDGE_CURVE ( 'NONE', #21807, #37240, #13742, .T. ) ;
#65806=CARTESIAN_POINT ( 'NONE',  ( 5.000000000000000000, 16.24494643555759410, -69.83755725260752456 ) ) ;
#65818=CARTESIAN_POINT ( 'NONE',  ( 0.7509181236780181345, 65.76106071587292945, -26.27764834702227859 ) ) ;
#65851=FACE_BOUND ( 'NONE', #27014, .T. ) ;
#65910=CARTESIAN_POINT ( 'NONE',  ( -5.000000000000000000, -50.64189880742087269, -41.08656465431914029 ) ) ;
#65939=CARTESIAN_POINT ( 'NONE',  ( 5.000000000000000000, -16.14408868864072844, 22.96238185062368586 ) ) ;
#65940=CARTESIAN_POINT ( 'NONE',  ( 3.369429374625380724, 50.21921270641779245, 40.85597392306867448 ) ) ;
#65943=VECTOR ( 'NONE', #34850, 1000.000000000000227 ) ;
#65951=CLOSED_SHELL ( 'NONE', ( #5048, #20109, #62756, #2521, #54703, #69827, #4653, #49223, #67920, #50465, #41614, #64927, #32303, #19616, #39133, #63729, #19142, #4995, #15939, #25025, #7971, #38978, #16511, #20620, #37527, #16638, #9312, #9960, #26100, #30013, #3688, #73038, #30098, #64800, #46858, #3745, #9500, #61181, #63380, #71549, #48048, #9091, #14153, #26324, #63000, #9456, #66358, #5417 ) ) ;
#65999=CARTESIAN_POINT ( 'NONE',  ( 4.999999999999997335, 16.24494643555759410, 69.83755725260752456 ) ) ;
#66056=DIRECTION ( 'NONE',  ( 0.000000000000000000, -0.02418647091589873691, 0.9997074645238147594 ) ) ;
#66119=ORIENTED_EDGE ( 'NONE', *, *, #20266, .F. ) ;
#66144=ORIENTED_EDGE ( 'NONE', *, *, #33288, .T. ) ;
#66148=VECTOR ( 'NONE', #10794, 1000.000000000000000 ) ;
#66168=CARTESIAN_POINT ( 'NONE',  ( -4.465349678513701015, -10.10202304668585604, 70.97395336192410298 ) ) ;
#66193=CARTESIAN_POINT ( 'NONE',  ( 2.266287154879886856, 60.33498852648239819, -22.96738997677231353 ) ) ;
#66198=EDGE_CURVE ( 'NONE', #37508, #20547, #68064, .T. ) ;
#66221=ORIENTED_EDGE ( 'NONE', *, *, #67650, .T. ) ;
#66231=CARTESIAN_POINT ( 'NONE',  ( 0.4369882809993350103, 51.14729664189524527, -48.52014062455030086 ) ) ;
#66268=CARTESIAN_POINT ( 'NONE',  ( -5.000000000000001776, -10.42446448370097833, -65.94449134867545581 ) ) ;
#66290=CYLINDRICAL_SURFACE ( 'NONE', #43584, 4.999999999999997335 ) ;
#66305=TOROIDAL_SURFACE ( 'NONE', #41017, 81.50000000000000000, 10.99999999999999822 ) ;
#66315=LINE ( 'NONE', #65939, #55708 ) ;
#66324=VECTOR ( 'NONE', #5780, 1000.000000000000000 ) ;
#66337=CARTESIAN_POINT ( 'NONE',  ( 5.000000000000000888, -13.57248045702109351, -69.64920683919133637 ) ) ;
#66358=ADVANCED_FACE ( 'NONE', ( #72297 ), #19491, .F. ) ;
#66370=CARTESIAN_POINT ( 'NONE',  ( -13.99999999999999822, 0.000000000000000000, 0.000000000000000000 ) ) ;
#66414=AXIS2_PLACEMENT_3D ( 'NONE', #33449, #15690, #33085 ) ;
#66462=CARTESIAN_POINT ( 'NONE',  ( -5.000000000000000000, 0.000000000000000000, 0.000000000000000000 ) ) ;
#66537=CARTESIAN_POINT ( 'NONE',  ( -5.126106709302933773, -16.23426604260537331, 69.90716554746668976 ) ) ;
#66552=ORIENTED_EDGE ( 'NONE', *, *, #50871, .F. ) ;
#66572=CARTESIAN_POINT ( 'NONE',  ( -4.999999999999999112, -61.23691386381970148, 23.51762333030202612 ) ) ;
#66616=ORIENTED_EDGE ( 'NONE', *, *, #27928, .T. ) ;
#66640=CARTESIAN_POINT ( 'NONE',  ( -4.999999999999999112, -14.13320814749881116, -69.81894086168458102 ) ) ;
#66691=CARTESIAN_POINT ( 'NONE',  ( 4.193030820682221105, 50.40097124335105860, 40.95512985425044405 ) ) ;
#66717=CARTESIAN_POINT ( 'NONE',  ( 5.000000000000000000, -10.26105934116143281, -64.40045319026697257 ) ) ;
#66728=ORIENTED_EDGE ( 'NONE', *, *, #70709, .F. ) ;
#66756=ORIENTED_EDGE ( 'NONE', *, *, #20866, .T. ) ;
#66763=CARTESIAN_POINT ( 'NONE',  ( 5.000000000000000000, -70.11723469343094450, -28.93519894129240910 ) ) ;
#66776=DIRECTION ( 'NONE',  ( -0.000000000000000000, -0.000000000000000000, -1.000000000000000000 ) ) ;
#66778=DIRECTION ( 'NONE',  ( 1.000000000000000000, 0.000000000000000000, 0.000000000000000000 ) ) ;
#66916=CARTESIAN_POINT ( 'NONE',  ( 2.726951573962122902E-14, -51.14729664189338365, -48.52014062455057797 ) ) ;
#66932=CARTESIAN_POINT ( 'NONE',  ( -5.000000000000000888, 53.57153130924434237, 46.19535935661121329 ) ) ;
#66957=CARTESIAN_POINT ( 'NONE',  ( -5.000000000000000000, 10.26105934116143281, -64.40045319026697257 ) ) ;
#66987=VECTOR ( 'NONE', #42331, 1000.000000000000000 ) ;
#67013=CARTESIAN_POINT ( 'NONE',  ( -0.3752463838826955445, -65.74564559951674880, -26.26824411939953308 ) ) ;
#67037=CARTESIAN_POINT ( 'NONE',  ( 3.074111742560679872, -51.58078258920428283, 48.68628732315335839 ) ) ;
#67039=CARTESIAN_POINT ( 'NONE',  ( 5.000000000000000000, -60.11723469343085213, -46.25570701698114107 ) ) ;
#67080=CARTESIAN_POINT ( 'NONE',  ( -0.8588954341814966087, 60.21087566322607643, -22.89167302533678594 ) ) ;
#67119=ORIENTED_EDGE ( 'NONE', *, *, #53720, .F. ) ;
#67126=CARTESIAN_POINT ( 'NONE',  ( -5.086519500888726952, -50.65542486323322890, -41.09394361258938488 ) ) ;
#67245=ORIENTED_EDGE ( 'NONE', *, *, #42848, .T. ) ;
#67299=CARTESIAN_POINT ( 'NONE',  ( -3.223881452093011024, -10.27322224982958865, 63.89771963198323590 ) ) ;
#67315=CIRCLE ( 'NONE', #72079, 71.70204102886728492 ) ;
#67330=CARTESIAN_POINT ( 'NONE',  ( -5.000000000000000000, -60.90295814858257017, 23.31388853594792820 ) ) ;
#67377=CARTESIAN_POINT ( 'NONE',  ( 5.000000000000000000, 53.53174224766643619, -46.57871628774325501 ) ) ;
#67388=CARTESIAN_POINT ( 'NONE',  ( 6.891449706534898745, -61.56004288261173230, -23.71475313281752051 ) ) ;
#67395=CARTESIAN_POINT ( 'NONE',  ( -5.000000000000001776, -10.28276986844632290, -65.17752827135417704 ) ) ;
#67414=PLANE ( 'NONE',  #70079 ) ;
#67442=VERTEX_POINT ( 'NONE', #27299 ) ;
#67445=CARTESIAN_POINT ( 'NONE',  ( -1.736494649845418126, -16.42394793108440254, 68.69316892220884085 ) ) ;
#67499=CARTESIAN_POINT ( 'NONE',  ( -2.990854866095042475, -55.96051345248228159, -43.98806351443467832 ) ) ;
#67537=CARTESIAN_POINT ( 'NONE',  ( 1.506680654948082232, 55.70239491600471382, -43.84725041001931345 ) ) ;
#67574=DIRECTION ( 'NONE',  ( 0.000000000000000000, 0.000000000000000000, -1.000000000000000000 ) ) ;
#67604=CARTESIAN_POINT ( 'NONE',  ( -3.369429374625495743, 10.27270496052241278, 63.91910092334656923 ) ) ;
#67621=CARTESIAN_POINT ( 'NONE',  ( 4.999999999999998224, 53.34243969459446078, 47.33397984627243460 ) ) ;
#67628=LINE ( 'NONE', #48767, #29224 ) ;
#67650=EDGE_CURVE ( 'NONE', #17726, #32715, #63312, .T. ) ;
#67671=CARTESIAN_POINT ( 'NONE',  ( 3.728321214185993160, -10.10963409588536521, 70.65936332841438627 ) ) ;
#67692=CARTESIAN_POINT ( 'NONE',  ( 0.8419854211626176532, 10.28111362163632947, -63.57154293063804573 ) ) ;
#67704=CARTESIAN_POINT ( 'NONE',  ( -4.999999999999999112, -61.58609660504387051, 23.68302032025066239 ) ) ;
#67710=CARTESIAN_POINT ( 'NONE',  ( -4.999999999999999112, 12.24343743989404310, -68.85270403949348861 ) ) ;
#67763=CARTESIAN_POINT ( 'NONE',  ( -1.877992804781005276, 55.75022808460100521, 43.87334515336361562 ) ) ;
#67765=CARTESIAN_POINT ( 'NONE',  ( -5.107860025160939621, -60.88642786446133925, -23.30380398316975388 ) ) ;
#67777=EDGE_LOOP ( 'NONE', ( #66552, #4858, #62056, #42439 ) ) ;
#67786=CARTESIAN_POINT ( 'NONE',  ( 0.3794862803132350582, -55.62190996747519023, 43.80334292620691627 ) ) ;
#67791=ORIENTED_EDGE ( 'NONE', *, *, #72173, .T. ) ;
#67814=ORIENTED_EDGE ( 'NONE', *, *, #44067, .F. ) ;
#67866=CARTESIAN_POINT ( 'NONE',  ( 1.558072418983080798, -51.25713184919913346, -48.56213741370739001 ) ) ;
#67905=CARTESIAN_POINT ( 'NONE',  ( 4.330454160156390842, 52.03352386568179355, -48.86100738216495643 ) ) ;
#67920=ADVANCED_FACE ( 'NONE', ( #73400 ), #68114, .F. ) ;
#67970=CARTESIAN_POINT ( 'NONE',  ( 1.704527592502714350, 10.27896685065642934, 63.66027613114050610 ) ) ;
#67983=CARTESIAN_POINT ( 'NONE',  ( -0.6547826978432378375, -60.19560277018450023, 22.88235556322767650 ) ) ;
#67985=CARTESIAN_POINT ( 'NONE',  ( 4.999999999999999112, 53.55923425356063916, 45.42020841079129667 ) ) ;
#68037=B_SPLINE_CURVE_WITH_KNOTS ( 'NONE', 3,
 ( #67330, #66572, #67704, #38667, #3582, #26954, #61669, #25823, #31877, #54900, #37541, #21663, #9988, #72227, #44317, #38289, #56022, #9621, #48842, #32641, #55650, #71850 ),
 .UNSPECIFIED., .F., .F.,
 ( 4, 2, 2, 2, 2, 2, 2, 2, 2, 2, 4 ),
 ( 0.000000000000000000, 0.001156727053362450498, 0.001735090580043667941, 0.002313454106724884950, 0.003470181160087358867, 0.004048544686768596260, 0.004626908213449832351, 0.005783635266812303666, 0.006940362320174774113, 0.008097089373537246296, 0.009253816426899716743 ),
 .UNSPECIFIED. ) ;
#68042=CARTESIAN_POINT ( 'NONE',  ( -5.000000000000000000, 67.53158052529128952, 22.66975313813598092 ) ) ;
#68053=DIRECTION ( 'NONE',  ( -1.000000000000000000, 0.000000000000000000, 0.000000000000000000 ) ) ;
#68060=CARTESIAN_POINT ( 'NONE',  ( -2.589639417659336917, -10.27590863719300707, -63.78668228762852976 ) ) ;
#68064=CIRCLE ( 'NONE', #41566, 8.000000000000000000 ) ;
#68114=PLANE ( 'NONE',  #53687 ) ;
#68119=CARTESIAN_POINT ( 'NONE',  ( 4.999999999999998224, 53.09993190648302175, -43.73864582539177093 ) ) ;
#68126=EDGE_LOOP ( 'NONE', ( #37683, #24310, #37840, #57095, #33282, #63148, #50370, #3696, #62690, #50932, #2037, #36370, #52181, #74426, #24497, #33800 ) ) ;
#68129=CARTESIAN_POINT ( 'NONE',  ( 0.7509181236778168511, 55.63764137817162236, 43.81192498624614728 ) ) ;
#68131=CARTESIAN_POINT ( 'NONE',  ( 4.737866951561470863, -68.48668487056480103, -20.75656675269368634 ) ) ;
#68161=ORIENTED_EDGE ( 'NONE', *, *, #54136, .T. ) ;
#68207=CARTESIAN_POINT ( 'NONE',  ( -5.000000000000001776, -11.69579520003552098, 68.31051037013783400 ) ) ;
#68212=CARTESIAN_POINT ( 'NONE',  ( 5.000000000000000888, -52.35862550122958936, 48.98731492261398301 ) ) ;
#68254=CARTESIAN_POINT ( 'NONE',  ( 0.4501631047671810215, 16.44600848780500257, 68.55503832938671849 ) ) ;
#68300=CARTESIAN_POINT ( 'NONE',  ( -4.104248244564889347, 10.10575198620099613, -70.81982386211636538 ) ) ;
#68356=CARTESIAN_POINT ( 'NONE',  ( -0.8997857291002455682, -67.61674724335095732, 20.05382624916412482 ) ) ;
#68365=CARTESIAN_POINT ( 'NONE',  ( 5.000000000000001776, 10.82431413986196134, 67.03128830763429846 ) ) ;
#68376=CARTESIAN_POINT ( 'NONE',  ( -4.999999999999999112, -68.33088307291099284, -21.57589723056520370 ) ) ;
#68404=CARTESIAN_POINT ( 'NONE',  ( 0.7509181236825389627, -10.12341933770111702, 70.08957333326995354 ) ) ;
#68414=CARTESIAN_POINT ( 'NONE',  ( 5.000000000000000000, 11.14555136602166741, -27.84144949604398889 ) ) ;
#68417=ORIENTED_EDGE ( 'NONE', *, *, #57922, .F. ) ;
#68423=CARTESIAN_POINT ( 'NONE',  ( -4.336811714531204842, -16.30209246798439082, -69.46462972172992067 ) ) ;
#68431=CARTESIAN_POINT ( 'NONE',  ( 0.8588954341815085991, -49.93020820668212423, 40.69831139579102341 ) ) ;
#68493=VECTOR ( 'NONE', #29821, 999.9999999999998863 ) ;
#68496=FACE_OUTER_BOUND ( 'NONE', #6000, .T. ) ;
#68506=LINE ( 'NONE', #74539, #38437 ) ;
#68520=CARTESIAN_POINT ( 'NONE',  ( -2.620431783929977332, 65.99617417813112752, -26.42108291243877005 ) ) ;
#68528=CARTESIAN_POINT ( 'NONE',  ( 5.000000000000000000, -60.11723469343116477, 46.25570701698070764 ) ) ;
#68546=DIRECTION ( 'NONE',  ( -1.000000000000000000, -0.000000000000000000, -0.000000000000000000 ) ) ;
#68556=CARTESIAN_POINT ( 'NONE',  ( -2.995737153982850121, -16.37687539610413978, 68.98994273414959366 ) ) ;
#68638=ORIENTED_EDGE ( 'NONE', *, *, #18166, .F. ) ;
#68643=DIRECTION ( 'NONE',  ( 0.000000000000000000, 0.000000000000000000, -1.000000000000000000 ) ) ;
#68648=DIRECTION ( 'NONE',  ( 0.000000000000000000, 0.000000000000000000, 1.000000000000000000 ) ) ;
#68678=DIRECTION ( 'NONE',  ( 0.000000000000000000, 0.8536788251726059595, -0.5207998305029671871 ) ) ;
#68732=B_SPLINE_CURVE_WITH_KNOTS ( 'NONE', 3,
 ( #25803, #14483, #55628, #32238, #2813, #37522, #8847, #50319, #10339, #55999, #55255, #44669, #60895, #72594, #31857, #66932, #4313, #3562, #32999, #20147, #61272, #20519 ),
 .UNSPECIFIED., .F., .F.,
 ( 4, 2, 2, 2, 2, 2, 2, 2, 2, 2, 4 ),
 ( 0.000000000000000000, 0.001156727053362453534, 0.001735090580043679217, 0.002313454106724904466, 0.003470181160087371444, 0.004048544686768605801, 0.004626908213449840157, 0.005783635266812312339, 0.006940362320174783654, 0.008097089373537254969, 0.009253816426899728886 ),
 .UNSPECIFIED. ) ;
#68734=CARTESIAN_POINT ( 'NONE',  ( 5.000000000000001776, 11.69579520003552098, 68.31051037013783400 ) ) ;
#68744=CARTESIAN_POINT ( 'NONE',  ( -4.999999999999999112, -68.48985753891567185, -21.22439692019679569 ) ) ;
#68776=CARTESIAN_POINT ( 'NONE',  ( -0.7581620860253960315, -10.12340554704839946, 70.09014334689044290 ) ) ;
#68778=CARTESIAN_POINT ( 'NONE',  ( -5.000000000000000000, 62.32183698944580641, 23.94439461060463259 ) ) ;
#68807=CARTESIAN_POINT ( 'NONE',  ( 1.688721909672341148, -49.97488762307337851, -40.72268565194301715 ) ) ;
#68862=CARTESIAN_POINT ( 'NONE',  ( -1.704527592502764755, -10.27896685065642934, 63.66027613114052031 ) ) ;
#68870=CARTESIAN_POINT ( 'NONE',  ( 1.780377099649100625, 51.29164421682855846, 48.57534666485179287 ) ) ;
#68889=CARTESIAN_POINT ( 'NONE',  ( 4.999999999999999112, -65.00653492603730399, -24.02639942437835074 ) ) ;
#68894=CARTESIAN_POINT ( 'NONE',  ( -2.436599634633485945, -51.42120007173235763, 48.62500384162273548 ) ) ;
#68932=ORIENTED_EDGE ( 'NONE', *, *, #72935, .T. ) ;
#68992=CARTESIAN_POINT ( 'NONE',  ( -3.107148544787702027E-14, -51.14729664189371761, 48.52014062455021559 ) ) ;
#69000=CARTESIAN_POINT ( 'NONE',  ( -7.456209740496428928, 10.23501300384517876, 65.47703513267222775 ) ) ;
#69026=DIRECTION ( 'NONE',  ( -1.000000000000000000, 0.000000000000000000, 0.000000000000000000 ) ) ;
#69045=VERTEX_POINT ( 'NONE', #60400 ) ;
#69062=VECTOR ( 'NONE', #48780, 1000.000000000000000 ) ;
#69081=CARTESIAN_POINT ( 'NONE',  ( -2.886287813027996254E-11, 51.14729664189304970, 48.52014062455092613 ) ) ;
#69099=CARTESIAN_POINT ( 'NONE',  ( -5.000000000000000000, -52.28182290968042167, -42.43119126381077422 ) ) ;
#69111=CARTESIAN_POINT ( 'NONE',  ( 4.999999999999999112, 12.24343743989404310, 68.85270403949348861 ) ) ;
#69112=CARTESIAN_POINT ( 'NONE',  ( 4.999999999999997335, 68.33088307291130548, -21.57589723056422315 ) ) ;
#69115=ORIENTED_EDGE ( 'NONE', *, *, #28386, .T. ) ;
#69117=EDGE_CURVE ( 'NONE', #6891, #41883, #34433, .T. ) ;
#69124=CARTESIAN_POINT ( 'NONE',  ( -4.999999999999999112, -66.11467145570883019, -23.67355326543064464 ) ) ;
#69153=CARTESIAN_POINT ( 'NONE',  ( 7.456209740496333005, -10.23501300384517876, 65.47703513267214248 ) ) ;
#69183=CARTESIAN_POINT ( 'NONE',  ( 3.373128826976394823, -50.22031155377536038, 40.85657338450043596 ) ) ;
#69240=CARTESIAN_POINT ( 'NONE',  ( 1.688721909672341814, -10.27943647337372468, 63.64086505882561795 ) ) ;
#69242=CARTESIAN_POINT ( 'NONE',  ( 0.000000000000000000, 0.000000000000000000, 0.000000000000000000 ) ) ;
#69246=CARTESIAN_POINT ( 'NONE',  ( 1.506524674527798480, 55.70638416847562979, 43.84942669317767638 ) ) ;
#69261=EDGE_CURVE ( 'NONE', #57455, #44017, #3833, .T. ) ;
#69269=CARTESIAN_POINT ( 'NONE',  ( -7.456209740496328564, -51.58726928745778650, 41.60229883572996101 ) ) ;
#69277=CARTESIAN_POINT ( 'NONE',  ( -1.347111479062088207E-15, 0.000000000000000000, 0.000000000000000000 ) ) ;
#69292=ORIENTED_EDGE ( 'NONE', *, *, #29605, .T. ) ;
#69358=CARTESIAN_POINT ( 'NONE',  ( -5.000000000000000000, 62.31673578527571777, -23.93255728291310902 ) ) ;
#69389=DIRECTION ( 'NONE',  ( 0.000000000000000000, 0.8778652960885079404, -0.4789076340208374138 ) ) ;
#69392=FACE_OUTER_BOUND ( 'NONE', #24025, .T. ) ;
#69448=EDGE_CURVE ( 'NONE', #22530, #24993, #2622, .T. ) ;
#69455=DIRECTION ( 'NONE',  ( 1.000000000000000000, -0.000000000000000000, -0.000000000000000000 ) ) ;
#69478=DIRECTION ( 'NONE',  ( 0.000000000000000000, 0.000000000000000000, 1.000000000000000000 ) ) ;
#69484=VECTOR ( 'NONE', #4544, 1000.000000000000227 ) ;
#69563=CARTESIAN_POINT ( 'NONE',  ( 5.000000000000000000, 0.000000000000000000, -71.70204102886728492 ) ) ;
#69582=CARTESIAN_POINT ( 'NONE',  ( 5.000000000000001776, 68.60357193678683529, 20.85024232999420946 ) ) ;
#69591=CIRCLE ( 'NONE', #21368, 70.50000000000000000 ) ;
#69642=CARTESIAN_POINT ( 'NONE',  ( -0.8997857291005014746, 67.61674724335088627, -20.05382624916449785 ) ) ;
#69654=CARTESIAN_POINT ( 'NONE',  ( 5.000000000000000000, -11.68639849891297366, 68.31608016562482533 ) ) ;
#69682=ORIENTED_EDGE ( 'NONE', *, *, #41198, .T. ) ;
#69746=CARTESIAN_POINT ( 'NONE',  ( -3.544144923084229681, 10.27124247550373681, 63.97955030411849009 ) ) ;
#69791=CARTESIAN_POINT ( 'NONE',  ( -1.781595147096111775, 16.42277972781688788, -68.70049804031586405 ) ) ;
#69827=ADVANCED_FACE ( 'NONE', ( #339 ), #51620, .T. ) ;
#69852=CARTESIAN_POINT ( 'NONE',  ( -5.000000000000000000, 16.14408868864073554, 27.96238185062412640 ) ) ;
#69877=ORIENTED_EDGE ( 'NONE', *, *, #2226, .T. ) ;
#69917=DIRECTION ( 'NONE',  ( 0.000000000000000000, 0.000000000000000000, -1.000000000000000000 ) ) ;
#69934=ORIENTED_EDGE ( 'NONE', *, *, #11808, .F. ) ;
#69982=B_SPLINE_CURVE_WITH_KNOTS ( 'NONE', 3,
 ( #63427, #74010, #5728, #28727, #22311, #23070, #69099, #17405, #23439, #63060, #28360, #22689, #17031, #63801, #33671, #11755, #74378, #34792, #57796, #6104, #29109, #52128 ),
 .UNSPECIFIED., .F., .F.,
 ( 4, 2, 2, 2, 2, 2, 2, 2, 2, 2, 4 ),
 ( 0.000000000000000000, 0.001156727053362455269, 0.001735090580043697431, 0.002313454106724939594, 0.003470181160087424353, 0.004048544686768665649, 0.004626908213449907811, 0.005783635266812366983, 0.006940362320174827022, 0.008097089373537286194, 0.009253816426899744499 ),
 .UNSPECIFIED. ) ;
#69996=CARTESIAN_POINT ( 'NONE',  ( 2.436599634630141065, 51.42120007173088680, 48.62500384162316180 ) ) ;
#70021=CARTESIAN_POINT ( 'NONE',  ( -3.228176881619886807, -50.21013539027978112, 40.85102191503833069 ) ) ;
#70041=EDGE_LOOP ( 'NONE', ( #29425, #22914, #34900, #65602, #27696 ) ) ;
#70047=CARTESIAN_POINT ( 'NONE',  ( 5.000000000000000000, -50.64189880742116401, 41.08656465431877791 ) ) ;
#70056=B_SPLINE_CURVE_WITH_KNOTS ( 'NONE', 3,
 ( #25199, #66691, #65940, #13866, #20662, #38032, #48212, #49334, #31243, #44060, #20279, #54269 ),
 .UNSPECIFIED., .F., .F.,
 ( 4, 2, 2, 2, 2, 4 ),
 ( 0.000000000000000000, 0.002547658444427994360, 0.005095316888855988720, 0.006369146111069985683, 0.007642975333283983513, 0.01019063377771197744 ),
 .UNSPECIFIED. ) ;
#70079=AXIS2_PLACEMENT_3D ( 'NONE', #67039, #32727, #44031 ) ;
#70080=LINE ( 'NONE', #6338, #45097 ) ;
#70125=CARTESIAN_POINT ( 'NONE',  ( -3.228176881614264193, 10.27295505383825791, 63.90876373295824209 ) ) ;
#70152=AXIS2_PLACEMENT_3D ( 'NONE', #10181, #39224, #29757 ) ;
#70167=CARTESIAN_POINT ( 'NONE',  ( 1.296342370383124054, 10.28012030475506755, -63.61260002839683381 ) ) ;
#70172=EDGE_LOOP ( 'NONE', ( #66119, #62724, #21594, #55614, #20494 ) ) ;
#70181=CARTESIAN_POINT ( 'NONE',  ( 0.000000000000000000, 9.980871413050930352E-15, 81.50000000000000000 ) ) ;
#70233=EDGE_CURVE ( 'NONE', #24993, #74331, #4314, .T. ) ;
#70257=ORIENTED_EDGE ( 'NONE', *, *, #71578, .T. ) ;
#70301=VERTEX_POINT ( 'NONE', #68414 ) ;
#70302=ORIENTED_EDGE ( 'NONE', *, *, #41198, .F. ) ;
#70337=( BOUNDED_SURFACE ( )  B_SPLINE_SURFACE ( 3, 2, ( 
 ( #43350, #12822, #41872 ),
 ( #1540, #24520, #47525 ),
 ( #13186, #36224, #1889 ),
 ( #9034, #67499, #67126 ),
 ( #21828, #73521, #33192 ),
 ( #38086, #61084, #15421 ),
 ( #55441, #62202, #32047 ),
 ( #27126, #44861, #61463 ),
 ( #33559, #56189, #21464 ),
 ( #22203, #9788, #50884 ),
 ( #55818, #61836, #9412 ),
 ( #67866, #16159, #32430 ),
 ( #50141, #39200, #73156 ),
 ( #21094, #4501, #44117 ),
 ( #10527, #44486, #72404 ),
 ( #73898, #3751, #38833 ),
 ( #55067, #3376, #26752 ),
 ( #56563, #14674, #26363 ) ),
 .UNSPECIFIED., .F., .F., .F. ) 
 B_SPLINE_SURFACE_WITH_KNOTS ( ( 4, 2, 2, 2, 2, 2, 2, 2, 4 ),
 ( 3, 3 ),
 ( 0.04202945594032911347, 0.04396162471216782941, 0.04589379348400654535, 0.04782596225584526128, 0.04975813102768398416, 0.05169029979952270704, 0.05265638418544206500, 0.05362246857136142297, 0.05748680611503885485 ),
 ( 0.000000000000000000, 1.000000000000000000 ),
 .UNSPECIFIED. ) 
 GEOMETRIC_REPRESENTATION_ITEM ( )  RATIONAL_B_SPLINE_SURFACE ( (
 ( 1.000000000000000000, 0.6241276099608163985, 1.000000000000000000),
 ( 1.000000000000000000, 0.6218761496797671207, 1.000000000000000000),
 ( 1.000000000000000000, 0.6198047272367630534, 1.000000000000000000),
 ( 1.000000000000000000, 0.6161935119820778350, 1.000000000000000000),
 ( 1.000000000000000000, 0.6146642324080543451, 1.000000000000000000),
 ( 1.000000000000000000, 0.6121850116871440095, 1.000000000000000000),
 ( 1.000000000000000000, 0.6112350889399758014, 1.000000000000000000),
 ( 1.000000000000000000, 0.6099522725972825743, 1.000000000000000000),
 ( 1.000000000000000000, 0.6096208180307998159, 1.000000000000000000),
 ( 1.000000000000000000, 0.6096183796349359252, 1.000000000000000000),
 ( 1.000000000000000000, 0.6099422200100031999, 1.000000000000000000),
 ( 1.000000000000000000, 0.6109087447824246286, 1.000000000000000000),
 ( 1.000000000000000000, 0.6113123981687531572, 1.000000000000000000),
 ( 1.000000000000000000, 0.6122677719810074581, 1.000000000000000000),
 ( 1.000000000000000000, 0.6128199619018938060, 1.000000000000000000),
 ( 1.000000000000000000, 0.6159350830273915278, 1.000000000000000000),
 ( 1.000000000000000000, 0.6195556778509463403, 1.000000000000000000),
 ( 1.000000000000000000, 0.6241278272307889674, 1.000000000000000000) ) ) 
 REPRESENTATION_ITEM ( '' )  SURFACE ( )  );
#70349=ORIENTED_EDGE ( 'NONE', *, *, #62531, .F. ) ;
#70369=CARTESIAN_POINT ( 'NONE',  ( -1.736494649865107265, -67.70200331863352972, 20.12302832235452144 ) ) ;
#70377=CARTESIAN_POINT ( 'NONE',  ( 1.688721909672330934, -60.25432409644731990, 22.91817940688270383 ) ) ;
#70386=CARTESIAN_POINT ( 'NONE',  ( 2.589639417652943365, 60.37884160281038248, -22.99414321703691755 ) ) ;
#70437=ORIENTED_EDGE ( 'NONE', *, *, #3858, .T. ) ;
#70471=CARTESIAN_POINT ( 'NONE',  ( -5.000000000000000000, 62.13136467933009754, -23.87699943806387282 ) ) ;
#70485=CARTESIAN_POINT ( 'NONE',  ( -1.296342370383214426, 10.28012030475506577, 63.61260002839684802 ) ) ;
#70488=CIRCLE ( 'NONE', #64461, 71.70204102886728492 ) ;
#70498=CARTESIAN_POINT ( 'NONE',  ( 1.308779242310877500, 60.23127520339582475, 22.90411807697773128 ) ) ;
#70525=EDGE_CURVE ( 'NONE', #54592, #12328, #54040, .T. ) ;
#70527=CARTESIAN_POINT ( 'NONE',  ( 3.544144923084140864, 10.27124247550373326, -63.97955030411847588 ) ) ;
#70559=CARTESIAN_POINT ( 'NONE',  ( 1.739508062077477657, -16.42388987907938613, 68.69353258878827262 ) ) ;
#70579=ORIENTED_EDGE ( 'NONE', *, *, #54232, .F. ) ;
#70634=CARTESIAN_POINT ( 'NONE',  ( -4.999999999999953815, -52.35862550122923409, -48.98731492261434539 ) ) ;
#70705=CARTESIAN_POINT ( 'NONE',  ( -4.999999999999996447, 18.53862685874492655, -23.57305537018094199 ) ) ;
#70709=EDGE_CURVE ( 'NONE', #16897, #41307, #13796, .T. ) ;
#70725=CARTESIAN_POINT ( 'NONE',  ( -2.584176044324953292, -67.83040087281803210, 20.22720375976441787 ) ) ;
#70732=ORIENTED_EDGE ( 'NONE', *, *, #35899, .F. ) ;
#70778=CARTESIAN_POINT ( 'NONE',  ( -5.000000000000000000, 0.000000000000000000, 0.000000000000000000 ) ) ;
#70795=CARTESIAN_POINT ( 'NONE',  ( 4.999999999999999112, 10.28276986844625718, -65.17752827135362281 ) ) ;
#70833=CARTESIAN_POINT ( 'NONE',  ( -4.999999999999998224, 61.23691386381984358, -23.51762333030159624 ) ) ;
#70850=CARTESIAN_POINT ( 'NONE',  ( -0.4368895104720006417, 67.59332269700051654, 20.03478791450398333 ) ) ;
#70863=CARTESIAN_POINT ( 'NONE',  ( -1.296342370383538389, 60.23018777774547061, 22.90345467631967935 ) ) ;
#70891=CARTESIAN_POINT ( 'NONE',  ( 5.107860025160332995, 10.26152767799288945, -64.38109526790006498 ) ) ;
#70892=VECTOR ( 'NONE', #23631, 1000.000000000000114 ) ;
#70951=EDGE_CURVE ( 'NONE', #72569, #25179, #39150, .T. ) ;
#70956=ORIENTED_EDGE ( 'NONE', *, *, #47948, .T. ) ;
#70975=B_SPLINE_CURVE_WITH_KNOTS ( 'NONE', 3,
 ( #60691, #48984, #24855, #19941, #13529, #13897, #36568, #54298, #43710, #59581, #14274, #25597 ),
 .UNSPECIFIED., .F., .F.,
 ( 4, 2, 2, 2, 2, 4 ),
 ( 2.602085213965210642E-18, 0.002547658444427999564, 0.005095316888855995659, 0.006369146111069992622, 0.007642975333283990452, 0.01019063377771198264 ),
 .UNSPECIFIED. ) ;
#71015=CARTESIAN_POINT ( 'NONE',  ( 2.726951573962122902E-14, -51.14729664189338365, -48.52014062455057797 ) ) ;
#71071=CARTESIAN_POINT ( 'NONE',  ( 4.231687259407054036, -51.96503165405668767, -48.83411696341865849 ) ) ;
#71074=ORIENTED_EDGE ( 'NONE', *, *, #24106, .F. ) ;
#71140=DIRECTION ( 'NONE',  ( 0.000000000000000000, 0.000000000000000000, -1.000000000000000000 ) ) ;
#71154=CARTESIAN_POINT ( 'NONE',  ( 5.000000000000000000, 12.24744670179850203, -68.85644987591957999 ) ) ;
#71213=CARTESIAN_POINT ( 'NONE',  ( 4.999999999999987566, -50.98531617258517912, 41.27391139027606926 ) ) ;
#71217=ORIENTED_EDGE ( 'NONE', *, *, #72173, .F. ) ;
#71218=CARTESIAN_POINT ( 'NONE',  ( -1.506524674528442853, 65.82790954191001731, 26.31843049628531261 ) ) ;
#71227=EDGE_LOOP ( 'NONE', ( #42264, #30096 ) ) ;
#71397=CARTESIAN_POINT ( 'NONE',  ( -1.296342370391298182, 49.95006747298977245, -40.70914535207419505 ) ) ;
#71456=VERTEX_POINT ( 'NONE', #58391 ) ;
#71462=CARTESIAN_POINT ( 'NONE',  ( 6.298842414714822979, -10.24914933418239649, -64.89273347873384523 ) ) ;
#71463=FACE_OUTER_BOUND ( 'NONE', #21684, .T. ) ;
#71489=EDGE_LOOP ( 'NONE', ( #56698, #72064, #62245, #55118 ) ) ;
#71501=DIRECTION ( 'NONE',  ( 1.000000000000000000, -0.000000000000000000, -0.000000000000000000 ) ) ;
#71519=( BOUNDED_SURFACE ( )  B_SPLINE_SURFACE ( 3, 2, ( 
 ( #38732, #56081, #43623 ),
 ( #68131, #39460, #67388 ),
 ( #37980, #26640, #55336 ),
 ( #27759, #20982, #50771 ),
 ( #73417, #8928, #60979 ),
 ( #4026, #3641, #15312 ),
 ( #16426, #32324, #55712 ),
 ( #32703, #9300, #49662 ),
 ( #44006, #16059, #45120 ),
 ( #50031, #67013, #31939 ),
 ( #73785, #4391, #27384 ),
 ( #72678, #73047, #3271 ),
 ( #21354, #26258, #61729 ),
 ( #38348, #21722, #49278 ),
 ( #50403, #22094, #61356 ),
 ( #10048, #44751, #67765 ),
 ( #39093, #62096, #10418 ),
 ( #35304, #40952, #45855 ) ),
 .UNSPECIFIED., .F., .F., .T. ) 
 B_SPLINE_SURFACE_WITH_KNOTS ( ( 4, 2, 2, 2, 2, 2, 2, 2, 4 ),
 ( 3, 3 ),
 ( 0.04202945594032918980, 0.04396162471216789880, 0.04589379348400660086, 0.04782596225584530986, 0.04975813102768401885, 0.05169029979952272785, 0.05265638418544207888, 0.05362246857136143685, 0.05748680611503884791 ),
 ( 0.000000000000000000, 1.000000000000000000 ),
 .UNSPECIFIED. ) 
 GEOMETRIC_REPRESENTATION_ITEM ( )  RATIONAL_B_SPLINE_SURFACE ( (
 ( 1.000000000000000000, 0.6241276099608161765, 1.000000000000000000),
 ( 1.000000000000000000, 0.6218761496801206157, 1.000000000000000000),
 ( 1.000000000000000000, 0.6198047272362935400, 1.000000000000000000),
 ( 1.000000000000000000, 0.6161935119825484586, 1.000000000000000000),
 ( 1.000000000000000000, 0.6146642324081265096, 1.000000000000000000),
 ( 1.000000000000000000, 0.6121850116870731773, 1.000000000000000000),
 ( 1.000000000000000000, 0.6112350889400474108, 1.000000000000000000),
 ( 1.000000000000000000, 0.6099522725972107429, 1.000000000000000000),
 ( 1.000000000000000000, 0.6096208180307641777, 1.000000000000000000),
 ( 1.000000000000000000, 0.6096183796349724515, 1.000000000000000000),
 ( 1.000000000000000000, 0.6099422200101473068, 1.000000000000000000),
 ( 1.000000000000000000, 0.6109087447823515760, 1.000000000000000000),
 ( 1.000000000000000000, 0.6113123981688074471, 1.000000000000000000),
 ( 1.000000000000000000, 0.6122677719809533903, 1.000000000000000000),
 ( 1.000000000000000000, 0.6128199619020369138, 1.000000000000000000),
 ( 1.000000000000000000, 0.6159350830268177646, 1.000000000000000000),
 ( 1.000000000000000000, 0.6195556778513775509, 1.000000000000000000),
 ( 1.000000000000000000, 0.6241278272307890784, 1.000000000000000000) ) ) 
 REPRESENTATION_ITEM ( '' )  SURFACE ( )  );
#71522=VERTEX_POINT ( 'NONE', #314 ) ;
#71535=AXIS2_PLACEMENT_3D ( 'NONE', #50375, #10026, #16037 ) ;
#71549=ADVANCED_FACE ( 'NONE', ( #47040 ), #74607, .F. ) ;
#71554=EDGE_CURVE ( 'NONE', #3989, #22076, #58122, .T. ) ;
#71578=EDGE_CURVE ( 'NONE', #40213, #38797, #11337, .T. ) ;
#71773=CARTESIAN_POINT ( 'NONE',  ( 0.6547826978327068170, 49.91450260127339078, -40.68974341348084778 ) ) ;
#71774=DIRECTION ( 'NONE',  ( 0.000000000000000000, 0.8536788251725985210, 0.5207998305029790664 ) ) ;
#71814=CARTESIAN_POINT ( 'NONE',  ( 2.170320029210518253, -51.35721532638415709, -48.60044191894306920 ) ) ;
#71825=B_SPLINE_CURVE_WITH_KNOTS ( 'NONE', 3,
 ( #74550, #17575, #12650, #5159, #23607, #11922, #40219, #22859, #45875, #35324, #23237, #68889, #995, #74173, #58336, #34207, #56838, #6640, #52659, #18323, #57969, #51916 ),
 .UNSPECIFIED., .F., .F.,
 ( 4, 2, 2, 2, 2, 2, 2, 2, 2, 2, 4 ),
 ( 0.000000000000000000, 0.001156727053362399758, 0.001735090580043607876, 0.002313454106724815995, 0.003470181160087273432, 0.004048544686768501717, 0.004626908213449730869, 0.005783635266812230807, 0.006940362320174731613, 0.008097089373537232418, 0.009253816426899732356 ),
 .UNSPECIFIED. ) ;
#71837=CARTESIAN_POINT ( 'NONE',  ( 2.990854866087931718, -10.11452374054218417, -70.45725801587312276 ) ) ;
#71843=CARTESIAN_POINT ( 'NONE',  ( 2.069125466538116243, 65.90280720052993502, -26.36412295902648850 ) ) ;
#71850=CARTESIAN_POINT ( 'NONE',  ( -4.999999999999952927, -68.60357193678709109, 20.85024232999324667 ) ) ;
#71880=CARTESIAN_POINT ( 'NONE',  ( 2.995737153994495916, 51.55860531535900293, -48.67776149471415437 ) ) ;
#71883=EDGE_CURVE ( 'NONE', #37723, #13141, #70488, .T. ) ;
#71893=EDGE_CURVE ( 'NONE', #56676, #57455, #28446, .T. ) ;
#71938=LINE ( 'NONE', #54613, #20672 ) ;
#72019=FACE_OUTER_BOUND ( 'NONE', #27377, .T. ) ;
#72032=CARTESIAN_POINT ( 'NONE',  ( -5.000000000000000000, -68.60357193678697740, -20.85024232999374050 ) ) ;
#72064=ORIENTED_EDGE ( 'NONE', *, *, #24957, .F. ) ;
#72079=AXIS2_PLACEMENT_3D ( 'NONE', #28939, #18733, #35362 ) ;
#72138=ORIENTED_EDGE ( 'NONE', *, *, #3142, .F. ) ;
#72141=CARTESIAN_POINT ( 'NONE',  ( -5.000000000000002665, 0.000000000000000000, -17.50000000000000000 ) ) ;
#72156=VERTEX_POINT ( 'NONE', #30400 ) ;
#72167=CARTESIAN_POINT ( 'NONE',  ( 5.000000000000000000, -11.14555136602166208, 27.84144949604419139 ) ) ;
#72173=EDGE_CURVE ( 'NONE', #28093, #4661, #65307, .T. ) ;
#72181=ORIENTED_EDGE ( 'NONE', *, *, #54912, .F. ) ;
#72190=CARTESIAN_POINT ( 'NONE',  ( 0.8721677472748814441, -51.17354301023269159, -48.53016177276447252 ) ) ;
#72227=CARTESIAN_POINT ( 'NONE',  ( -5.000000000000000888, -65.74990953739990118, 23.82322416715286906 ) ) ;
#72267=B_SPLINE_CURVE_WITH_KNOTS ( 'NONE', 3,
 ( #39704, #68744, #68376, #45730, #62704, #11043, #115, #23094, #46105, #69124, #17429, #17058, #5382, #17806, #34073, #6128, #40453, #63452, #63085, #51024 ),
 .UNSPECIFIED., .F., .F.,
 ( 4, 2, 2, 2, 2, 2, 2, 2, 2, 4 ),
 ( 0.000000000000000000, 0.001156441540184011043, 0.001734662310276010276, 0.002312883080368009509, 0.003469324620552014914, 0.004625766160736019886, 0.005782207700920026158, 0.006938649241104030696, 0.008095090781288035234, 0.009251532321472039772 ),
 .UNSPECIFIED. ) ;
#72269=CARTESIAN_POINT ( 'NONE',  ( 13.99999999999999822, 0.000000000000000000, 17.50000000000000000 ) ) ;
#72297=FACE_OUTER_BOUND ( 'NONE', #4038, .T. ) ;
#72322=CARTESIAN_POINT ( 'NONE',  ( 5.000000000000000000, 18.53862685874501537, 23.57305537018163477 ) ) ;
#72341=CARTESIAN_POINT ( 'NONE',  ( 4.999999999999999112, -53.31073972600200506, 44.28411094575963602 ) ) ;
#72350=CARTESIAN_POINT ( 'NONE',  ( 5.000000000000000000, 66.10919140997964405, 23.67639547906079400 ) ) ;
#72404=CARTESIAN_POINT ( 'NONE',  ( 3.544144923083023979, -50.27229464832290518, -40.88493206427763482 ) ) ;
#72420=CARTESIAN_POINT ( 'NONE',  ( -1.739508062077480988, -67.70228923712446090, -20.12326043015357868 ) ) ;
#72431=STYLED_ITEM('',(#74692),#17160);
#72433=CARTESIAN_POINT ( 'NONE',  ( 2.584176044310537712, -67.83040087281474939, -20.22720375976230756 ) ) ;
#72436=VERTEX_POINT ( 'NONE', #53973 ) ;
#72439=FACE_OUTER_BOUND ( 'NONE', #10596, .T. ) ;
#72456=ORIENTED_EDGE ( 'NONE', *, *, #58337, .T. ) ;
#72506=LINE ( 'NONE', #14398, #29846 ) ;
#72508=AXIS2_PLACEMENT_3D ( 'NONE', #33113, #37636, #21381 ) ;
#72538=CIRCLE ( 'NONE', #61711, 71.70204102886728492 ) ;
#72556=AXIS2_PLACEMENT_3D ( 'NONE', #36462, #59476, #71140 ) ;
#72569=VERTEX_POINT ( 'NONE', #31322 ) ;
#72594=CARTESIAN_POINT ( 'NONE',  ( -5.000000000000000000, 53.50647209750528077, 45.02947987234111338 ) ) ;
#72604=EDGE_CURVE ( 'NONE', #54592, #46734, #61491, .T. ) ;
#72621=CARTESIAN_POINT ( 'NONE',  ( -4.999999999999999112, 15.47455834364811622, -69.96446835377025764 ) ) ;
#72660=ORIENTED_EDGE ( 'NONE', *, *, #15001, .T. ) ;
#72664=CARTESIAN_POINT ( 'NONE',  ( 5.000000000000000000, 52.85372778481389133, -48.38359481482837765 ) ) ;
#72678=CARTESIAN_POINT ( 'NONE',  ( -1.558072418983381668, -67.68461058694114740, -20.10890959968054048 ) ) ;
#72685=CARTESIAN_POINT ( 'NONE',  ( -5.000000000000000888, -11.68639849891318683, -68.31608016562505270 ) ) ;
#72711=ORIENTED_EDGE ( 'NONE', *, *, #41704, .F. ) ;
#72712=CARTESIAN_POINT ( 'NONE',  ( 4.999999999999995559, -15.86406185656353429, 69.92615499037644611 ) ) ;
#72724=CARTESIAN_POINT ( 'NONE',  ( 5.000000000000000000, -53.53174224766610223, 46.57871628774361739 ) ) ;
#72732=CARTESIAN_POINT ( 'NONE',  ( 5.000000000000000000, 63.84827628760491791, 24.15557308422392069 ) ) ;
#72830=VERTEX_POINT ( 'NONE', #27152 ) ;
#72935=EDGE_CURVE ( 'NONE', #35502, #2210, #62135, .T. ) ;
#73008=ORIENTED_EDGE ( 'NONE', *, *, #63735, .F. ) ;
#73038=ADVANCED_FACE ( 'NONE', ( #40712 ), #46308, .F. ) ;
#73047=CARTESIAN_POINT ( 'NONE',  ( -1.317228840344807583, -65.80815776305057341, -26.30638062134362443 ) ) ;
#73052=CARTESIAN_POINT ( 'NONE',  ( -5.000000000000000888, -11.43937387734372990, -68.01947305042943981 ) ) ;
#73068=CARTESIAN_POINT ( 'NONE',  ( 0.7581620860263087458, -55.63814191976401702, 43.81219804999812339 ) ) ;
#73091=VECTOR ( 'NONE', #18078, 1000.000000000000000 ) ;
#73100=DIRECTION ( 'NONE',  ( 1.000000000000000000, 0.000000000000000000, 0.000000000000000000 ) ) ;
#73149=ORIENTED_EDGE ( 'NONE', *, *, #51567, .F. ) ;
#73156=CARTESIAN_POINT ( 'NONE',  ( 2.589639417653723186, -50.10293296561477661, -40.79253907059064232 ) ) ;
#73172=CARTESIAN_POINT ( 'NONE',  ( 2.990854866096223752, 10.11452374054098335, 70.45725801588044135 ) ) ;
#73185=CYLINDRICAL_SURFACE ( 'NONE', #9927, 8.000000000000000000 ) ;
#73219=AXIS2_PLACEMENT_3D ( 'NONE', #43366, #53959, #2272 ) ;
#73261=CARTESIAN_POINT ( 'NONE',  ( 0.8588954341814317717, 10.28066745654381542, 63.58998442112849858 ) ) ;
#73331=CARTESIAN_POINT ( 'NONE',  ( -5.000000000000000000, 61.58678017309354402, 23.68362420833388171 ) ) ;
#73342=LINE ( 'NONE', #9971, #61613 ) ;
#73344=CIRCLE ( 'NONE', #21525, 71.70204102886728492 ) ;
#73347=CARTESIAN_POINT ( 'NONE',  ( -4.465384415997257328, -10.10202268796506431, -70.97396818905022542 ) ) ;
#73365=CARTESIAN_POINT ( 'NONE',  ( -5.000000000000000000, 10.43216530810821219, -65.93415491242824089 ) ) ;
#73400=FACE_OUTER_BOUND ( 'NONE', #2129, .T. ) ;
#73405=CARTESIAN_POINT ( 'NONE',  ( 5.000000000000000000, 52.35862550122993042, -48.98731492261362064 ) ) ;
#73417=CARTESIAN_POINT ( 'NONE',  ( 3.074111742569078043, -67.95395293240328272, -20.32712440775801710 ) ) ;
#73461=CARTESIAN_POINT ( 'NONE',  ( 5.000000000000000888, -51.88457047716737947, 42.00159762951442843 ) ) ;
#73468=CARTESIAN_POINT ( 'NONE',  ( -4.217983994790210467, -16.30587161610658598, 69.44297314766851059 ) ) ;
#73473=ORIENTED_EDGE ( 'NONE', *, *, #27928, .F. ) ;
#73508=CARTESIAN_POINT ( 'NONE',  ( 0.000000000000000000, 0.000000000000000000, 0.000000000000000000 ) ) ;
#73521=CARTESIAN_POINT ( 'NONE',  ( -2.620431783930857073, -55.87941608673560978, -43.94382193462958952 ) ) ;
#73547=PLANE ( 'NONE',  #70152 ) ;
#73561=CARTESIAN_POINT ( 'NONE',  ( -1.506524674531526609, 55.70638416847363317, -43.84942669317677399 ) ) ;
#73629=CARTESIAN_POINT ( 'NONE',  ( 3.373128826976369066, 10.27267468567300135, 63.92035228378879452 ) ) ;
#73640=CARTESIAN_POINT ( 'NONE',  ( -5.000000000000000000, 52.35862550122993042, -48.98731492261362064 ) ) ;
#73642=CARTESIAN_POINT ( 'NONE',  ( 6.308070865160535057, -61.28915309311908288, 23.54949267151385683 ) ) ;
#73674=APPLICATION_CONTEXT ( 'automotive_design' ) ;
#73713=CARTESIAN_POINT ( 'NONE',  ( -0.8912353796373386761, -16.44139524822816867, -68.58382889509265112 ) ) ;
#73751=CIRCLE ( 'NONE', #35205, 5.000000000000000000 ) ;
#73767=EDGE_CURVE ( 'NONE', #45708, #53358, #58919, .T. ) ;
#73783=CARTESIAN_POINT ( 'NONE',  ( -0.6547826978426952715, 49.91450260127079019, 40.68974341348092594 ) ) ;
#73785=CARTESIAN_POINT ( 'NONE',  ( -0.8912353796317742383, -67.61603573606902273, -20.05324848892005818 ) ) ;
#73790=CARTESIAN_POINT ( 'NONE',  ( 5.000000000000000000, -52.16438407847132197, -42.28020805311216179 ) ) ;
#73792=CARTESIAN_POINT ( 'NONE',  ( -5.000000000000000000, -13.57926339724869536, -69.65188861886713312 ) ) ;
#73807=CARTESIAN_POINT ( 'NONE',  ( 0.4501631047598074753, -51.14740050676115146, 48.52018030598782161 ) ) ;
#73815=DIRECTION ( 'NONE',  ( 0.000000000000000000, 0.000000000000000000, -1.000000000000000000 ) ) ;
#73835=LINE ( 'NONE', #3411, #44748 ) ;
#73898=CARTESIAN_POINT ( 'NONE',  ( 3.511653767257713277, -51.69076377080163098, -48.72852442694656361 ) ) ;
#73906=AXIS2_PLACEMENT_3D ( 'NONE', #61944, #9149, #16276 ) ;
#73911=CARTESIAN_POINT ( 'NONE',  ( 0.8997857291009798697, 16.44125064681837145, 68.58473395859593325 ) ) ;
#73934=CARTESIAN_POINT ( 'NONE',  ( -7.456209740496333893, 51.58726928745807072, -41.60229883572960574 ) ) ;
#73957=DIRECTION ( 'NONE',  ( -1.000000000000000000, -0.000000000000000000, -0.000000000000000000 ) ) ;
#73958=DIRECTION ( 'NONE',  ( 1.000000000000000000, -0.000000000000000000, -0.000000000000000000 ) ) ;
#73960=CARTESIAN_POINT ( 'NONE',  ( -7.456155213548130156, 10.23501372118544595, -65.47700548260780806 ) ) ;
#73962=EDGE_LOOP ( 'NONE', ( #53289, #72181, #59641, #22701 ) ) ;
#74010=CARTESIAN_POINT ( 'NONE',  ( -5.000000000000000888, -50.98531617258489490, -41.27391139027643874 ) ) ;
#74012=CARTESIAN_POINT ( 'NONE',  ( 0.8912353796318864818, -67.61603573606915063, 20.05324848891959277 ) ) ;
#74066=CARTESIAN_POINT ( 'NONE',  ( 0.8912353796376716319, -16.44139524822715259, 68.58382889509293534 ) ) ;
#74068=CARTESIAN_POINT ( 'NONE',  ( -5.000000000000001776, 68.02455775458903986, 22.06917953199582527 ) ) ;
#74087=CARTESIAN_POINT ( 'NONE',  ( 2.216418498311750085, -16.40908668940260284, -68.78644440154761242 ) ) ;
#74144=CARTESIAN_POINT ( 'NONE',  ( 5.000000000000000000, 51.30314553820254275, -41.49361401976463526 ) ) ;
#74151=ORIENTED_EDGE ( 'NONE', *, *, #6602, .F. ) ;
#74161=CARTESIAN_POINT ( 'NONE',  ( 5.000000000000000000, -53.53067326687862248, -46.58593137613121371 ) ) ;
#74164=CARTESIAN_POINT ( 'NONE',  ( 2.995737153982838574, -16.37687539610413978, -68.98994273414959366 ) ) ;
#74173=CARTESIAN_POINT ( 'NONE',  ( 5.000000000000000000, -65.74990953739971644, -23.82322416715333802 ) ) ;
#74177=CARTESIAN_POINT ( 'NONE',  ( -2.069125466539885050, -55.78340383128265501, 43.89144373685536493 ) ) ;
#74219=VERTEX_POINT ( 'NONE', #69582 ) ;
#74237=CARTESIAN_POINT ( 'NONE',  ( -4.999999999999999112, -14.70234347858786528, 69.93881661156081009 ) ) ;
#74239=CARTESIAN_POINT ( 'NONE',  ( 5.000000000000000000, -65.75515815785553286, 23.82162496270619911 ) ) ;
#74324=VERTEX_POINT ( 'NONE', #7685 ) ;
#74331=VERTEX_POINT ( 'NONE', #59012 ) ;
#74336=VECTOR ( 'NONE', #44221, 1000.000000000000000 ) ;
#74361=ORIENTED_EDGE ( 'NONE', *, *, #32233, .T. ) ;
#74378=CARTESIAN_POINT ( 'NONE',  ( -5.000000000000000000, -53.53174224766578959, -46.57871628774400108 ) ) ;
#74426=ORIENTED_EDGE ( 'NONE', *, *, #61527, .T. ) ;
#74436=CARTESIAN_POINT ( 'NONE',  ( 1.780377099653073225, -16.42166210098330481, 68.70754022607324885 ) ) ;
#74453=CIRCLE ( 'NONE', #34737, 17.50000000000000000 ) ;
#74456=CARTESIAN_POINT ( 'NONE',  ( -3.373128826976392602, 10.27267468567300135, -63.92035228378879452 ) ) ;
#74464=CARTESIAN_POINT ( 'NONE',  ( -1.688721909672337596, -49.97488762307366272, 40.72268565194266188 ) ) ;
#74530=CARTESIAN_POINT ( 'NONE',  ( 0.6474643998345609441, 49.91423208894323693, 40.68959583911007627 ) ) ;
#74539=CARTESIAN_POINT ( 'NONE',  ( 0.000000000000000000, 2.143131898507868248E-15, 17.50000000000000000 ) ) ;
#74546=CARTESIAN_POINT ( 'NONE',  ( -3.373128826976391270, -60.49298623944831377, 23.06377889928812763 ) ) ;
#74550=CARTESIAN_POINT ( 'NONE',  ( 5.000000000000000000, -60.90295814858238543, -23.31388853594834032 ) ) ;
#74554=CARTESIAN_POINT ( 'NONE',  ( -0.6474643998432249026, -49.91423208894380537, 40.68959583910937994 ) ) ;
#74567=CARTESIAN_POINT ( 'NONE',  ( 5.000000000000000000, -12.24744670179850203, 68.85644987591957999 ) ) ;
#74571=LINE ( 'NONE', #64368, #70892 ) ;
#74607=CYLINDRICAL_SURFACE ( 'NONE', #18669, 5.000000000000000000 ) ;
#74612=CARTESIAN_POINT ( 'NONE',  ( 1.739508062057873339, 16.42388987907992970, -68.69353258878480517 ) ) ;
#74615=CARTESIAN_POINT ( 'NONE',  ( 5.000000000000000000, -61.23620218020172246, 23.51718915682053890 ) ) ;
#74627=ORIENTED_EDGE ( 'NONE', *, *, #34510, .F. ) ;
#74686=COLOUR_RGB('Sky Blue',0.24,0.69,0.87);
#74687=FILL_AREA_STYLE_COLOUR('',#74686);
#74688=FILL_AREA_STYLE('',(#74687));
#74689=SURFACE_STYLE_FILL_AREA(#74688);
#74690=SURFACE_SIDE_STYLE('',(#74689));
#74691=SURFACE_STYLE_USAGE(.BOTH.,#74690);
#74692=PRESENTATION_STYLE_ASSIGNMENT((#74691));
ENDSEC;
END-ISO-10303-21;
